ISO-10303-21;
HEADER;
FILE_DESCRIPTION (('STEP AP214'),
    '1' );
FILE_NAME ('barrel.step',
    '2026-10-26T19:46:16',
    ( '' ),
    ( '' ),
    'SwSTEP 2.0',
    'SolidWorks 2025',
    '' );
FILE_SCHEMA (( 'AUTOMOTIVE_DESIGN' ));
ENDSEC;

DATA;
#11=CARTESIAN_POINT ( 'NONE',  ( -2.679491924311222295, 249.1666666734946887, 10.00000000000000178 ) ) ;
#62=CARTESIAN_POINT ( 'NONE',  ( 3.042071309553163960, 237.7604166700806161, -11.35316468749999785 ) ) ;
#71=CARTESIAN_POINT ( 'NONE',  ( -7.320508075688770155, 240.6249999999999716, 7.320508075688774596 ) ) ;
#80=CARTESIAN_POINT ( 'NONE',  ( 2.679491924311234730, 226.4583333333333144, 9.999999999999998224 ) ) ;
#100=CARTESIAN_POINT ( 'NONE',  ( 8.311093377946834337, 262.0312500034139589, -8.311093377946836114 ) ) ;
#136=CARTESIAN_POINT ( 'NONE',  ( -8.660254037844385522, 220.4166666666666856, 5.000000000000004441 ) ) ;
#147=CARTESIAN_POINT ( 'NONE',  ( 5.000000000000004441, 251.6666666666667140, 8.660254037844385522 ) ) ;
#152=CARTESIAN_POINT ( 'NONE',  ( -7.320508075688771932, 234.3750000000000000, -7.320508075688771932 ) ) ;
#153=DIRECTION ( 'NONE',  ( -0.000000000000000000, -1.000000000000000000, -0.000000000000000000 ) ) ;
#235=CARTESIAN_POINT ( 'NONE',  ( 9.832129032723420536, 250.9895833367473017, 5.676582343749996262 ) ) ;
#239=CARTESIAN_POINT ( 'NONE',  ( -9.950350709847000985, 219.9999999999999432, 3.187220239308521386 ) ) ;
#268=CARTESIAN_POINT ( 'NONE',  ( -11.35316468749999785, 244.0104166700806729, -3.042071309553164848 ) ) ;
#297=CARTESIAN_POINT ( 'NONE',  ( -7.320508075688770155, 218.7500000068280031, 7.320508075688774596 ) ) ;
#324=CARTESIAN_POINT ( 'NONE',  ( -5.676582343749992710, 239.7395833367473301, 9.832129032723422313 ) ) ;
#328=CARTESIAN_POINT ( 'NONE',  ( -9.832129032723418760, 243.8020833367473301, -5.676582343749998927 ) ) ;
#337=DIRECTION ( 'NONE',  ( 0.000000000000000000, 0.000000000000000000, -1.000000000000000000 ) ) ;
#369=VECTOR ( 'NONE', #48280, 1000.000000000000000 ) ;
#384=CARTESIAN_POINT ( 'NONE',  ( -10.00000000000000000, 253.1250000068279746, 0.000000000000000000 ) ) ;
#434=CARTESIAN_POINT ( 'NONE',  ( 11.35316468749999963, 236.7187500034139873, -1.390361679473963556E-15 ) ) ;
#469=CARTESIAN_POINT ( 'NONE',  ( 3.042071309553163960, 252.4479166700806729, -11.35316468749999785 ) ) ;
#480=ORIENTED_EDGE ( 'NONE', *, *, #52569, .F. ) ;
#494=CARTESIAN_POINT ( 'NONE',  ( -7.320508075688771932, 262.5000000068279746, -7.320508075688771932 ) ) ;
#518=CARTESIAN_POINT ( 'NONE',  ( 7.320508075688771044, 233.1250000000000284, -7.320508075688771932 ) ) ;
#525=CARTESIAN_POINT ( 'NONE',  ( 1.836970198721029589E-15, 229.3750000068279746, 10.00000000000000000 ) ) ;
#604=CARTESIAN_POINT ( 'NONE',  ( -9.832129032723415207, 244.3229166700806445, 5.676582343750005144 ) ) ;
#614=CARTESIAN_POINT ( 'NONE',  ( -10.99999999999999822, 218.7023502760175973, 0.000000000000000000 ) ) ;
#618=DIRECTION ( 'NONE',  ( -0.000000000000000000, -1.000000000000000000, -0.000000000000000000 ) ) ;
#640=CARTESIAN_POINT ( 'NONE',  ( -5.676582343749992710, 245.0520833367473301, 9.832129032723422313 ) ) ;
#642=ORIENTED_EDGE ( 'NONE', *, *, #30933, .T. ) ;
#670=CARTESIAN_POINT ( 'NONE',  ( 1.836970198721029589E-15, 241.2500000000000284, 10.00000000000000000 ) ) ;
#684=FACE_OUTER_BOUND ( 'NONE', #68235, .T. ) ;
#694=CARTESIAN_POINT ( 'NONE',  ( -6.951808397369817780E-16, 232.6562500034139873, -11.35316468749999963 ) ) ;
#697=CARTESIAN_POINT ( 'NONE',  ( -9.832129032723418760, 238.8020833367473301, -5.676582343749998927 ) ) ;
#753=CARTESIAN_POINT ( 'NONE',  ( 10.00000000000000178, 250.4166666734946887, 2.679491924311222739 ) ) ;
#803=CARTESIAN_POINT ( 'NONE',  ( -3.042071309553159075, 230.2604166700806445, 11.35316468749999963 ) ) ;
#827=CYLINDRICAL_SURFACE ( 'NONE', #62611, 10.00000000000000000 ) ;
#839=CARTESIAN_POINT ( 'NONE',  ( -6.951808397369817780E-16, 247.6562500034140157, -11.35316468749999963 ) ) ;
#862=CARTESIAN_POINT ( 'NONE',  ( -6.123233995736766282E-16, 261.8750000068280315, -10.00000000000000178 ) ) ;
#889=CARTESIAN_POINT ( 'NONE',  ( 2.679491924311225848, 223.5416666666666856, -10.00000000000000000 ) ) ;
#896=CARTESIAN_POINT ( 'NONE',  ( -6.123233995736766282E-16, 226.8750000068279746, -10.00000000000000000 ) ) ;
#959=CARTESIAN_POINT ( 'NONE',  ( 8.660254037844389075, 250.2083333401612890, 4.999999999999997335 ) ) ;
#964=CARTESIAN_POINT ( 'NONE',  ( -6.123233995736766282E-16, 256.8750000068279746, -10.00000000000000000 ) ) ;
#974=CARTESIAN_POINT ( 'NONE',  ( 11.35316468749999963, 251.4062500034139873, -1.390361679473963556E-15 ) ) ;
#987=CARTESIAN_POINT ( 'NONE',  ( -10.99999999999999822, 219.4226497308103774, 0.000000000000000000 ) ) ;
#1001=CARTESIAN_POINT ( 'NONE',  ( -8.660254037844385522, 238.5416666734946318, 5.000000000000004441 ) ) ;
#1003=ORIENTED_EDGE ( 'NONE', *, *, #50615, .F. ) ;
#1007=CARTESIAN_POINT ( 'NONE',  ( 3.042071309553173286, 240.6770833367473017, 11.35316468749999608 ) ) ;
#1017=EDGE_CURVE ( 'NONE', #43392, #29523, #38248, .T. ) ;
#1021=ORIENTED_EDGE ( 'NONE', *, *, #61089, .F. ) ;
#1061=CARTESIAN_POINT ( 'NONE',  ( 9.832129032723420536, 235.9895833367473301, 5.676582343749996262 ) ) ;
#1062=DIRECTION ( 'NONE',  ( -0.000000000000000000, -1.000000000000000000, -0.000000000000000000 ) ) ;
#1066=CARTESIAN_POINT ( 'NONE',  ( -11.35316468749999785, 244.0104166700806729, -3.042071309553164848 ) ) ;
#1118=CARTESIAN_POINT ( 'NONE',  ( 4.999999999999997335, 263.3333333333333712, -8.660254037844387298 ) ) ;
#1121=CARTESIAN_POINT ( 'NONE',  ( 4.999999999999997335, 246.4583333401613174, -8.660254037844387298 ) ) ;
#1136=AXIS2_PLACEMENT_3D ( 'NONE', #60648, #56493, #21766 ) ;
#1168=CARTESIAN_POINT ( 'NONE',  ( -3.042071309553159075, 225.2604166700806161, 11.35316468749999963 ) ) ;
#1205=CARTESIAN_POINT ( 'NONE',  ( 8.311093377946834337, 247.0312500034139873, -8.311093377946836114 ) ) ;
#1210=PLANE ( 'NONE',  #5022 ) ;
#1237=ORIENTED_EDGE ( 'NONE', *, *, #15505, .F. ) ;
#1246=AXIS2_PLACEMENT_3D ( 'NONE', #47272, #48380, #71383 ) ;
#1256=CARTESIAN_POINT ( 'NONE',  ( -10.00000000000000000, 229.7916666666666572, -2.679491924311226292 ) ) ;
#1297=AXIS2_PLACEMENT_3D ( 'NONE', #53284, #8736, #42682 ) ;
#1327=EDGE_LOOP ( 'NONE', ( #36800, #14255 ) ) ;
#1329=EDGE_CURVE ( 'NONE', #9311, #18027, #60342, .T. ) ;
#1341=CARTESIAN_POINT ( 'NONE',  ( 5.676582343749997150, 232.2395833367473301, -9.832129032723418760 ) ) ;
#1376=CARTESIAN_POINT ( 'NONE',  ( -11.35316468749999608, 244.4270833367473017, 3.042071309553173730 ) ) ;
#1394=CARTESIAN_POINT ( 'NONE',  ( 0.000000000000000000, 0.000000000000000000, 0.000000000000000000 ) ) ;
#1432=CARTESIAN_POINT ( 'NONE',  ( 3.042071309553163516, 237.4479166700806729, -11.35316468749999785 ) ) ;
#1437=CARTESIAN_POINT ( 'NONE',  ( -9.832129032723415207, 239.6354166700806445, 5.676582343750005144 ) ) ;
#1489=CARTESIAN_POINT ( 'NONE',  ( 9.999999999999998224, 262.7083333333333144, -2.679491924311229401 ) ) ;
#1492=CARTESIAN_POINT ( 'NONE',  ( 8.660254037844385522, 246.0416666734946318, -5.000000000000003553 ) ) ;
#1539=CARTESIAN_POINT ( 'NONE',  ( 1.836970198721029589E-15, 251.2500000000000284, 10.00000000000000000 ) ) ;
#1541=CARTESIAN_POINT ( 'NONE',  ( 3.042071309553173286, 225.6770833367473017, 11.35316468749999608 ) ) ;
#1547=CARTESIAN_POINT ( 'NONE',  ( -2.679491924311287132, 238.9583333333333997, -9.999999999999968026 ) ) ;
#1576=CARTESIAN_POINT ( 'NONE',  ( 11.35316468749999963, 246.4062500034139873, -1.390361679473963556E-15 ) ) ;
#1578=ORIENTED_EDGE ( 'NONE', *, *, #56098, .T. ) ;
#1583=ORIENTED_EDGE ( 'NONE', *, *, #71237, .T. ) ;
#1622=CARTESIAN_POINT ( 'NONE',  ( 9.999999999999998224, 227.7083333333333144, -2.679491924311229401 ) ) ;
#1647=CARTESIAN_POINT ( 'NONE',  ( 0.000000000000000000, 0.000000000000000000, 0.000000000000000000 ) ) ;
#1659=ORIENTED_EDGE ( 'NONE', *, *, #40654, .T. ) ;
#1695=CARTESIAN_POINT ( 'NONE',  ( 2.679491924311350193, 254.5833333401612606, 9.999999999999930722 ) ) ;
#1706=CARTESIAN_POINT ( 'NONE',  ( 5.676582343749997150, 237.2395833367473301, -9.832129032723418760 ) ) ;
#1711=CARTESIAN_POINT ( 'NONE',  ( -8.660254037844385522, 260.4166666666666856, 5.000000000000004441 ) ) ;
#1715=CARTESIAN_POINT ( 'NONE',  ( 8.660254037844389075, 240.2083333401613174, 4.999999999999997335 ) ) ;
#1738=CARTESIAN_POINT ( 'NONE',  ( -8.311093377946834337, 229.8437500034140157, 8.311093377946837890 ) ) ;
#1786=CARTESIAN_POINT ( 'NONE',  ( -3.042071309553166625, 232.8645833367473017, -11.35316468749999608 ) ) ;
#1789=CARTESIAN_POINT ( 'NONE',  ( -6.951808397369817780E-16, 222.9687500034139873, -11.35316468749999963 ) ) ;
#1817=( BOUNDED_CURVE ( )  B_SPLINE_CURVE ( 2, ( #60506, #33631, #16991, #40018, #8832, #54863, #31843, #72580, #4952, #57005, #54494, #39646, #27951 ),
 .UNSPECIFIED., .F., .F. ) 
 B_SPLINE_CURVE_WITH_KNOTS ( ( 3, 2, 2, 2, 2, 2, 3 ),
 ( 0.1944444444444440034, 0.2037037037037032483, 0.2129629629629625209, 0.2222222222222217658, 0.2314814814814810662, 0.2407407407407403110, 0.2499999999999995837 ),
 .UNSPECIFIED. ) 
 CURVE ( )  GEOMETRIC_REPRESENTATION_ITEM ( )  RATIONAL_B_SPLINE_CURVE ( ( 1.000000000000001554, 0.9659258262890666469, 1.000000000000000000, 0.9659258262890683122, 1.000000000000000000, 0.9659258262890683122, 1.000000000000000000, 0.9659258262890683122, 1.000000000000000000, 0.9659258262890683122, 1.000000000000000000, 0.9659258262890698665, 0.9999999999999984457 ) ) 
 REPRESENTATION_ITEM ( '' )  );
#1821=CARTESIAN_POINT ( 'NONE',  ( 8.660254037844389075, 232.0833333333333428, 4.999999999999997335 ) ) ;
#1843=CARTESIAN_POINT ( 'NONE',  ( 2.679491924311375506, 261.4583333333334281, 9.999999999999916511 ) ) ;
#1846=CARTESIAN_POINT ( 'NONE',  ( 1.836970198721029589E-15, 244.3750000068280031, 10.00000000000000000 ) ) ;
#1852=ORIENTED_EDGE ( 'NONE', *, *, #9486, .F. ) ;
#1882=CARTESIAN_POINT ( 'NONE',  ( -2.679491924311193429, 234.1666666734946034, 10.00000000000001954 ) ) ;
#1890=CARTESIAN_POINT ( 'NONE',  ( -11.35316468749999785, 224.0104166700806161, -3.042071309553164848 ) ) ;
#1899=ORIENTED_EDGE ( 'NONE', *, *, #64384, .F. ) ;
#1900=CYLINDRICAL_SURFACE ( 'NONE', #47044, 10.00000000000000000 ) ;
#1927=CARTESIAN_POINT ( 'NONE',  ( -3.042071309553166181, 242.8645833367473017, -11.35316468749999608 ) ) ;
#1965=EDGE_CURVE ( 'NONE', #29935, #21159, #53818, .T. ) ;
#1974=CARTESIAN_POINT ( 'NONE',  ( 9.999999999999998224, 222.7083333333333428, -2.679491924311229401 ) ) ;
#1983=CARTESIAN_POINT ( 'NONE',  ( -10.00000000000000000, 228.1250000068279746, 0.000000000000000000 ) ) ;
#2058=CARTESIAN_POINT ( 'NONE',  ( -9.832129032723415207, 229.3229166700806729, 5.676582343750005144 ) ) ;
#2062=CARTESIAN_POINT ( 'NONE',  ( 8.660254037844389075, 262.0833333333333144, 4.999999999999997335 ) ) ;
#2091=CARTESIAN_POINT ( 'NONE',  ( -11.35316468749999963, 234.2187500034139873, 0.000000000000000000 ) ) ;
#2105=EDGE_CURVE ( 'NONE', #58601, #16650, #4546, .T. ) ;
#2119=LINE ( 'NONE', #54555, #72362 ) ;
#2145=CARTESIAN_POINT ( 'NONE',  ( 5.676582343750005144, 230.5729166700806729, 9.832129032723416984 ) ) ;
#2149=CARTESIAN_POINT ( 'NONE',  ( 8.311093377946834337, 222.3437500034139589, -8.311093377946836114 ) ) ;
#2155=EDGE_LOOP ( 'NONE', ( #70942, #23548, #36486, #17977 ) ) ;
#2184=EDGE_LOOP ( 'NONE', ( #39855, #1852 ) ) ;
#2191=AXIS2_PLACEMENT_3D ( 'NONE', #17510, #45436, #34523 ) ;
#2208=CARTESIAN_POINT ( 'NONE',  ( 10.00000000000000000, 235.6250000068279746, -1.224646799147353256E-15 ) ) ;
#2257=CARTESIAN_POINT ( 'NONE',  ( -11.35316468749999608, 224.4270833367473017, 3.042071309553173730 ) ) ;
#2290=CARTESIAN_POINT ( 'NONE',  ( 5.676582343750005144, 240.5729166700806445, 9.832129032723416984 ) ) ;
#2342=CARTESIAN_POINT ( 'NONE',  ( -10.00000000000000000, 224.7916666666666288, -2.679491924311226292 ) ) ;
#2360=CYLINDRICAL_SURFACE ( 'NONE', #29807, 19.00000000000001776 ) ;
#2429=CARTESIAN_POINT ( 'NONE',  ( 8.311093377946834337, 227.0312500034140157, -8.311093377946836114 ) ) ;
#2463=CARTESIAN_POINT ( 'NONE',  ( 8.660254037844385522, 221.0416666734946602, -5.000000000000003553 ) ) ;
#2466=CARTESIAN_POINT ( 'NONE',  ( -6.951808397369817780E-16, 232.9687500034139873, -11.35316468749999963 ) ) ;
#2514=AXIS2_PLACEMENT_3D ( 'NONE', #45979, #16928, #68995 ) ;
#2522=CARTESIAN_POINT ( 'NONE',  ( -5.676582343750000703, 228.3854166700806729, -9.832129032723418760 ) ) ;
#2528=CARTESIAN_POINT ( 'NONE',  ( -10.99999999999999822, 218.7023502760175973, 0.000000000000000000 ) ) ;
#2549=DIRECTION ( 'NONE',  ( 0.000000000000000000, 0.000000000000000000, -1.000000000000000000 ) ) ;
#2583=CARTESIAN_POINT ( 'NONE',  ( -9.999999999999998224, 243.3333333401612606, 2.679491924311235618 ) ) ;
#2624=CARTESIAN_POINT ( 'NONE',  ( -7.320508075688771932, 232.5000000068279746, -7.320508075688771932 ) ) ;
#2667=CARTESIAN_POINT ( 'NONE',  ( -8.311093377946836114, 238.2812500034140157, -8.311093377946836114 ) ) ;
#2670=EDGE_CURVE ( 'NONE', #52445, #16856, #18110, .T. ) ;
#2698=VERTEX_POINT ( 'NONE', #9552 ) ;
#2716=CARTESIAN_POINT ( 'NONE',  ( 9.832129032723416984, 252.1354166700806445, -5.676582343750003368 ) ) ;
#2801=CARTESIAN_POINT ( 'NONE',  ( 5.676582343750005144, 230.5729166700806729, 9.832129032723416984 ) ) ;
#2810=LINE ( 'NONE', #30737, #19905 ) ;
#2833=CARTESIAN_POINT ( 'NONE',  ( 11.35316468749999963, 236.5104166700806445, 3.042071309553159519 ) ) ;
#2842=CARTESIAN_POINT ( 'NONE',  ( 1.298305728747444210, 220.0000000000000853, 10.86222807232588394 ) ) ;
#2887=CARTESIAN_POINT ( 'NONE',  ( -9.832129032723415207, 224.3229166700806729, 5.676582343750005144 ) ) ;
#2890=CARTESIAN_POINT ( 'NONE',  ( -5.676582343749992710, 220.0520833367473301, 9.832129032723422313 ) ) ;
#2897=( BOUNDED_CURVE ( )  B_SPLINE_CURVE ( 2, ( #49241, #72256, #26221, #32667, #9646, #27724, #26981, #56047, #20570, #4356, #14904, #73382, #49995 ),
 .UNSPECIFIED., .F., .F. ) 
 B_SPLINE_CURVE_WITH_KNOTS ( ( 3, 2, 2, 2, 2, 2, 3 ),
 ( 0.5833333333333331483, 0.5925925925925923377, 0.6018518518518516380, 0.6111111111111109384, 0.6203703703703702388, 0.6296296296296295392, 0.6388888888888887285 ),
 .UNSPECIFIED. ) 
 CURVE ( )  GEOMETRIC_REPRESENTATION_ITEM ( )  RATIONAL_B_SPLINE_CURVE ( ( 1.000000000000000888, 0.9659258262890675351, 1.000000000000000000, 0.9659258262890683122, 1.000000000000000000, 0.9659258262890683122, 1.000000000000000000, 0.9659258262890683122, 1.000000000000000000, 0.9659258262890683122, 1.000000000000000000, 0.9659258262890687563, 0.9999999999999995559 ) ) 
 REPRESENTATION_ITEM ( '' )  );
#2952=CARTESIAN_POINT ( 'NONE',  ( 7.320508075688776373, 235.0000000068279746, 7.320508075688767491 ) ) ;
#2975=CARTESIAN_POINT ( 'NONE',  ( 9.832129032723416984, 256.8229166700806445, -5.676582343750003368 ) ) ;
#2978=CARTESIAN_POINT ( 'NONE',  ( -3.042071309553166181, 263.1770833367473301, -11.35316468749999608 ) ) ;
#2995=CARTESIAN_POINT ( 'NONE',  ( -6.123233995736766282E-16, 231.8750000068279746, -10.00000000000000000 ) ) ;
#3003=DIRECTION ( 'NONE',  ( 0.000000000000000000, 0.000000000000000000, -1.000000000000000000 ) ) ;
#3041=CARTESIAN_POINT ( 'NONE',  ( -3.042071309553166181, 232.8645833367473017, -11.35316468749999608 ) ) ;
#3091=CARTESIAN_POINT ( 'NONE',  ( 2.085542519210945334E-15, 260.4687500034140157, 11.35316468749999963 ) ) ;
#3116=AXIS2_PLACEMENT_3D ( 'NONE', #32314, #67758, #16051 ) ;
#3177=CARTESIAN_POINT ( 'NONE',  ( 9.832129032723420536, 220.9895833367473301, 5.676582343749996262 ) ) ;
#3182=CARTESIAN_POINT ( 'NONE',  ( 4.999999999999997335, 253.3333333333333428, -8.660254037844387298 ) ) ;
#3190=CARTESIAN_POINT ( 'NONE',  ( 8.660254037844385522, 261.0416666734946602, -5.000000000000003553 ) ) ;
#3211=CARTESIAN_POINT ( 'NONE',  ( 8.311093377946839666, 236.0937500034139589, 8.311093377946830785 ) ) ;
#3233=CARTESIAN_POINT ( 'NONE',  ( 7.320508075688771044, 246.2500000068279746, -7.320508075688771932 ) ) ;
#3267=CARTESIAN_POINT ( 'NONE',  ( 3.042071309553163960, 227.7604166700806445, -11.35316468749999785 ) ) ;
#3302=CARTESIAN_POINT ( 'NONE',  ( 10.00000000000000178, 232.2916666666666856, 2.679491924311222739 ) ) ;
#3328=CARTESIAN_POINT ( 'NONE',  ( -9.999999999999998224, 233.3333333401613174, 2.679491924311235618 ) ) ;
#3347=CARTESIAN_POINT ( 'NONE',  ( -5.676582343750000703, 253.0729166700807014, -9.832129032723418760 ) ) ;
#3414=CARTESIAN_POINT ( 'NONE',  ( 3.042071309553173286, 230.3645833367472733, 11.35316468749999608 ) ) ;
#3433=VERTEX_POINT ( 'NONE', #10472 ) ;
#3461=CARTESIAN_POINT ( 'NONE',  ( 0.000000000000000000, 0.000000000000000000, -19.00000000000000000 ) ) ;
#3464=CARTESIAN_POINT ( 'NONE',  ( 3.042071309553163960, 257.7604166700806445, -11.35316468749999785 ) ) ;
#3497=CARTESIAN_POINT ( 'NONE',  ( 1.836970198721029589E-15, 229.3750000068279746, 10.00000000000000000 ) ) ;
#3505=CARTESIAN_POINT ( 'NONE',  ( -11.35316468749999963, 219.0625000034139873, 0.000000000000000000 ) ) ;
#3554=CARTESIAN_POINT ( 'NONE',  ( -8.660254037844385522, 255.4166666666666856, 5.000000000000004441 ) ) ;
#3634=CARTESIAN_POINT ( 'NONE',  ( -11.35316468749999608, 224.1145833367473301, 3.042071309553173730 ) ) ;
#3637=CARTESIAN_POINT ( 'NONE',  ( -11.35316468749999785, 258.6979166700807014, -3.042071309553164848 ) ) ;
#3672=CARTESIAN_POINT ( 'NONE',  ( -8.660254037844385522, 223.5416666734946602, 5.000000000000004441 ) ) ;
#3673=CARTESIAN_POINT ( 'NONE',  ( 8.311093377946834337, 262.3437500034139589, -8.311093377946836114 ) ) ;
#3703=CARTESIAN_POINT ( 'NONE',  ( 1.836970198721029589E-15, 224.3750000068279746, 10.00000000000000000 ) ) ;
#3724=CARTESIAN_POINT ( 'NONE',  ( 3.042071309553173286, 260.3645833367473301, 11.35316468749999608 ) ) ;
#3728=CARTESIAN_POINT ( 'NONE',  ( -3.042071309553166181, 253.1770833367473017, -11.35316468749999608 ) ) ;
#3752=CARTESIAN_POINT ( 'NONE',  ( 5.676582343750005144, 220.8854166700806445, 9.832129032723416984 ) ) ;
#3791=CARTESIAN_POINT ( 'NONE',  ( 9.832129032723420536, 220.9895833367473301, 5.676582343749996262 ) ) ;
#3845=CARTESIAN_POINT ( 'NONE',  ( -5.676582343749992710, 260.0520833367473301, 9.832129032723422313 ) ) ;
#3892=ORIENTED_EDGE ( 'NONE', *, *, #61089, .T. ) ;
#3937=CARTESIAN_POINT ( 'NONE',  ( -5.000000000000000888, 249.1666666666666856, -8.660254037844387298 ) ) ;
#3961=CYLINDRICAL_SURFACE ( 'NONE', #45557, 10.00000000000000000 ) ;
#4009=ORIENTED_EDGE ( 'NONE', *, *, #48376, .T. ) ;
#4022=CARTESIAN_POINT ( 'NONE',  ( -3.042071309553166181, 262.8645833367473301, -11.35316468749999608 ) ) ;
#4058=CARTESIAN_POINT ( 'NONE',  ( 11.35316468749999963, 261.7187500034140157, -1.390361679473963556E-15 ) ) ;
#4084=CARTESIAN_POINT ( 'NONE',  ( 8.660254037844389075, 225.2083333401613174, 4.999999999999997335 ) ) ;
#4104=CARTESIAN_POINT ( 'NONE',  ( -8.660254037844387298, 257.7083333401612890, -4.999999999999999112 ) ) ;
#4105=CARTESIAN_POINT ( 'NONE',  ( -11.35316468749999963, 258.9062500034140157, 0.000000000000000000 ) ) ;
#4110=CARTESIAN_POINT ( 'NONE',  ( 11.35316468749999963, 256.5104166700807014, 3.042071309553159519 ) ) ;
#4135=CARTESIAN_POINT ( 'NONE',  ( -4.999999999999992895, 235.8333333333333428, 8.660254037844390851 ) ) ;
#4161=DIRECTION ( 'NONE',  ( 0.000000000000000000, 0.000000000000000000, -1.000000000000000000 ) ) ;
#4172=CARTESIAN_POINT ( 'NONE',  ( 3.042071309553173286, 220.3645833367472733, 11.35316468749999608 ) ) ;
#4219=CARTESIAN_POINT ( 'NONE',  ( 11.35316468749999963, 256.7187500034139589, -1.390361679473963556E-15 ) ) ;
#4254=CARTESIAN_POINT ( 'NONE',  ( 3.042071309553173286, 260.3645833367473301, 11.35316468749999608 ) ) ;
#4262=CARTESIAN_POINT ( 'NONE',  ( 9.999999999999998224, 230.8333333401612890, -2.679491924311229401 ) ) ;
#4306=CARTESIAN_POINT ( 'NONE',  ( 5.000000000000004441, 246.6666666666666856, 8.660254037844385522 ) ) ;
#4345=CARTESIAN_POINT ( 'NONE',  ( 2.679491924311350193, 256.4583333333333712, 9.999999999999930722 ) ) ;
#4356=CARTESIAN_POINT ( 'NONE',  ( 7.320508075688776373, 236.8749999999999716, 7.320508075688767491 ) ) ;
#4387=CARTESIAN_POINT ( 'NONE',  ( -8.311093377946836114, 258.2812500034140157, -8.311093377946836114 ) ) ;
#4420=CARTESIAN_POINT ( 'NONE',  ( 11.35316468749999963, 256.7187500034139589, -1.390361679473963556E-15 ) ) ;
#4448=CARTESIAN_POINT ( 'NONE',  ( 7.320508075688776373, 225.0000000068279746, 7.320508075688767491 ) ) ;
#4459=ADVANCED_FACE ( 'NONE', ( #22548 ), #18021, .F. ) ;
#4474=CARTESIAN_POINT ( 'NONE',  ( 11.35316468749999963, 251.1979166700806729, 3.042071309553159519 ) ) ;
#4479=CARTESIAN_POINT ( 'NONE',  ( 8.311093377946839666, 256.0937500034140157, 8.311093377946829008 ) ) ;
#4481=ORIENTED_EDGE ( 'NONE', *, *, #56056, .F. ) ;
#4516=CARTESIAN_POINT ( 'NONE',  ( -2.679491924311150353, 246.0416666666666856, 10.00000000000004441 ) ) ;
#4537=CARTESIAN_POINT ( 'NONE',  ( 1.836970198721029589E-15, 259.3750000068280315, 10.00000000000000000 ) ) ;
#4546=( BOUNDED_CURVE ( )  B_SPLINE_CURVE ( 2, ( #74186, #5170, #68159, #50431, #21753, #56111, #38761, #15345, #51178, #3673, #26671, #55741, #4058, #73816, #49696, #67795, #16458, #27051, #27415, #9711, #4797, #62125, #44781, #73077, #28166, #10449, #45513, #61385, #72709, #32733, #21013, #67420, #15719, #44407, #33853, #56481, #4420, #50063, #21384, #22491, #33479, #38009, #38381, #50804, #62490, #67045, #68529, #44037, #61007, #61761, #16086, #10079, #33117, #73446, #39121, #27791, #22124, #45149, #9333, #39495, #10818, #56851, #32353, #55367, #46631, #70028, #57602, #6287, #63235, #58349, #58709, #29294, #23251, #40607, #34967, #24359, #34222, #52304, #11562, #17964, #7019, #69278, #46259, #12663, #35337, #57984, #5912, #51931, #53043, #63990, #51546, #18336, #640, #28914, #40232, #1376, #47367, #268, #16832, #39859, #23987, #17213, #17589, #22876, #46996, #23622, #69651, #6654, #34595, #62860, #11194, #12304, #63609, #1007, #52671, #40982, #29656, #57224, #41351, #64361, #35694, #30028, #11936, #5536, #28538, #74564, #45889, #68902, #25824, #20167, #31879, #71476, #48843, #2833, #41716, #3211, #19802, #71852, #25084, #43185, #13754, #8488, #42808, #60543, #2091, #19430, #66201, #8122, #64728, #60169, #2466, #59808, #31507, #14132, #59080, #54526, #65080, #25457, #14505, #37544, #48100, #71109, #42441, #24719, #13393, #1738, #48471, #70393, #7390, #7758, #65825, #54902, #8868, #30396, #26199, #18708, #13026, #37167, #36063, #65460, #53415, #47728, #36430, #70752, #19068, #42071, #36798, #59444, #30761, #31125, #53782, #54155, #49603, #33761, #56762, #44690, #43944, #33387, #10362, #33023, #9992, #61672, #39402, #72617, #4707, #15630, #66953, #68076, #66574, #56387, #32262, #5083, #27701, #73728, #10728, #50339, #50712 ),
 .UNSPECIFIED., .F., .F. ) 
 B_SPLINE_CURVE_WITH_KNOTS ( ( 3, 2, 2, 2, 2, 2, 2, 2, 2, 2, 2, 2, 2, 2, 2, 2, 2, 2, 2, 2, 2, 2, 2, 2, 2, 2, 2, 2, 2, 2, 2, 2, 2, 2, 2, 2, 2, 2, 2, 2, 2, 2, 2, 2, 2, 2, 2, 2, 2, 2, 2, 2, 2, 2, 2, 2, 2, 2, 2, 2, 2, 2, 2, 2, 2, 2, 2, 2, 2, 2, 2, 2, 2, 2, 2, 2, 2, 2, 2, 2, 2, 2, 2, 2, 2, 2, 2, 2, 2, 2, 2, 2, 2, 2, 2, 2, 2, 2, 2, 2, 2, 2, 2, 2, 2, 2, 2, 2, 3 ),
 ( 0.000000000000000000, 0.009259259259259258745, 0.01851851851851851749, 0.02777777777777777624, 0.03703703703703703498, 0.04629629629629629373, 0.05555555555555555247, 0.06481481481481481122, 0.07407407407407406996, 0.08333333333333332871, 0.09259259259259258745, 0.1018518518518518462, 0.1111111111111111049, 0.1203703703703703637, 0.1296296296296296224, 0.1388888888888888951, 0.1481481481481481399, 0.1574074074074074125, 0.1666666666666666574, 0.1759259259259259300, 0.1851851851851851749, 0.1944444444444444475, 0.2037037037037036924, 0.2129629629629629650, 0.2222222222222222099, 0.2314814814814814825, 0.2407407407407407274, 0.2500000000000000000, 0.2592592592592592449, 0.2685185185185185452, 0.2777777777777777901, 0.2870370370370370350, 0.2962962962962962798, 0.3055555555555555802, 0.3148148148148148251, 0.3240740740740740700, 0.3333333333333333148, 0.3425925925925926152, 0.3518518518518518601, 0.3611111111111111049, 0.3703703703703703498, 0.3796296296296296502, 0.3888888888888888951, 0.3981481481481481399, 0.4074074074074073848, 0.4166666666666666852, 0.4259259259259259300, 0.4351851851851851749, 0.4444444444444444198, 0.4537037037037037202, 0.4629629629629629650, 0.4722222222222222099, 0.4814814814814814548, 0.4907407407407407551, 0.5000000000000000000, 0.5092592592592593004, 0.5185185185185184897, 0.5277777777777777901, 0.5370370370370370905, 0.5462962962962962798, 0.5555555555555555802, 0.5648148148148147696, 0.5740740740740740700, 0.5833333333333333703, 0.5925925925925925597, 0.6018518518518518601, 0.6111111111111111605, 0.6203703703703703498, 0.6296296296296296502, 0.6388888888888888395, 0.6481481481481481399, 0.6574074074074074403, 0.6666666666666666297, 0.6759259259259259300, 0.6851851851851852304, 0.6944444444444444198, 0.7037037037037037202, 0.7129629629629629095, 0.7222222222222222099, 0.7314814814814815103, 0.7407407407407406996, 0.7500000000000000000, 0.7592592592592593004, 0.7685185185185184897, 0.7777777777777777901, 0.7870370370370370905, 0.7962962962962962798, 0.8055555555555555802, 0.8148148148148147696, 0.8240740740740740700, 0.8333333333333333703, 0.8425925925925925597, 0.8518518518518518601, 0.8611111111111111605, 0.8703703703703703498, 0.8796296296296296502, 0.8888888888888888395, 0.8981481481481481399, 0.9074074074074074403, 0.9166666666666666297, 0.9259259259259259300, 0.9351851851851852304, 0.9444444444444444198, 0.9537037037037037202, 0.9629629629629629095, 0.9722222222222222099, 0.9814814814814815103, 0.9907407407407406996, 1.000000000000000000 ),
 .UNSPECIFIED. ) 
 CURVE ( )  GEOMETRIC_REPRESENTATION_ITEM ( )  RATIONAL_B_SPLINE_CURVE ( ( 1.000000000000000000, 0.9659258262890683122, 1.000000000000000000, 0.9659258262890683122, 1.000000000000000000, 0.9659258262890683122, 1.000000000000000000, 0.9659258262890683122, 1.000000000000000000, 0.9659258262890683122, 1.000000000000000000, 0.9659258262890683122, 1.000000000000000000, 0.9659258262890683122, 1.000000000000000000, 0.9659258262890683122, 1.000000000000000000, 0.9659258262890683122, 1.000000000000000000, 0.9659258262890683122, 1.000000000000000000, 0.9659258262890683122, 1.000000000000000000, 0.9659258262890683122, 1.000000000000000000, 0.9659258262890683122, 1.000000000000000000, 0.9659258262890683122, 1.000000000000000000, 0.9659258262890683122, 1.000000000000000000, 0.9659258262890683122, 1.000000000000000000, 0.9659258262890683122, 1.000000000000000000, 0.9659258262890683122, 1.000000000000000000, 0.9659258262890683122, 1.000000000000000000, 0.9659258262890683122, 1.000000000000000000, 0.9659258262890683122, 1.000000000000000000, 0.9659258262890683122, 1.000000000000000000, 0.9659258262890683122, 1.000000000000000000, 0.9659258262890683122, 1.000000000000000000, 0.9659258262890683122, 1.000000000000000000, 0.9659258262890683122, 1.000000000000000000, 0.9659258262890683122, 1.000000000000000000, 0.9659258262890683122, 1.000000000000000000, 0.9659258262890683122, 1.000000000000000000, 0.9659258262890683122, 1.000000000000000000, 0.9659258262890683122, 1.000000000000000000, 0.9659258262890683122, 1.000000000000000000, 0.9659258262890683122, 1.000000000000000000, 0.9659258262890683122, 1.000000000000000000, 0.9659258262890683122, 1.000000000000000000, 0.9659258262890683122, 1.000000000000000000, 0.9659258262890683122, 1.000000000000000000, 0.9659258262890683122, 1.000000000000000000, 0.9659258262890683122, 1.000000000000000000, 0.9659258262890683122, 1.000000000000000000, 0.9659258262890683122, 1.000000000000000000, 0.9659258262890683122, 1.000000000000000000, 0.9659258262890683122, 1.000000000000000000, 0.9659258262890683122, 1.000000000000000000, 0.9659258262890683122, 1.000000000000000000, 0.9659258262890683122, 1.000000000000000000, 0.9659258262890683122, 1.000000000000000000, 0.9659258262890683122, 1.000000000000000000, 0.9659258262890683122, 1.000000000000000000, 0.9659258262890683122, 1.000000000000000000, 0.9659258262890683122, 1.000000000000000000, 0.9659258262890683122, 1.000000000000000000, 0.9659258262890683122, 1.000000000000000000, 0.9659258262890683122, 1.000000000000000000, 0.9659258262890683122, 1.000000000000000000, 0.9659258262890683122, 1.000000000000000000, 0.9659258262890683122, 1.000000000000000000, 0.9659258262890683122, 1.000000000000000000, 0.9659258262890683122, 1.000000000000000000, 0.9659258262890683122, 1.000000000000000000, 0.9659258262890683122, 1.000000000000000000, 0.9659258262890683122, 1.000000000000000000, 0.9659258262890683122, 1.000000000000000000, 0.9659258262890683122, 1.000000000000000000, 0.9659258262890683122, 1.000000000000000000, 0.9659258262890683122, 1.000000000000000000, 0.9659258262890683122, 1.000000000000000000, 0.9659258262890683122, 1.000000000000000000, 0.9659258262890683122, 1.000000000000000000, 0.9659258262890683122, 1.000000000000000000, 0.9659258262890683122, 1.000000000000000000, 0.9659258262890683122, 1.000000000000000000, 0.9659258262890683122, 1.000000000000000000, 0.9659258262890683122, 1.000000000000000000, 0.9659258262890683122, 1.000000000000000000, 0.9659258262890683122, 1.000000000000000000, 0.9659258262890683122, 1.000000000000000000, 0.9659258262890683122, 1.000000000000000000, 0.9659258262890683122, 1.000000000000000000, 0.9659258262890683122, 1.000000000000000000, 0.9659258262890683122, 1.000000000000000000, 0.9659258262890683122, 1.000000000000000000, 0.9659258262890683122, 1.000000000000000000, 0.9659258262890683122, 1.000000000000000000, 0.9659258262890683122, 1.000000000000000000, 0.9659258262890683122, 1.000000000000000000, 0.9659258262890683122, 1.000000000000000000, 0.9659258262890683122, 1.000000000000000000, 0.9659258262890683122, 1.000000000000000000, 0.9659258262890683122, 1.000000000000000000, 0.9659258262890683122, 1.000000000000000000, 0.9659258262890683122, 1.000000000000000000, 0.9659258262890683122, 1.000000000000000000, 0.9659258262890683122, 1.000000000000000000, 0.9659258262890683122, 1.000000000000000000, 0.9659258262890683122, 1.000000000000000000, 0.9659258262890683122, 1.000000000000000000, 0.9659258262890683122, 1.000000000000000000, 0.9659258262890683122, 1.000000000000000000, 0.9659258262890683122, 1.000000000000000000, 0.9659258262890683122, 1.000000000000000000, 0.9659258262890683122, 1.000000000000000000, 0.9659258262890683122, 1.000000000000000000, 0.9659258262890683122, 1.000000000000000000, 0.9659258262890683122, 1.000000000000000000, 0.9659258262890683122, 1.000000000000000000, 0.9659258262890683122, 1.000000000000000000, 0.9659258262890683122, 1.000000000000000000 ) ) 
 REPRESENTATION_ITEM ( '' )  );
#4564=( BOUNDED_CURVE ( )  B_SPLINE_CURVE ( 2, ( #30025, #19799, #24717, #53413, #2463, #64357, #58706, #7016, #42806, #37165, #19066 ),
 .UNSPECIFIED., .F., .F. ) 
 B_SPLINE_CURVE_WITH_KNOTS ( ( 3, 2, 2, 2, 2, 3 ),
 ( 0.9166666666666668517, 0.9259259259259261521, 0.9351851851851853414, 0.9444444444444445308, 0.9537037037037037202, 0.9583333334824809535 ),
 .UNSPECIFIED. ) 
 CURVE ( )  GEOMETRIC_REPRESENTATION_ITEM ( )  RATIONAL_B_SPLINE_CURVE ( ( 0.9999999999999992228, 0.9659258262890690894, 1.000000000000000000, 0.9659258262890683122, 1.000000000000000000, 0.9659258262890683122, 1.000000000000000000, 0.9659258262890683122, 1.000000000000000000, 0.9829629125956692581, 0.9829629131445342116 ) ) 
 REPRESENTATION_ITEM ( '' )  );
#4585=SHAPE_REPRESENTATION ( 'barrel', ( #57354 ), #47738 ) ;
#4590=CARTESIAN_POINT ( 'NONE',  ( 11.35316468749999608, 236.9270833367473017, -3.042071309553167069 ) ) ;
#4621=CARTESIAN_POINT ( 'NONE',  ( 0.000000000000000000, 265.0000000000000000, 10.00000000000000000 ) ) ;
#4671=CARTESIAN_POINT ( 'NONE',  ( -5.676582343750000703, 223.0729166700806729, -9.832129032723418760 ) ) ;
#4677=CARTESIAN_POINT ( 'NONE',  ( -9.999999999999998224, 255.2083333333333712, 2.679491924311235618 ) ) ;
#4707=CARTESIAN_POINT ( 'NONE',  ( 11.35316468749999963, 221.7187500034139873, -1.390361679473963556E-15 ) ) ;
#4715=CARTESIAN_POINT ( 'NONE',  ( 7.320508075688776373, 246.8750000000000000, 7.320508075688767491 ) ) ;
#4762=CARTESIAN_POINT ( 'NONE',  ( -9.832129032723415207, 254.3229166700806729, 5.676582343750005144 ) ) ;
#4797=CARTESIAN_POINT ( 'NONE',  ( -5.676582343749992710, 260.0520833367473301, 9.832129032723422313 ) ) ;
#4825=CARTESIAN_POINT ( 'NONE',  ( -8.660254037844387298, 227.7083333401613174, -4.999999999999999112 ) ) ;
#4850=CARTESIAN_POINT ( 'NONE',  ( 3.042071309553173286, 245.3645833367473017, 11.35316468749999608 ) ) ;
#4854=CARTESIAN_POINT ( 'NONE',  ( -6.951808397369817780E-16, 247.9687500034140157, -11.35316468749999963 ) ) ;
#4917=CARTESIAN_POINT ( 'NONE',  ( -11.35316468749999963, 223.9062500034139873, 0.000000000000000000 ) ) ;
#4952=CARTESIAN_POINT ( 'NONE',  ( -8.660254037844387298, 254.5833333333333144, -4.999999999999999112 ) ) ;
#4965=CARTESIAN_POINT ( 'NONE',  ( 3.042071309553173286, 235.6770833367473017, 11.35316468749999608 ) ) ;
#4971=DIRECTION ( 'NONE',  ( -0.000000000000000000, -1.000000000000000000, -0.000000000000000000 ) ) ;
#5002=CARTESIAN_POINT ( 'NONE',  ( 2.085542519210945334E-15, 260.1562500034140157, 11.35316468749999963 ) ) ;
#5022=AXIS2_PLACEMENT_3D ( 'NONE', #69487, #12502, #51758 ) ;
#5036=VERTEX_POINT ( 'NONE', #39820 ) ;
#5053=CARTESIAN_POINT ( 'NONE',  ( 9.999999999999998224, 232.7083333333333712, -2.679491924311229401 ) ) ;
#5083=CARTESIAN_POINT ( 'NONE',  ( -3.042071309553159075, 220.2604166700806445, 11.35316468749999963 ) ) ;
#5136=CARTESIAN_POINT ( 'NONE',  ( -6.951808397369817780E-16, 262.6562500034140157, -11.35316468749999963 ) ) ;
#5170=CARTESIAN_POINT ( 'NONE',  ( -11.35316468749999785, 264.0104166700807014, -3.042071309553164848 ) ) ;
#5197=CARTESIAN_POINT ( 'NONE',  ( 10.00000000000000000, 220.6250000068279746, -1.224646799147353256E-15 ) ) ;
#5219=CARTESIAN_POINT ( 'NONE',  ( 9.832129032723416984, 251.8229166700806729, -5.676582343750003368 ) ) ;
#5222=( BOUNDED_CURVE ( )  B_SPLINE_CURVE ( 2, ( #33162, #71992, #55415, #21434, #26722, #14270, #60303, #37686, #4104, #32020, #49742, #56159, #26337 ),
 .UNSPECIFIED., .F., .F. ) 
 B_SPLINE_CURVE_WITH_KNOTS ( ( 3, 2, 2, 2, 2, 2, 3 ),
 ( 0.08333333333333278747, 0.09259259259259206010, 0.1018518518518513188, 0.1111111111111105776, 0.1203703703703698502, 0.1296296296296291228, 0.1388888888888883955 ),
 .UNSPECIFIED. ) 
 CURVE ( )  GEOMETRIC_REPRESENTATION_ITEM ( )  RATIONAL_B_SPLINE_CURVE ( ( 1.000000000000001998, 0.9659258262890662028, 1.000000000000000000, 0.9659258262890683122, 1.000000000000000000, 0.9659258262890683122, 1.000000000000000000, 0.9659258262890683122, 1.000000000000000000, 0.9659258262890683122, 1.000000000000000000, 0.9659258262890701996, 0.9999999999999981126 ) ) 
 REPRESENTATION_ITEM ( '' )  );
#5224=CARTESIAN_POINT ( 'NONE',  ( 8.311093377946834337, 247.3437500034139589, -8.311093377946836114 ) ) ;
#5250=CARTESIAN_POINT ( 'NONE',  ( -9.999999999999998224, 235.2083333333333428, 2.679491924311235174 ) ) ;
#5284=EDGE_CURVE ( 'NONE', #15595, #18027, #1817, .T. ) ;
#5286=CARTESIAN_POINT ( 'NONE',  ( -10.00000000000000000, 263.1250000068279746, 0.000000000000000000 ) ) ;
#5333=CARTESIAN_POINT ( 'NONE',  ( 11.35316468749999963, 246.5104166700806161, 3.042071309553159519 ) ) ;
#5369=CARTESIAN_POINT ( 'NONE',  ( -5.676582343750000703, 263.0729166700806445, -9.832129032723418760 ) ) ;
#5411=CARTESIAN_POINT ( 'NONE',  ( 9.999999999999998224, 252.7083333333333712, -2.679491924311229401 ) ) ;
#5415=CARTESIAN_POINT ( 'NONE',  ( 1.836970198721029589E-15, 231.2500000000000000, 10.00000000000000000 ) ) ;
#5436=( BOUNDED_CURVE ( )  B_SPLINE_CURVE ( 2, ( #17539, #34550, #74511, #22443, #18287, #46949, #40932, #52255, #959, #23942, #57555, #74140, #16781 ),
 .UNSPECIFIED., .F., .F. ) 
 B_SPLINE_CURVE_WITH_KNOTS ( ( 3, 2, 2, 2, 2, 2, 3 ),
 ( 0.2499999999999995837, 0.2592592592592589118, 0.2685185185185183232, 0.2777777777777776791, 0.2870370370370370350, 0.2962962962962963909, 0.3055555555555558023 ),
 .UNSPECIFIED. ) 
 CURVE ( )  GEOMETRIC_REPRESENTATION_ITEM ( )  RATIONAL_B_SPLINE_CURVE ( ( 1.000000000000001554, 0.9659258262890668689, 1.000000000000000000, 0.9659258262890683122, 1.000000000000000000, 0.9659258262890683122, 1.000000000000000000, 0.9659258262890683122, 1.000000000000000000, 0.9659258262890683122, 1.000000000000000000, 0.9659258262890675351, 1.000000000000000888 ) ) 
 REPRESENTATION_ITEM ( '' )  );
#5456=CARTESIAN_POINT ( 'NONE',  ( 7.320508075688771044, 248.1250000000000000, -7.320508075688771932 ) ) ;
#5486=EDGE_CURVE ( 'NONE', #71847, #71972, #48240, .T. ) ;
#5504=CARTESIAN_POINT ( 'NONE',  ( -9.832129032723418760, 238.4895833367473301, -5.676582343749998927 ) ) ;
#5536=CARTESIAN_POINT ( 'NONE',  ( -8.311093377946836114, 238.5937500034139589, -8.311093377946836114 ) ) ;
#5557=( BOUNDED_CURVE ( )  B_SPLINE_CURVE ( 2, ( #60665, #21412, #32760, #20667, #9361, #10107, #72355, #50456, #73471, #39149, #55768, #20285, #14626 ),
 .UNSPECIFIED., .F., .F. ) 
 B_SPLINE_CURVE_WITH_KNOTS ( ( 3, 2, 2, 2, 2, 2, 3 ),
 ( 0.1944444444444440034, 0.2037037037037032483, 0.2129629629629625209, 0.2222222222222217658, 0.2314814814814810662, 0.2407407407407403110, 0.2499999999999995837 ),
 .UNSPECIFIED. ) 
 CURVE ( )  GEOMETRIC_REPRESENTATION_ITEM ( )  RATIONAL_B_SPLINE_CURVE ( ( 1.000000000000001554, 0.9659258262890666469, 1.000000000000000000, 0.9659258262890683122, 1.000000000000000000, 0.9659258262890683122, 1.000000000000000000, 0.9659258262890683122, 1.000000000000000000, 0.9659258262890683122, 1.000000000000000000, 0.9659258262890698665, 0.9999999999999984457 ) ) 
 REPRESENTATION_ITEM ( '' )  );
#5595=CARTESIAN_POINT ( 'NONE',  ( -8.311093377946836114, 243.2812500034139589, -8.311093377946836114 ) ) ;
#5599=CARTESIAN_POINT ( 'NONE',  ( -3.042071309553159075, 235.2604166700806161, 11.35316468749999963 ) ) ;
#5654=CARTESIAN_POINT ( 'NONE',  ( -6.123233995736766282E-16, 251.8750000068280031, -10.00000000000000000 ) ) ;
#5687=AXIS2_PLACEMENT_3D ( 'NONE', #19771, #72585, #66539 ) ;
#5702=CARTESIAN_POINT ( 'NONE',  ( 9.832129032723420536, 236.3020833367473301, 5.676582343749996262 ) ) ;
#5716=CARTESIAN_POINT ( 'NONE',  ( 5.000000000000004441, 226.6666666666666856, 8.660254037844385522 ) ) ;
#5753=CARTESIAN_POINT ( 'NONE',  ( 1.224646799147353256E-15, 0.000000000000000000, 10.00000000000000000 ) ) ;
#5792=CARTESIAN_POINT ( 'NONE',  ( 7.320508075688771044, 243.1249999999999716, -7.320508075688771932 ) ) ;
#5807=CARTESIAN_POINT ( 'NONE',  ( -6.123233995736766282E-16, 226.8750000068279746, -10.00000000000000000 ) ) ;
#5866=VERTEX_POINT ( 'NONE', #33460 ) ;
#5879=CARTESIAN_POINT ( 'NONE',  ( 8.311093377946834337, 247.0312500034139873, -8.311093377946836114 ) ) ;
#5912=CARTESIAN_POINT ( 'NONE',  ( 9.832129032723420536, 246.3020833367473301, 5.676582343749996262 ) ) ;
#5951=VERTEX_POINT ( 'NONE', #67399 ) ;
#5963=CARTESIAN_POINT ( 'NONE',  ( -3.042071309553166625, 247.8645833367473017, -11.35316468749999608 ) ) ;
#5967=CARTESIAN_POINT ( 'NONE',  ( -11.35316468749999785, 234.0104166700806161, -3.042071309553164848 ) ) ;
#6024=CARTESIAN_POINT ( 'NONE',  ( -10.00000000000000000, 247.9166666734946887, -2.679491924311226292 ) ) ;
#6074=CARTESIAN_POINT ( 'NONE',  ( -3.042071309553166181, 248.1770833367472733, -11.35316468749999608 ) ) ;
#6113=CARTESIAN_POINT ( 'NONE',  ( 5.676582343750005144, 250.5729166700807014, 9.832129032723416984 ) ) ;
#6163=CARTESIAN_POINT ( 'NONE',  ( -8.660254037844385522, 240.4166666666666572, 5.000000000000004441 ) ) ;
#6164=CARTESIAN_POINT ( 'NONE',  ( 1.224646799147353256E-15, 0.000000000000000000, 10.00000000000000000 ) ) ;
#6171=CARTESIAN_POINT ( 'NONE',  ( -5.000000000000000888, 227.2916666734946602, -8.660254037844387298 ) ) ;
#6253=CARTESIAN_POINT ( 'NONE',  ( 8.311093377946839666, 245.7812500034139873, 8.311093377946829008 ) ) ;
#6283=VERTEX_POINT ( 'NONE', #987 ) ;
#6287=CARTESIAN_POINT ( 'NONE',  ( -3.042071309553159075, 250.2604166700806445, 11.35316468749999963 ) ) ;
#6345=CARTESIAN_POINT ( 'NONE',  ( -11.35316468749999785, 238.6979166700806729, -3.042071309553164848 ) ) ;
#6350=( BOUNDED_CURVE ( )  B_SPLINE_CURVE ( 2, ( #62322, #51008, #45344, #11026, #51376, #74387, #47562, #30594, #7222, #17791, #30958, #64917, #53612 ),
 .UNSPECIFIED., .F., .F. ) 
 B_SPLINE_CURVE_WITH_KNOTS ( ( 3, 2, 2, 2, 2, 2, 3 ),
 ( 0.8055555555555555802, 0.8148148148148147696, 0.8240740740740740700, 0.8333333333333333703, 0.8425925925925925597, 0.8518518518518518601, 0.8611111111111111605 ),
 .UNSPECIFIED. ) 
 CURVE ( )  GEOMETRIC_REPRESENTATION_ITEM ( )  RATIONAL_B_SPLINE_CURVE ( ( 1.000000000000000000, 0.9659258262890683122, 1.000000000000000000, 0.9659258262890683122, 1.000000000000000000, 0.9659258262890683122, 1.000000000000000000, 0.9659258262890683122, 1.000000000000000000, 0.9659258262890683122, 1.000000000000000000, 0.9659258262890683122, 1.000000000000000000 ) ) 
 REPRESENTATION_ITEM ( '' )  );
#6351=CARTESIAN_POINT ( 'NONE',  ( 3.042071309553173286, 240.6770833367473301, 11.35316468749999608 ) ) ;
#6363=DIRECTION ( 'NONE',  ( -1.000000000000000000, 0.000000000000000000, -0.000000000000000000 ) ) ;
#6404=CARTESIAN_POINT ( 'NONE',  ( 10.00000000000000000, 255.6250000068279746, -1.224646799147353256E-15 ) ) ;
#6411=VERTEX_POINT ( 'NONE', #36411 ) ;
#6453=CARTESIAN_POINT ( 'NONE',  ( 3.042071309553163960, 222.7604166700806161, -11.35316468749999785 ) ) ;
#6460=CARTESIAN_POINT ( 'NONE',  ( -10.00000000000000000, 239.7916666666666572, -2.679491924311226292 ) ) ;
#6487=CARTESIAN_POINT ( 'NONE',  ( 3.042071309553173286, 245.3645833367472733, 11.35316468749999608 ) ) ;
#6528=CARTESIAN_POINT ( 'NONE',  ( 2.679491924311335982, 251.4583333333333428, 9.999999999999939604 ) ) ;
#6533=CARTESIAN_POINT ( 'NONE',  ( 1.836970198721029589E-15, 241.2500000000000284, 10.00000000000000000 ) ) ;
#6553=( BOUNDED_CURVE ( )  B_SPLINE_CURVE ( 2, ( #67340, #57140, #39409, #5456, #15636, #50348, #74478, #62409, #67714, #4715, #22784, #58535, #21673 ),
 .UNSPECIFIED., .F., .F. ) 
 B_SPLINE_CURVE_WITH_KNOTS ( ( 3, 2, 2, 2, 2, 2, 3 ),
 ( 0.3611111111111107719, 0.3703703703703700167, 0.3796296296296293171, 0.3888888888888886175, 0.3981481481481478624, 0.4074074074074071072, 0.4166666666666664076 ),
 .UNSPECIFIED. ) 
 CURVE ( )  GEOMETRIC_REPRESENTATION_ITEM ( )  RATIONAL_B_SPLINE_CURVE ( ( 1.000000000000001332, 0.9659258262890670910, 1.000000000000000000, 0.9659258262890683122, 1.000000000000000000, 0.9659258262890683122, 1.000000000000000000, 0.9659258262890683122, 1.000000000000000000, 0.9659258262890683122, 1.000000000000000000, 0.9659258262890693114, 0.9999999999999990008 ) ) 
 REPRESENTATION_ITEM ( '' )  );
#6574=CIRCLE ( 'NONE', #17373, 8.749999999999998224 ) ;
#6595=UNCERTAINTY_MEASURE_WITH_UNIT (LENGTH_MEASURE( 1.000000000000000082E-05 ), #32875, 'distance_accuracy_value', 'NONE');
#6597=CIRCLE ( 'NONE', #40302, 19.00000000000000000 ) ;
#6608=ORIENTED_EDGE ( 'NONE', *, *, #50752, .T. ) ;
#6619=CARTESIAN_POINT ( 'NONE',  ( 2.085542519210945334E-15, 240.1562500034140157, 11.35316468749999963 ) ) ;
#6654=CARTESIAN_POINT ( 'NONE',  ( 11.35316468749999608, 241.9270833367473301, -3.042071309553167513 ) ) ;
#6682=CARTESIAN_POINT ( 'NONE',  ( -10.00000000000000000, 218.1250000068279746, 0.000000000000000000 ) ) ;
#6706=CARTESIAN_POINT ( 'NONE',  ( -5.676582343750000703, 238.0729166700806445, -9.832129032723418760 ) ) ;
#6710=CARTESIAN_POINT ( 'NONE',  ( 9.832129032723416984, 237.1354166700806445, -5.676582343750003368 ) ) ;
#6761=DIRECTION ( 'NONE',  ( 0.000000000000000000, 0.000000000000000000, -1.000000000000000000 ) ) ;
#6766=CARTESIAN_POINT ( 'NONE',  ( -7.320508075688771932, 252.5000000068279178, -7.320508075688771932 ) ) ;
#6788=VERTEX_POINT ( 'NONE', #62379 ) ;
#6810=CARTESIAN_POINT ( 'NONE',  ( 11.35316468749999608, 226.9270833367473301, -3.042071309553167069 ) ) ;
#6846=CARTESIAN_POINT ( 'NONE',  ( -8.311093377946834337, 254.5312500034139873, 8.311093377946837890 ) ) ;
#6865=( BOUNDED_CURVE ( )  B_SPLINE_CURVE ( 2, ( #41943, #7621, #12165, #29525, #136, #23112, #48709 ),
 .UNSPECIFIED., .F., .F. ) 
 B_SPLINE_CURVE_WITH_KNOTS ( ( 3, 2, 2, 3 ),
 ( 0.9722222222222223209, 0.9814814814814816213, 0.9907407407407406996, 1.000000000000000000 ),
 .UNSPECIFIED. ) 
 CURVE ( )  GEOMETRIC_REPRESENTATION_ITEM ( )  RATIONAL_B_SPLINE_CURVE ( ( 0.9999999999999995559, 0.9659258262890687563, 1.000000000000000000, 0.9659258262890683122, 1.000000000000000000, 0.9659258262890683122, 1.000000000000000000 ) ) 
 REPRESENTATION_ITEM ( '' )  );
#6897=CARTESIAN_POINT ( 'NONE',  ( 10.00000000000000000, 227.5000000000000000, -1.224646799147353256E-15 ) ) ;
#6977=VECTOR ( 'NONE', #18255, 1000.000000000000000 ) ;
#6983=CARTESIAN_POINT ( 'NONE',  ( -11.35316468749999785, 243.6979166700806445, -3.042071309553164848 ) ) ;
#6989=CARTESIAN_POINT ( 'NONE',  ( 4.999999999999997335, 258.3333333333333712, -8.660254037844387298 ) ) ;
#7014=CARTESIAN_POINT ( 'NONE',  ( -6.123233995736766282E-16, 236.8750000068279746, -10.00000000000000000 ) ) ;
#7016=CARTESIAN_POINT ( 'NONE',  ( 10.00000000000000178, 220.4166666734946318, 2.679491924311222739 ) ) ;
#7019=CARTESIAN_POINT ( 'NONE',  ( 5.676582343749997150, 247.5520833367473301, -9.832129032723418760 ) ) ;
#7044=ORIENTED_EDGE ( 'NONE', *, *, #25924, .F. ) ;
#7050=CARTESIAN_POINT ( 'NONE',  ( -10.00000000000000000, 264.7916666666666856, -2.679491924311226292 ) ) ;
#7074=CARTESIAN_POINT ( 'NONE',  ( -3.042071309553166625, 237.8645833367473301, -11.35316468749999608 ) ) ;
#7077=CARTESIAN_POINT ( 'NONE',  ( -3.042071309553166181, 243.1770833367473017, -11.35316468749999608 ) ) ;
#7134=CARTESIAN_POINT ( 'NONE',  ( -8.660254037844385522, 258.5416666734946602, 5.000000000000004441 ) ) ;
#7137=VERTEX_POINT ( 'NONE', #35952 ) ;
#7184=CARTESIAN_POINT ( 'NONE',  ( 11.35316468749999963, 226.7187500034139873, -1.390361679473963556E-15 ) ) ;
#7222=CARTESIAN_POINT ( 'NONE',  ( 8.660254037844389075, 225.2083333401613174, 4.999999999999997335 ) ) ;
#7223=CARTESIAN_POINT ( 'NONE',  ( 2.085542519210945334E-15, 250.1562500034140157, 11.35316468749999963 ) ) ;
#7269=CARTESIAN_POINT ( 'NONE',  ( 7.320508075688771044, 228.1249999999999716, -7.320508075688771932 ) ) ;
#7277=CARTESIAN_POINT ( 'NONE',  ( -6.123233995736766282E-16, 243.7500000000000284, -10.00000000000000000 ) ) ;
#7344=CARTESIAN_POINT ( 'NONE',  ( 5.000000000000004441, 254.7916666734946318, 8.660254037844385522 ) ) ;
#7354=CARTESIAN_POINT ( 'NONE',  ( -11.35316468749999963, 228.9062500034139873, 0.000000000000000000 ) ) ;
#7363=CARTESIAN_POINT ( 'NONE',  ( 8.660254037844385522, 241.0416666734946318, -5.000000000000003553 ) ) ;
#7390=CARTESIAN_POINT ( 'NONE',  ( -11.35316468749999963, 229.2187500034139873, 0.000000000000000000 ) ) ;
#7402=EDGE_LOOP ( 'NONE', ( #52197, #49905, #23086, #40851 ) ) ;
#7404=CARTESIAN_POINT ( 'NONE',  ( -6.123233995736766282E-16, 258.7500000000000568, -10.00000000000000000 ) ) ;
#7444=CARTESIAN_POINT ( 'NONE',  ( -5.676582343749992710, 234.7395833367473301, 9.832129032723422313 ) ) ;
#7448=CARTESIAN_POINT ( 'NONE',  ( 8.311093377946839666, 231.0937500034139873, 8.311093377946829008 ) ) ;
#7463=CARTESIAN_POINT ( 'NONE',  ( -11.35316468749999963, 219.0625000034139873, 0.000000000000000000 ) ) ;
#7480=LINE ( 'NONE', #31220, #27832 ) ;
#7504=CARTESIAN_POINT ( 'NONE',  ( -8.660254037844387298, 242.7083333401613174, -4.999999999999999112 ) ) ;
#7522=ORIENTED_EDGE ( 'NONE', *, *, #2105, .T. ) ;
#7549=CARTESIAN_POINT ( 'NONE',  ( -9.999999999999998224, 243.3333333401612606, 2.679491924311235174 ) ) ;
#7553=CARTESIAN_POINT ( 'NONE',  ( -3.042071309553166181, 223.1770833367473017, -11.35316468749999608 ) ) ;
#7588=CARTESIAN_POINT ( 'NONE',  ( 8.311093377946839666, 250.7812500034139873, 8.311093377946829008 ) ) ;
#7621=CARTESIAN_POINT ( 'NONE',  ( -2.679491924311250717, 221.0416666666666856, 9.999999999999984013 ) ) ;
#7638=CARTESIAN_POINT ( 'NONE',  ( -6.951808397369817780E-16, 262.9687500034140157, -11.35316468749999963 ) ) ;
#7647=CARTESIAN_POINT ( 'NONE',  ( 10.00000000000000178, 242.2916666666666572, 2.679491924311222739 ) ) ;
#7667=ORIENTED_EDGE ( 'NONE', *, *, #25072, .T. ) ;
#7694=EDGE_CURVE ( 'NONE', #16846, #11938, #50780, .T. ) ;
#7723=CARTESIAN_POINT ( 'NONE',  ( -8.311093377946834337, 229.5312500034139873, 8.311093377946837890 ) ) ;
#7751=CARTESIAN_POINT ( 'NONE',  ( -8.660254037844387298, 237.7083333401613174, -4.999999999999999112 ) ) ;
#7758=CARTESIAN_POINT ( 'NONE',  ( -11.35316468749999785, 229.0104166700806445, -3.042071309553164848 ) ) ;
#7765=CARTESIAN_POINT ( 'NONE',  ( 0.000000000000000000, 0.000000000000000000, -10.00000000000000000 ) ) ;
#7810=CARTESIAN_POINT ( 'NONE',  ( -5.676582343750000703, 233.0729166700806729, -9.832129032723418760 ) ) ;
#7813=CARTESIAN_POINT ( 'NONE',  ( 5.676582343749997150, 227.5520833367473017, -9.832129032723418760 ) ) ;
#7872=CARTESIAN_POINT ( 'NONE',  ( -8.660254037844385522, 233.5416666734946318, 5.000000000000004441 ) ) ;
#7880=EDGE_CURVE ( 'NONE', #29199, #43392, #26281, .T. ) ;
#7894=CARTESIAN_POINT ( 'NONE',  ( -6.123233995736766282E-16, 221.8750000068279746, -10.00000000000000000 ) ) ;
#7916=CARTESIAN_POINT ( 'NONE',  ( 3.042071309553163960, 232.7604166700806445, -11.35316468749999785 ) ) ;
#7956=CARTESIAN_POINT ( 'NONE',  ( -9.832129032723418760, 228.4895833367473585, -5.676582343749998927 ) ) ;
#8001=CARTESIAN_POINT ( 'NONE',  ( 2.679491924311235174, 221.4583333333333428, 9.999999999999998224 ) ) ;
#8086=CARTESIAN_POINT ( 'NONE',  ( -6.951808397369817780E-16, 227.6562500034139873, -11.35316468749999963 ) ) ;
#8090=CARTESIAN_POINT ( 'NONE',  ( -2.679491924311228512, 258.9583333333332575, -9.999999999999998224 ) ) ;
#8122=CARTESIAN_POINT ( 'NONE',  ( -8.311093377946836114, 233.5937500034139589, -8.311093377946836114 ) ) ;
#8177=CARTESIAN_POINT ( 'NONE',  ( -8.311093377946834337, 224.8437500034139589, 8.311093377946837890 ) ) ;
#8203=DIRECTION ( 'NONE',  ( -0.000000000000000000, -1.000000000000000000, -0.000000000000000000 ) ) ;
#8236=CARTESIAN_POINT ( 'NONE',  ( -7.320508075688771932, 237.5000000068279746, -7.320508075688771932 ) ) ;
#8253=ORIENTED_EDGE ( 'NONE', *, *, #57635, .F. ) ;
#8254=EDGE_CURVE ( 'NONE', #52326, #17439, #70775, .T. ) ;
#8319=CARTESIAN_POINT ( 'NONE',  ( -5.676582343749992710, 229.7395833367473301, 9.832129032723422313 ) ) ;
#8328=VERTEX_POINT ( 'NONE', #11929 ) ;
#8367=CARTESIAN_POINT ( 'NONE',  ( -2.679491924311228512, 228.9583333333333144, -9.999999999999998224 ) ) ;
#8388=CARTESIAN_POINT ( 'NONE',  ( -10.00000000000000000, 230.0000000000000000, 0.000000000000000000 ) ) ;
#8399=( BOUNDED_CURVE ( )  B_SPLINE_CURVE ( 2, ( #7404, #30411, #56038, #61311, #54915, #43198, #37182, #8880, #60557, #44332, #31894, #4345, #26970 ),
 .UNSPECIFIED., .F., .F. ) 
 B_SPLINE_CURVE_WITH_KNOTS ( ( 3, 2, 2, 2, 2, 2, 3 ),
 ( 0.1388888888888883955, 0.1481481481481476403, 0.1574074074074069407, 0.1666666666666661856, 0.1759259259259254859, 0.1851851851851847308, 0.1944444444444440034 ),
 .UNSPECIFIED. ) 
 CURVE ( )  GEOMETRIC_REPRESENTATION_ITEM ( )  RATIONAL_B_SPLINE_CURVE ( ( 1.000000000000001776, 0.9659258262890664248, 1.000000000000000000, 0.9659258262890683122, 1.000000000000000000, 0.9659258262890683122, 1.000000000000000000, 0.9659258262890683122, 1.000000000000000000, 0.9659258262890683122, 1.000000000000000000, 0.9659258262890699775, 0.9999999999999983347 ) ) 
 REPRESENTATION_ITEM ( '' )  );
#8443=DIRECTION ( 'NONE',  ( 0.000000000000000000, 0.000000000000000000, -1.000000000000000000 ) ) ;
#8453=CARTESIAN_POINT ( 'NONE',  ( -8.311093377946836114, 228.2812500034140157, -8.311093377946836114 ) ) ;
#8458=CARTESIAN_POINT ( 'NONE',  ( -6.123233995736766282E-16, 263.7500000000000568, -10.00000000000000000 ) ) ;
#8461=CARTESIAN_POINT ( 'NONE',  ( 10.00000000000000000, 240.6250000068279746, -1.224646799147353256E-15 ) ) ;
#8488=CARTESIAN_POINT ( 'NONE',  ( -8.311093377946834337, 234.8437500034139305, 8.311093377946837890 ) ) ;
#8549=CARTESIAN_POINT ( 'NONE',  ( 2.085542519210945334E-15, 220.4687500034139873, 11.35316468749999963 ) ) ;
#8608=CARTESIAN_POINT ( 'NONE',  ( -10.00000000000000000, 243.1250000068280031, 0.000000000000000000 ) ) ;
#8617=VECTOR ( 'NONE', #13837, 1000.000000000000227 ) ;
#8628=DIRECTION ( 'NONE',  ( 0.000000000000000000, 0.000000000000000000, -1.000000000000000000 ) ) ;
#8633=CARTESIAN_POINT ( 'NONE',  ( 2.085542519210945334E-15, 260.1562500034140157, 11.35316468749999963 ) ) ;
#8636=CARTESIAN_POINT ( 'NONE',  ( -9.832129032723418760, 263.8020833367473301, -5.676582343749998927 ) ) ;
#8657=CARTESIAN_POINT ( 'NONE',  ( 1.836970198721029589E-15, 244.3750000068280031, 10.00000000000000000 ) ) ;
#8690=CYLINDRICAL_SURFACE ( 'NONE', #53431, 19.00000000000001776 ) ;
#8697=CARTESIAN_POINT ( 'NONE',  ( -9.832129032723415207, 229.3229166700806729, 5.676582343750005144 ) ) ;
#8729=ORIENTED_EDGE ( 'NONE', *, *, #17798, .F. ) ;
#8736=DIRECTION ( 'NONE',  ( -0.000000000000000000, -1.000000000000000000, -0.000000000000000000 ) ) ;
#8750=CARTESIAN_POINT ( 'NONE',  ( -11.35316468749999963, 249.2187500034139873, 0.000000000000000000 ) ) ;
#8762=ADVANCED_FACE ( 'NONE', ( #31409 ), #31732, .F. ) ;
#8832=CARTESIAN_POINT ( 'NONE',  ( -8.660254037844385522, 255.4166666666666856, 5.000000000000004441 ) ) ;
#8834=CARTESIAN_POINT ( 'NONE',  ( 11.35316468749999963, 226.1979166700806729, 3.042071309553159519 ) ) ;
#8839=CARTESIAN_POINT ( 'NONE',  ( 2.679491924311235174, 246.4583333333333428, 9.999999999999998224 ) ) ;
#8864=DIRECTION ( 'NONE',  ( 0.000000000000000000, 0.000000000000000000, -1.000000000000000000 ) ) ;
#8868=CARTESIAN_POINT ( 'NONE',  ( -5.676582343750000703, 228.3854166700806729, -9.832129032723418760 ) ) ;
#8870=ORIENTED_EDGE ( 'NONE', *, *, #58546, .F. ) ;
#8879=VERTEX_POINT ( 'NONE', #12935 ) ;
#8880=CARTESIAN_POINT ( 'NONE',  ( 10.00000000000000178, 257.2916666666666856, 2.679491924311222739 ) ) ;
#8920=CARTESIAN_POINT ( 'NONE',  ( 8.311093377946834337, 222.0312500034139873, -8.311093377946836114 ) ) ;
#8923=CARTESIAN_POINT ( 'NONE',  ( -11.35316468749999785, 229.0104166700806445, -3.042071309553164848 ) ) ;
#8969=CYLINDRICAL_SURFACE ( 'NONE', #1136, 10.00000000000000000 ) ;
#8985=CARTESIAN_POINT ( 'NONE',  ( 9.999999999999998224, 235.8333333401613174, -2.679491924311229401 ) ) ;
#9007=CARTESIAN_POINT ( 'NONE',  ( -9.832129032723418760, 253.4895833367473017, -5.676582343749998927 ) ) ;
#9010=CARTESIAN_POINT ( 'NONE',  ( -11.35316468749999785, 264.0104166700807014, -3.042071309553164848 ) ) ;
#9032=CARTESIAN_POINT ( 'NONE',  ( -4.999999999999992895, 243.9583333401613174, 8.660254037844390851 ) ) ;
#9049=CARTESIAN_POINT ( 'NONE',  ( -8.660254037844387298, 259.5833333333333144, -4.999999999999999112 ) ) ;
#9074=CARTESIAN_POINT ( 'NONE',  ( -11.35316468749999608, 234.1145833367473017, 3.042071309553173730 ) ) ;
#9122=CARTESIAN_POINT ( 'NONE',  ( 5.676582343749997150, 257.5520833367473301, -9.832129032723418760 ) ) ;
#9174=CARTESIAN_POINT ( 'NONE',  ( -4.999999999999992895, 248.9583333401613174, 8.660254037844390851 ) ) ;
#9205=CARTESIAN_POINT ( 'NONE',  ( -11.35316468749999963, 218.9062500034139873, 0.000000000000000000 ) ) ;
#9210=CARTESIAN_POINT ( 'NONE',  ( -2.679491924311222295, 246.0416666666666856, 10.00000000000000178 ) ) ;
#9283=( BOUNDED_CURVE ( )  B_SPLINE_CURVE ( 2, ( #964, #35651, #47325, #18663, #12982, #36019, #19024, #59037, #65037, #53372, #7344, #1695, #36384 ),
 .UNSPECIFIED., .F., .F. ) 
 B_SPLINE_CURVE_WITH_KNOTS ( ( 3, 2, 2, 2, 2, 2, 3 ),
 ( 0.1388888888888883955, 0.1481481481481476403, 0.1574074074074069407, 0.1666666666666661856, 0.1759259259259254859, 0.1851851851851847308, 0.1944444444444440034 ),
 .UNSPECIFIED. ) 
 CURVE ( )  GEOMETRIC_REPRESENTATION_ITEM ( )  RATIONAL_B_SPLINE_CURVE ( ( 1.000000000000001776, 0.9659258262890664248, 1.000000000000000000, 0.9659258262890683122, 1.000000000000000000, 0.9659258262890683122, 1.000000000000000000, 0.9659258262890683122, 1.000000000000000000, 0.9659258262890683122, 1.000000000000000000, 0.9659258262890699775, 0.9999999999999983347 ) ) 
 REPRESENTATION_ITEM ( '' )  );
#9291=FACE_OUTER_BOUND ( 'NONE', #17603, .T. ) ;
#9292=CARTESIAN_POINT ( 'NONE',  ( 2.085542519210945334E-15, 225.1562500034139873, 11.35316468749999963 ) ) ;
#9295=CARTESIAN_POINT ( 'NONE',  ( 8.311093377946834337, 252.0312500034139589, -8.311093377946836114 ) ) ;
#9299=DIRECTION ( 'NONE',  ( 0.000000000000000000, 0.000000000000000000, -1.000000000000000000 ) ) ;
#9311=VERTEX_POINT ( 'NONE', #69072 ) ;
#9333=CARTESIAN_POINT ( 'NONE',  ( 9.832129032723416984, 252.1354166700806445, -5.676582343750003368 ) ) ;
#9360=CARTESIAN_POINT ( 'NONE',  ( 9.999999999999998224, 225.8333333401612606, -2.679491924311229401 ) ) ;
#9361=CARTESIAN_POINT ( 'NONE',  ( -8.660254037844385522, 253.5416666734946602, 5.000000000000004441 ) ) ;
#9382=CARTESIAN_POINT ( 'NONE',  ( -8.311093377946834337, 259.5312500034139589, 8.311093377946837890 ) ) ;
#9386=CARTESIAN_POINT ( 'NONE',  ( 9.832129032723416984, 257.1354166700806445, -5.676582343750003368 ) ) ;
#9425=VECTOR ( 'NONE', #4971, 1000.000000000000000 ) ;
#9428=CARTESIAN_POINT ( 'NONE',  ( 1.836970198721029589E-15, 261.2500000000000568, 10.00000000000000000 ) ) ;
#9440=FACE_OUTER_BOUND ( 'NONE', #35406, .T. ) ;
#9453=CARTESIAN_POINT ( 'NONE',  ( -11.35316468749999785, 228.6979166700806729, -3.042071309553164848 ) ) ;
#9486=EDGE_CURVE ( 'NONE', #7137, #25962, #66695, .T. ) ;
#9507=CARTESIAN_POINT ( 'NONE',  ( -3.042071309553166181, 258.1770833367473301, -11.35316468749999608 ) ) ;
#9548=CARTESIAN_POINT ( 'NONE',  ( 0.000000000000000000, 265.0000000000000000, 0.000000000000000000 ) ) ;
#9552=CARTESIAN_POINT ( 'NONE',  ( 2.326828918379972154E-15, 0.000000000000000000, 19.00000000000000000 ) ) ;
#9594=CARTESIAN_POINT ( 'NONE',  ( -2.679491924311222295, 251.0416666666665719, 10.00000000000000178 ) ) ;
#9633=DIRECTION ( 'NONE',  ( 0.000000000000000000, 0.000000000000000000, -1.000000000000000000 ) ) ;
#9646=CARTESIAN_POINT ( 'NONE',  ( 8.660254037844385522, 237.9166666666666572, -5.000000000000003553 ) ) ;
#9654=EDGE_CURVE ( 'NONE', #14438, #29935, #39054, .T. ) ;
#9675=CARTESIAN_POINT ( 'NONE',  ( -11.35316468749999608, 219.1145833367473017, 3.042071309553173730 ) ) ;
#9679=CARTESIAN_POINT ( 'NONE',  ( 5.676582343750005144, 260.5729166700806445, 9.832129032723416984 ) ) ;
#9711=CARTESIAN_POINT ( 'NONE',  ( -3.042071309553159075, 260.2604166700805877, 11.35316468749999963 ) ) ;
#9737=CARTESIAN_POINT ( 'NONE',  ( 5.000000000000004441, 219.7916666734946318, 8.660254037844385522 ) ) ;
#9762=CARTESIAN_POINT ( 'NONE',  ( -5.676582343749992710, 254.7395833367473301, 9.832129032723422313 ) ) ;
#9766=CARTESIAN_POINT ( 'NONE',  ( -5.676582343750000703, 248.3854166700806445, -9.832129032723418760 ) ) ;
#9822=CARTESIAN_POINT ( 'NONE',  ( 7.320508075688776373, 260.0000000068279746, 7.320508075688767491 ) ) ;
#9831=ORIENTED_EDGE ( 'NONE', *, *, #57824, .T. ) ;
#9875=CARTESIAN_POINT ( 'NONE',  ( 2.085542519210945334E-15, 250.4687500034140157, 11.35316468749999963 ) ) ;
#9886=VECTOR ( 'NONE', #36621, 1000.000000000000000 ) ;
#9893=CARTESIAN_POINT ( 'NONE',  ( -6.123233995736766282E-16, 228.7500000000000000, -10.00000000000000000 ) ) ;
#9906=CARTESIAN_POINT ( 'NONE',  ( -9.832129032723415207, 259.3229166700806445, 5.676582343750005144 ) ) ;
#9959=CARTESIAN_POINT ( 'NONE',  ( 7.320508075688771044, 248.1250000000000284, -7.320508075688771932 ) ) ;
#9992=CARTESIAN_POINT ( 'NONE',  ( 5.676582343749997150, 222.5520833367473017, -9.832129032723418760 ) ) ;
#10003=CARTESIAN_POINT ( 'NONE',  ( 0.000000000000000000, 0.000000000000000000, 0.000000000000000000 ) ) ;
#10037=AXIS2_PLACEMENT_3D ( 'NONE', #33906, #39545, #35386 ) ;
#10044=CARTESIAN_POINT ( 'NONE',  ( -8.311093377946834337, 259.5312500034139589, 8.311093377946837890 ) ) ;
#10079=CARTESIAN_POINT ( 'NONE',  ( -8.311093377946836114, 253.5937500034139873, -8.311093377946836114 ) ) ;
#10106=CARTESIAN_POINT ( 'NONE',  ( -9.999999999999998224, 223.3333333401613174, 2.679491924311235618 ) ) ;
#10107=CARTESIAN_POINT ( 'NONE',  ( -9.999999999999998224, 253.3333333401613174, 2.679491924311235174 ) ) ;
#10130=CARTESIAN_POINT ( 'NONE',  ( 11.35316468749999963, 256.7187500034139589, -1.390361679473963556E-15 ) ) ;
#10155=CARTESIAN_POINT ( 'NONE',  ( -2.679491924311193429, 236.0416666666666572, 10.00000000000001954 ) ) ;
#10194=CARTESIAN_POINT ( 'NONE',  ( -9.832129032723418760, 223.4895833367473301, -5.676582343749998927 ) ) ;
#10243=DIRECTION ( 'NONE',  ( -0.000000000000000000, -1.000000000000000000, -0.000000000000000000 ) ) ;
#10245=CARTESIAN_POINT ( 'NONE',  ( -11.35316468749999785, 239.0104166700806161, -3.042071309553164848 ) ) ;
#10251=CARTESIAN_POINT ( 'NONE',  ( 0.000000000000000000, 0.000000000000000000, -10.00000000000000000 ) ) ;
#10280=CARTESIAN_POINT ( 'NONE',  ( -8.311093377946836114, 263.2812500034139020, -8.311093377946836114 ) ) ;
#10289=CARTESIAN_POINT ( 'NONE',  ( 4.999999999999997335, 231.4583333401613174, -8.660254037844387298 ) ) ;
#10326=CARTESIAN_POINT ( 'NONE',  ( 3.042071309553173286, 220.3645833367472733, 11.35316468749999608 ) ) ;
#10332=CARTESIAN_POINT ( 'NONE',  ( -4.999999999999992895, 255.8333333333333712, 8.660254037844390851 ) ) ;
#10362=CARTESIAN_POINT ( 'NONE',  ( -6.951808397369817780E-16, 222.9687500034139873, -11.35316468749999963 ) ) ;
#10394=EDGE_CURVE ( 'NONE', #21159, #24629, #29357, .T. ) ;
#10414=CARTESIAN_POINT ( 'NONE',  ( -3.042071309553166181, 257.8645833367473301, -11.35316468749999608 ) ) ;
#10449=CARTESIAN_POINT ( 'NONE',  ( -11.35316468749999785, 259.0104166700807014, -3.042071309553164848 ) ) ;
#10460=CARTESIAN_POINT ( 'NONE',  ( 0.000000000000000000, 0.000000000000000000, 0.000000000000000000 ) ) ;
#10472=CARTESIAN_POINT ( 'NONE',  ( 1.148106374200643592E-15, 45.00000000000000000, 8.749999999999998224 ) ) ;
#10475=CARTESIAN_POINT ( 'NONE',  ( 2.679491924311235174, 224.5833333401613174, 9.999999999999998224 ) ) ;
#10498=CARTESIAN_POINT ( 'NONE',  ( 11.35316468749999963, 251.4062500034139873, -1.390361679473963556E-15 ) ) ;
#10504=CARTESIAN_POINT ( 'NONE',  ( -11.35316468749999785, 259.0104166700807014, -3.042071309553164848 ) ) ;
#10542=CARTESIAN_POINT ( 'NONE',  ( -9.999999999999998224, 245.2083333333333428, 2.679491924311235174 ) ) ;
#10564=CARTESIAN_POINT ( 'NONE',  ( 5.676582343749997150, 227.2395833367473301, -9.832129032723418760 ) ) ;
#10617=CARTESIAN_POINT ( 'NONE',  ( 5.676582343750005144, 235.8854166700806729, 9.832129032723416984 ) ) ;
#10649=CARTESIAN_POINT ( 'NONE',  ( 5.676582343750005144, 260.5729166700806445, 9.832129032723416984 ) ) ;
#10694=CARTESIAN_POINT ( 'NONE',  ( 4.999999999999997335, 253.3333333333333428, -8.660254037844387298 ) ) ;
#10699=CARTESIAN_POINT ( 'NONE',  ( -10.00000000000000000, 239.7916666666666288, -2.679491924311226292 ) ) ;
#10728=CARTESIAN_POINT ( 'NONE',  ( -9.832129032723415207, 219.6354166700806445, 5.676582343750005144 ) ) ;
#10730=ORIENTED_EDGE ( 'NONE', *, *, #37000, .F. ) ;
#10764=EDGE_CURVE ( 'NONE', #8328, #14438, #2897, .T. ) ;
#10781=ORIENTED_EDGE ( 'NONE', *, *, #23627, .T. ) ;
#10782=CARTESIAN_POINT ( 'NONE',  ( 11.35316468749999963, 256.4062500034140157, -1.390361679473963556E-15 ) ) ;
#10786=CARTESIAN_POINT ( 'NONE',  ( -8.224976990608492855, 220.0000000000001421, 7.304091559116764110 ) ) ;
#10818=CARTESIAN_POINT ( 'NONE',  ( 11.35316468749999963, 251.7187500034139873, -1.390361679473963556E-15 ) ) ;
#10847=CARTESIAN_POINT ( 'NONE',  ( 7.320508075688776373, 230.0000000068279178, 7.320508075688767491 ) ) ;
#10872=CARTESIAN_POINT ( 'NONE',  ( -11.35316468749999963, 243.9062500034140157, 0.000000000000000000 ) ) ;
#10877=CARTESIAN_POINT ( 'NONE',  ( -11.35316468749999785, 249.0104166700806445, -3.042071309553164848 ) ) ;
#10938=CARTESIAN_POINT ( 'NONE',  ( 5.676582343750005144, 225.5729166700806729, 9.832129032723416984 ) ) ;
#10961=CARTESIAN_POINT ( 'NONE',  ( 7.320508075688771044, 223.1250000000000284, -7.320508075688771932 ) ) ;
#10990=CARTESIAN_POINT ( 'NONE',  ( 5.676582343750005144, 240.8854166700806445, 9.832129032723416984 ) ) ;
#11026=CARTESIAN_POINT ( 'NONE',  ( 7.320508075688771044, 226.2500000068279746, -7.320508075688771932 ) ) ;
#11027=CARTESIAN_POINT ( 'NONE',  ( -11.35316468749999608, 259.1145833367473301, 3.042071309553173730 ) ) ;
#11030=ADVANCED_FACE ( 'NONE', ( #44082 ), #67093, .F. ) ;
#11045=LINE ( 'NONE', #57072, #50838 ) ;
#11078=CARTESIAN_POINT ( 'NONE',  ( -5.000000000000000888, 239.1666666666666572, -8.660254037844387298 ) ) ;
#11162=CARTESIAN_POINT ( 'NONE',  ( -11.35316468749999608, 239.1145833367473301, 3.042071309553173730 ) ) ;
#11194=CARTESIAN_POINT ( 'NONE',  ( 9.832129032723420536, 241.3020833367473301, 5.676582343749996262 ) ) ;
#11247=CARTESIAN_POINT ( 'NONE',  ( -6.951808397369817780E-16, 247.6562500034140157, -11.35316468749999963 ) ) ;
#11251=CARTESIAN_POINT ( 'NONE',  ( 5.676582343749997150, 242.5520833367473301, -9.832129032723418760 ) ) ;
#11310=CARTESIAN_POINT ( 'NONE',  ( -10.00000000000000000, 262.9166666734946034, -2.679491924311226292 ) ) ;
#11336=ORIENTED_EDGE ( 'NONE', *, *, #58546, .T. ) ;
#11358=CARTESIAN_POINT ( 'NONE',  ( 5.676582343749997150, 237.5520833367473301, -9.832129032723418760 ) ) ;
#11394=CARTESIAN_POINT ( 'NONE',  ( 5.676582343750005144, 255.5729166700806445, 9.832129032723416984 ) ) ;
#11422=DIRECTION ( 'NONE',  ( 0.000000000000000000, 0.000000000000000000, 1.000000000000000000 ) ) ;
#11444=CARTESIAN_POINT ( 'NONE',  ( 2.679491924311235174, 241.4583333333333144, 9.999999999999998224 ) ) ;
#11474=ORIENTED_EDGE ( 'NONE', *, *, #2670, .T. ) ;
#11530=CARTESIAN_POINT ( 'NONE',  ( -11.35316468749999963, 248.9062500034139873, 0.000000000000000000 ) ) ;
#11538=CARTESIAN_POINT ( 'NONE',  ( -6.123233995736766282E-16, 263.7500000000000568, -10.00000000000000000 ) ) ;
#11556=CARTESIAN_POINT ( 'NONE',  ( -10.00000000000000000, 225.0000000000000000, 0.000000000000000000 ) ) ;
#11562=CARTESIAN_POINT ( 'NONE',  ( -6.951808397369817780E-16, 247.9687500034140157, -11.35316468749999963 ) ) ;
#11602=( BOUNDED_CURVE ( )  B_SPLINE_CURVE ( 2, ( #9428, #55455, #48651, #43748, #71659, #14688, #37729, #60727, #9049, #68624, #44500, #21843, #33947 ),
 .UNSPECIFIED., .F., .F. ) 
 B_SPLINE_CURVE_WITH_KNOTS ( ( 3, 2, 2, 2, 2, 2, 3 ),
 ( 0.08333333333333278747, 0.09259259259259206010, 0.1018518518518513188, 0.1111111111111105776, 0.1203703703703698502, 0.1296296296296291228, 0.1388888888888883955 ),
 .UNSPECIFIED. ) 
 CURVE ( )  GEOMETRIC_REPRESENTATION_ITEM ( )  RATIONAL_B_SPLINE_CURVE ( ( 1.000000000000001998, 0.9659258262890662028, 1.000000000000000000, 0.9659258262890683122, 1.000000000000000000, 0.9659258262890683122, 1.000000000000000000, 0.9659258262890683122, 1.000000000000000000, 0.9659258262890683122, 1.000000000000000000, 0.9659258262890701996, 0.9999999999999981126 ) ) 
 REPRESENTATION_ITEM ( '' )  );
#11615=CARTESIAN_POINT ( 'NONE',  ( 8.311093377946834337, 252.0312500034139873, -8.311093377946836114 ) ) ;
#11620=CARTESIAN_POINT ( 'NONE',  ( -5.676582343750000703, 238.3854166700806445, -9.832129032723418760 ) ) ;
#11643=CARTESIAN_POINT ( 'NONE',  ( -8.660254037844387298, 234.5833333333333428, -4.999999999999999112 ) ) ;
#11675=CARTESIAN_POINT ( 'NONE',  ( -9.999999999999998224, 248.3333333401613174, 2.679491924311235618 ) ) ;
#11727=CARTESIAN_POINT ( 'NONE',  ( -11.35316468749999963, 239.2187500034139873, 0.000000000000000000 ) ) ;
#11735=CARTESIAN_POINT ( 'NONE',  ( 1.836970198721029589E-15, 234.3750000068279746, 10.00000000000000000 ) ) ;
#11764=CARTESIAN_POINT ( 'NONE',  ( 9.832129032723416984, 246.8229166700806729, -5.676582343750003368 ) ) ;
#11770=ORIENTED_EDGE ( 'NONE', *, *, #1017, .F. ) ;
#11813=CARTESIAN_POINT ( 'NONE',  ( -7.320508075688771932, 244.3750000000000000, -7.320508075688771932 ) ) ;
#11822=CARTESIAN_POINT ( 'NONE',  ( -9.999999999999998224, 228.3333333401613174, 2.679491924311235174 ) ) ;
#11902=CARTESIAN_POINT ( 'NONE',  ( -5.676582343749992710, 249.7395833367473301, 9.832129032723422313 ) ) ;
#11929=CARTESIAN_POINT ( 'NONE',  ( -6.123233995736766282E-16, 238.7500000000000284, -10.00000000000000000 ) ) ;
#11936=CARTESIAN_POINT ( 'NONE',  ( -9.832129032723418760, 238.8020833367473301, -5.676582343749998927 ) ) ;
#11938=VERTEX_POINT ( 'NONE', #23948 ) ;
#11988=CARTESIAN_POINT ( 'NONE',  ( 5.676582343749997150, 242.2395833367473301, -9.832129032723418760 ) ) ;
#11992=CARTESIAN_POINT ( 'NONE',  ( 8.311093377946839666, 246.0937500034139873, 8.311093377946829008 ) ) ;
#12047=CARTESIAN_POINT ( 'NONE',  ( -8.660254037844385522, 248.5416666734946318, 5.000000000000004441 ) ) ;
#12093=CARTESIAN_POINT ( 'NONE',  ( 11.35316468749999963, 226.5104166700806445, 3.042071309553159519 ) ) ;
#12129=CARTESIAN_POINT ( 'NONE',  ( -11.35316468749999963, 243.9062500034140157, 0.000000000000000000 ) ) ;
#12160=EDGE_CURVE ( 'NONE', #2698, #23527, #6597, .T. ) ;
#12165=CARTESIAN_POINT ( 'NONE',  ( -4.999999999999992895, 220.8333333333333428, 8.660254037844390851 ) ) ;
#12178=CARTESIAN_POINT ( 'NONE',  ( 8.660254037844385522, 232.9166666666666572, -5.000000000000003553 ) ) ;
#12267=CARTESIAN_POINT ( 'NONE',  ( -5.676582343749992710, 244.7395833367473301, 9.832129032723422313 ) ) ;
#12297=CARTESIAN_POINT ( 'NONE',  ( -7.320508075688771932, 224.3750000000000000, -7.320508075688771932 ) ) ;
#12304=CARTESIAN_POINT ( 'NONE',  ( 8.311093377946839666, 241.0937500034139873, 8.311093377946830785 ) ) ;
#12355=CARTESIAN_POINT ( 'NONE',  ( -11.35316468749999785, 228.6979166700806445, -3.042071309553164848 ) ) ;
#12356=DIRECTION ( 'NONE',  ( 0.000000000000000000, 0.000000000000000000, -1.000000000000000000 ) ) ;
#12359=CARTESIAN_POINT ( 'NONE',  ( 11.35316468749999963, 241.7187500034139873, -1.390361679473963556E-15 ) ) ;
#12369=ORIENTED_EDGE ( 'NONE', *, *, #63840, .T. ) ;
#12412=CYLINDRICAL_SURFACE ( 'NONE', #50191, 10.00000000000000000 ) ;
#12413=CARTESIAN_POINT ( 'NONE',  ( 2.679491924311225848, 256.6666666734946602, -10.00000000000000000 ) ) ;
#12461=CARTESIAN_POINT ( 'NONE',  ( -6.951808397369817780E-16, 232.9687500034139873, -11.35316468749999963 ) ) ;
#12498=CARTESIAN_POINT ( 'NONE',  ( 8.311093377946834337, 242.0312500034140157, -8.311093377946836114 ) ) ;
#12502=DIRECTION ( 'NONE',  ( 0.000000000000000000, 1.000000000000000000, 0.000000000000000000 ) ) ;
#12518=EDGE_LOOP ( 'NONE', ( #45950, #48424, #46910, #53725 ) ) ;
#12549=CARTESIAN_POINT ( 'NONE',  ( -7.320508075688771932, 224.3749999999999716, -7.320508075688771932 ) ) ;
#12625=AXIS2_PLACEMENT_3D ( 'NONE', #66397, #71673, #61114 ) ;
#12630=CARTESIAN_POINT ( 'NONE',  ( -3.042071309553159075, 239.9479166700806729, 11.35316468749999963 ) ) ;
#12657=CARTESIAN_POINT ( 'NONE',  ( -7.320508075688771932, 237.5000000068279746, -7.320508075688771932 ) ) ;
#12663=CARTESIAN_POINT ( 'NONE',  ( 11.35316468749999608, 246.9270833367473017, -3.042071309553167513 ) ) ;
#12698=( GEOMETRIC_REPRESENTATION_CONTEXT ( 3 ) GLOBAL_UNCERTAINTY_ASSIGNED_CONTEXT ( ( #46574 ) ) GLOBAL_UNIT_ASSIGNED_CONTEXT ( ( #67017, #28512, #18311 ) ) REPRESENTATION_CONTEXT ( 'NONE', 'WORKASPACE' ) );
#12702=CARTESIAN_POINT ( 'NONE',  ( 0.000000000000000000, 0.000000000000000000, 0.000000000000000000 ) ) ;
#12715=CARTESIAN_POINT ( 'NONE',  ( -8.311093377946836114, 228.2812500034139589, -8.311093377946836114 ) ) ;
#12719=CARTESIAN_POINT ( 'NONE',  ( 11.35316468749999963, 236.7187500034139873, -1.390361679473963556E-15 ) ) ;
#12773=CARTESIAN_POINT ( 'NONE',  ( 8.660254037844389075, 262.0833333333333144, 4.999999999999997335 ) ) ;
#12776=CARTESIAN_POINT ( 'NONE',  ( -9.999999999999998224, 258.3333333401612890, 2.679491924311235618 ) ) ;
#12823=CARTESIAN_POINT ( 'NONE',  ( -9.832129032723415207, 234.6354166700806445, 5.676582343750005144 ) ) ;
#12857=CARTESIAN_POINT ( 'NONE',  ( -9.832129032723415207, 249.3229166700806729, 5.676582343750005144 ) ) ;
#12909=CARTESIAN_POINT ( 'NONE',  ( -10.00000000000000000, 230.0000000000000000, 0.000000000000000000 ) ) ;
#12935=CARTESIAN_POINT ( 'NONE',  ( 1.836970198721029589E-15, 254.3750000068280031, 10.00000000000000000 ) ) ;
#12954=ORIENTED_EDGE ( 'NONE', *, *, #5284, .F. ) ;
#12982=CARTESIAN_POINT ( 'NONE',  ( 8.660254037844385522, 256.0416666734946602, -5.000000000000003553 ) ) ;
#12992=CARTESIAN_POINT ( 'NONE',  ( 3.042071309553163960, 237.4479166700806729, -11.35316468749999785 ) ) ;
#13026=CARTESIAN_POINT ( 'NONE',  ( 5.676582343749997150, 227.5520833367473017, -9.832129032723418760 ) ) ;
#13029=EDGE_CURVE ( 'NONE', #16856, #52326, #74441, .T. ) ;
#13054=CARTESIAN_POINT ( 'NONE',  ( -7.320508075688771932, 264.3750000000000000, -7.320508075688771932 ) ) ;
#13079=CARTESIAN_POINT ( 'NONE',  ( 11.35316468749999963, 226.4062500034139873, -1.390361679473963556E-15 ) ) ;
#13083=CARTESIAN_POINT ( 'NONE',  ( -9.832129032723418760, 223.8020833367473301, -5.676582343749998927 ) ) ;
#13136=CARTESIAN_POINT ( 'NONE',  ( 1.836970198721029589E-15, 261.2500000000000568, 10.00000000000000000 ) ) ;
#13139=CARTESIAN_POINT ( 'NONE',  ( -8.660254037844387298, 252.7083333401612890, -4.999999999999999112 ) ) ;
#13187=CARTESIAN_POINT ( 'NONE',  ( 2.085542519210945334E-15, 225.4687500034139873, 11.35316468749999963 ) ) ;
#13195=LINE ( 'NONE', #34775, #57588 ) ;
#13213=DIRECTION ( 'NONE',  ( 0.000000000000000000, 0.000000000000000000, -1.000000000000000000 ) ) ;
#13227=CARTESIAN_POINT ( 'NONE',  ( 11.35316468749999963, 251.1979166700807014, 3.042071309553159519 ) ) ;
#13264=DIRECTION ( 'NONE',  ( -0.000000000000000000, -1.000000000000000000, -0.000000000000000000 ) ) ;
#13273=CARTESIAN_POINT ( 'NONE',  ( -6.123233995736766282E-16, 228.7500000000000000, -10.00000000000000000 ) ) ;
#13357=CARTESIAN_POINT ( 'NONE',  ( 11.35316468749999963, 231.4062500034139873, -1.390361679473963556E-15 ) ) ;
#13393=CARTESIAN_POINT ( 'NONE',  ( -5.676582343749992710, 230.0520833367473017, 9.832129032723422313 ) ) ;
#13446=CARTESIAN_POINT ( 'NONE',  ( -9.832129032723415207, 234.3229166700806445, 5.676582343750005144 ) ) ;
#13449=CARTESIAN_POINT ( 'NONE',  ( -8.311093377946834337, 229.8437500034140157, 8.311093377946837890 ) ) ;
#13506=CARTESIAN_POINT ( 'NONE',  ( 1.836970198721029589E-15, 239.3750000068279746, 10.00000000000000000 ) ) ;
#13543=CARTESIAN_POINT ( 'NONE',  ( -9.999999999999998224, 233.3333333401613174, 2.679491924311235174 ) ) ;
#13552=CARTESIAN_POINT ( 'NONE',  ( -2.679491924311315110, 248.9583333333333428, -9.999999999999950262 ) ) ;
#13554=CARTESIAN_POINT ( 'NONE',  ( -6.951808397369817780E-16, 227.9687500034139873, -11.35316468749999963 ) ) ;
#13583=LINE ( 'NONE', #58260, #9886 ) ;
#13594=CARTESIAN_POINT ( 'NONE',  ( 5.676582343750005144, 230.5729166700806729, 9.832129032723416984 ) ) ;
#13617=DIRECTION ( 'NONE',  ( -0.000000000000000000, -1.000000000000000000, -0.000000000000000000 ) ) ;
#13642=CARTESIAN_POINT ( 'NONE',  ( -2.679491924311222295, 231.0416666666666856, 10.00000000000000178 ) ) ;
#13720=CARTESIAN_POINT ( 'NONE',  ( -11.35316468749999608, 234.1145833367473017, 3.042071309553173730 ) ) ;
#13724=CARTESIAN_POINT ( 'NONE',  ( -10.00000000000000000, 265.0000000000000000, 0.000000000000000000 ) ) ;
#13754=CARTESIAN_POINT ( 'NONE',  ( -5.676582343749992710, 235.0520833367473301, 9.832129032723422313 ) ) ;
#13794=DIRECTION ( 'NONE',  ( 0.000000000000000000, 0.000000000000000000, -1.000000000000000000 ) ) ;
#13808=CARTESIAN_POINT ( 'NONE',  ( 3.042071309553163516, 222.4479166700806729, -11.35316468749999785 ) ) ;
#13812=CARTESIAN_POINT ( 'NONE',  ( 9.832129032723420536, 226.3020833367473301, 5.676582343749996262 ) ) ;
#13814=LINE ( 'NONE', #59866, #53830 ) ;
#13837=DIRECTION ( 'NONE',  ( 0.8660254037844389297, -0.4999999999999994449, 0.000000000000000000 ) ) ;
#13870=CARTESIAN_POINT ( 'NONE',  ( 7.320508075688771044, 236.2500000068279746, -7.320508075688771932 ) ) ;
#13955=CARTESIAN_POINT ( 'NONE',  ( 2.085542519210945334E-15, 235.1562500034140157, 11.35316468749999963 ) ) ;
#14009=CARTESIAN_POINT ( 'NONE',  ( 10.00000000000000178, 227.2916666666666572, 2.679491924311222739 ) ) ;
#14096=CARTESIAN_POINT ( 'NONE',  ( 3.042071309553173286, 225.3645833367473301, 11.35316468749999608 ) ) ;
#14132=CARTESIAN_POINT ( 'NONE',  ( 8.311093377946834337, 232.3437500034140442, -8.311093377946836114 ) ) ;
#14189=CARTESIAN_POINT ( 'NONE',  ( 3.042071309553173286, 220.6770833367472733, 11.35316468749999608 ) ) ;
#14221=CARTESIAN_POINT ( 'NONE',  ( -6.123233995736766282E-16, 233.7500000000000000, -10.00000000000000000 ) ) ;
#14253=CARTESIAN_POINT ( 'NONE',  ( 8.660254037844389075, 245.2083333401613174, 4.999999999999997335 ) ) ;
#14255=ORIENTED_EDGE ( 'NONE', *, *, #72486, .T. ) ;
#14270=CARTESIAN_POINT ( 'NONE',  ( -9.999999999999998224, 258.3333333401612890, 2.679491924311235174 ) ) ;
#14271=CARTESIAN_POINT ( 'NONE',  ( 9.832129032723420536, 260.9895833367473301, 5.676582343749996262 ) ) ;
#14295=CARTESIAN_POINT ( 'NONE',  ( -8.660254037844387298, 242.7083333401613174, -4.999999999999999112 ) ) ;
#14338=CARTESIAN_POINT ( 'NONE',  ( -8.311093377946834337, 239.5312500034140157, 8.311093377946837890 ) ) ;
#14352=CIRCLE ( 'NONE', #58973, 11.00000000000000000 ) ;
#14388=CARTESIAN_POINT ( 'NONE',  ( 0.000000000000000000, 0.000000000000000000, 0.000000000000000000 ) ) ;
#14389=CARTESIAN_POINT ( 'NONE',  ( -9.832129032723418760, 258.8020833367473301, -5.676582343749998927 ) ) ;
#14418=ORIENTED_EDGE ( 'NONE', *, *, #19012, .F. ) ;
#14438=VERTEX_POINT ( 'NONE', #22765 ) ;
#14471=CARTESIAN_POINT ( 'NONE',  ( 11.35316468749999963, 236.4062500034140157, -1.390361679473963556E-15 ) ) ;
#14476=CARTESIAN_POINT ( 'NONE',  ( 8.660254037844385522, 252.9166666666666856, -5.000000000000003553 ) ) ;
#14479=CARTESIAN_POINT ( 'NONE',  ( 4.999999999999997335, 241.4583333401613174, -8.660254037844387298 ) ) ;
#14505=CARTESIAN_POINT ( 'NONE',  ( 9.832129032723420536, 231.3020833367473301, 5.676582343749996262 ) ) ;
#14513=CARTESIAN_POINT ( 'NONE',  ( -10.67658234375000070, 218.5156250051209668, 0.000000000000000000 ) ) ;
#14535=VERTEX_POINT ( 'NONE', #19975 ) ;
#14553=ADVANCED_FACE ( 'NONE', ( #19237 ), #1900, .F. ) ;
#14564=CARTESIAN_POINT ( 'NONE',  ( 11.35316468749999963, 231.7187500034139873, -1.390361679473963556E-15 ) ) ;
#14599=CARTESIAN_POINT ( 'NONE',  ( 8.660254037844385522, 232.9166666666666572, -5.000000000000003553 ) ) ;
#14625=CARTESIAN_POINT ( 'NONE',  ( -7.320508075688770155, 238.7500000068279462, 7.320508075688774596 ) ) ;
#14626=CARTESIAN_POINT ( 'NONE',  ( -6.123233995736766282E-16, 251.8750000068280031, -10.00000000000000000 ) ) ;
#14628=ORIENTED_EDGE ( 'NONE', *, *, #64384, .T. ) ;
#14640=DIRECTION ( 'NONE',  ( -0.000000000000000000, -1.000000000000000000, -0.000000000000000000 ) ) ;
#14647=CARTESIAN_POINT ( 'NONE',  ( -3.042071309553166625, 262.8645833367473301, -11.35316468749999608 ) ) ;
#14675=CARTESIAN_POINT ( 'NONE',  ( 9.832129032723420536, 221.3020833367473301, 5.676582343749996262 ) ) ;
#14688=CARTESIAN_POINT ( 'NONE',  ( -9.999999999999998224, 260.2083333333333144, 2.679491924311235174 ) ) ;
#14713=CARTESIAN_POINT ( 'NONE',  ( 11.35316468749999963, 236.1979166700806445, 3.042071309553159519 ) ) ;
#14732=VECTOR ( 'NONE', #28773, 1000.000000000000227 ) ;
#14762=CARTESIAN_POINT ( 'NONE',  ( 5.676582343750005144, 260.8854166700806445, 9.832129032723416984 ) ) ;
#14807=CARTESIAN_POINT ( 'NONE',  ( 10.00000000000000178, 230.4166666734946034, 2.679491924311222739 ) ) ;
#14845=CARTESIAN_POINT ( 'NONE',  ( -11.35316468749999785, 223.6979166700806445, -3.042071309553164848 ) ) ;
#14850=CARTESIAN_POINT ( 'NONE',  ( 7.320508075688776373, 251.8750000000000000, 7.320508075688767491 ) ) ;
#14857=CARTESIAN_POINT ( 'NONE',  ( 1.836970198721029589E-15, 259.3750000068280315, 10.00000000000000000 ) ) ;
#14890=DIRECTION ( 'NONE',  ( -0.000000000000000000, -1.000000000000000000, -0.000000000000000000 ) ) ;
#14904=CARTESIAN_POINT ( 'NONE',  ( 5.000000000000004441, 236.6666666666666856, 8.660254037844385522 ) ) ;
#14932=CARTESIAN_POINT ( 'NONE',  ( 11.35316468749999608, 221.6145833367473017, -3.042071309553167513 ) ) ;
#14937=CARTESIAN_POINT ( 'NONE',  ( -6.951808397369817780E-16, 257.6562500034140157, -11.35316468749999963 ) ) ;
#14971=CARTESIAN_POINT ( 'NONE',  ( -7.320508075688770155, 223.7500000068279746, 7.320508075688774596 ) ) ;
#14998=CARTESIAN_POINT ( 'NONE',  ( 8.660254037844385522, 226.0416666734946602, -5.000000000000003553 ) ) ;
#15024=CARTESIAN_POINT ( 'NONE',  ( 3.042071309553163516, 252.4479166700806445, -11.35316468749999785 ) ) ;
#15088=CARTESIAN_POINT ( 'NONE',  ( 3.042071309553173286, 240.3645833367473301, 11.35316468749999608 ) ) ;
#15099=EDGE_LOOP ( 'NONE', ( #1003, #72241 ) ) ;
#15116=CARTESIAN_POINT ( 'NONE',  ( 9.999999999999998224, 235.8333333401613174, -2.679491924311229401 ) ) ;
#15142=CARTESIAN_POINT ( 'NONE',  ( 11.35316468749999963, 251.5104166700806729, 3.042071309553159519 ) ) ;
#15165=ADVANCED_FACE ( 'NONE', ( #64080 ), #22973, .F. ) ;
#15197=CARTESIAN_POINT ( 'NONE',  ( -8.660254037844387298, 247.7083333401613174, -4.999999999999999112 ) ) ;
#15229=CARTESIAN_POINT ( 'NONE',  ( 10.00000000000000178, 252.2916666666666856, 2.679491924311222739 ) ) ;
#15266=CARTESIAN_POINT ( 'NONE',  ( 5.292292394482791984, 220.0000000000000568, 8.892157229669562568 ) ) ;
#15305=CARTESIAN_POINT ( 'NONE',  ( -5.676582343749992710, 219.7395833367473301, 9.832129032723422313 ) ) ;
#15308=CARTESIAN_POINT ( 'NONE',  ( -9.832129032723415207, 259.3229166700806445, 5.676582343750005144 ) ) ;
#15345=CARTESIAN_POINT ( 'NONE',  ( 3.042071309553163516, 262.7604166700806445, -11.35316468749999785 ) ) ;
#15373=CARTESIAN_POINT ( 'NONE',  ( 7.320508075688771044, 221.2500000068280031, -7.320508075688771932 ) ) ;
#15384=EDGE_CURVE ( 'NONE', #46331, #72211, #7480, .T. ) ;
#15386=ORIENTED_EDGE ( 'NONE', *, *, #5486, .T. ) ;
#15395=CARTESIAN_POINT ( 'NONE',  ( -11.35316468749999785, 263.6979166700807014, -3.042071309553164848 ) ) ;
#15398=CARTESIAN_POINT ( 'NONE',  ( -5.676582343749992710, 250.0520833367473301, 9.832129032723422313 ) ) ;
#15460=CARTESIAN_POINT ( 'NONE',  ( -6.123233995736766282E-16, 261.8750000068280315, -10.00000000000000000 ) ) ;
#15486=CARTESIAN_POINT ( 'NONE',  ( 2.679491924311206308, 221.4583333333333144, 10.00000000000001421 ) ) ;
#15505=EDGE_CURVE ( 'NONE', #46331, #56463, #64157, .T. ) ;
#15513=CARTESIAN_POINT ( 'NONE',  ( -6.951808397369817780E-16, 252.9687500034140157, -11.35316468749999963 ) ) ;
#15541=EDGE_LOOP ( 'NONE', ( #41570, #71865, #26652 ) ) ;
#15549=CARTESIAN_POINT ( 'NONE',  ( -9.832129032723418760, 258.4895833367473301, -5.676582343749998927 ) ) ;
#15569=PRODUCT ( 'barrel', 'barrel', '', ( #21802 ) ) ;
#15595=VERTEX_POINT ( 'NONE', #44406 ) ;
#15596=CARTESIAN_POINT ( 'NONE',  ( -5.676582343749992710, 219.7395833367473301, 9.832129032723422313 ) ) ;
#15601=CARTESIAN_POINT ( 'NONE',  ( -7.320508075688771932, 254.3750000000000284, -7.320508075688771932 ) ) ;
#15630=CARTESIAN_POINT ( 'NONE',  ( 11.35316468749999963, 221.5104166700806161, 3.042071309553159519 ) ) ;
#15636=CARTESIAN_POINT ( 'NONE',  ( 8.660254037844385522, 247.9166666666666856, -5.000000000000003553 ) ) ;
#15686=CARTESIAN_POINT ( 'NONE',  ( 9.832129032723420536, 260.9895833367473301, 5.676582343749996262 ) ) ;
#15718=CARTESIAN_POINT ( 'NONE',  ( -9.999999999999998224, 223.3333333401613174, 2.679491924311235174 ) ) ;
#15719=CARTESIAN_POINT ( 'NONE',  ( 5.676582343749997150, 257.5520833367473301, -9.832129032723418760 ) ) ;
#15745=CARTESIAN_POINT ( 'NONE',  ( -7.320508075688771932, 227.5000000068279462, -7.320508075688771932 ) ) ;
#15769=CARTESIAN_POINT ( 'NONE',  ( -8.311093377946834337, 254.5312500034139873, 8.311093377946837890 ) ) ;
#15775=CARTESIAN_POINT ( 'NONE',  ( 11.35316468749999963, 251.5104166700806729, 3.042071309553159519 ) ) ;
#15833=CARTESIAN_POINT ( 'NONE',  ( 11.35316468749999608, 226.6145833367473301, -3.042071309553167069 ) ) ;
#15886=CARTESIAN_POINT ( 'NONE',  ( 3.042071309553173286, 260.6770833367473301, 11.35316468749999608 ) ) ;
#15920=CARTESIAN_POINT ( 'NONE',  ( -11.35316468749999785, 258.6979166700807014, -3.042071309553164848 ) ) ;
#15924=CARTESIAN_POINT ( 'NONE',  ( 1.836970198721029589E-15, 251.2500000000000284, 10.00000000000000000 ) ) ;
#15936=CARTESIAN_POINT ( 'NONE',  ( -2.679491924311280471, 249.1666666734946887, 9.999999999999971578 ) ) ;
#15974=CARTESIAN_POINT ( 'NONE',  ( -7.320508075688770155, 250.6249999999999432, 7.320508075688774596 ) ) ;
#15981=CARTESIAN_POINT ( 'NONE',  ( 10.00000000000000178, 260.4166666734946034, 2.679491924311222739 ) ) ;
#16023=ORIENTED_EDGE ( 'NONE', *, *, #42423, .F. ) ;
#16047=CIRCLE ( 'NONE', #10037, 10.00000000000000000 ) ;
#16051=DIRECTION ( 'NONE',  ( 0.000000000000000000, 0.000000000000000000, -1.000000000000000000 ) ) ;
#16055=CARTESIAN_POINT ( 'NONE',  ( -8.311093377946834337, 219.8437500034139873, 8.311093377946837890 ) ) ;
#16058=CARTESIAN_POINT ( 'NONE',  ( -9.628968395985378237, 219.9999999999999716, 4.435878529719882835 ) ) ;
#16086=CARTESIAN_POINT ( 'NONE',  ( -9.832129032723418760, 253.8020833367473017, -5.676582343749998927 ) ) ;
#16111=CARTESIAN_POINT ( 'NONE',  ( -7.320508075688770155, 223.7500000068280031, 7.320508075688774596 ) ) ;
#16131=CARTESIAN_POINT ( 'NONE',  ( 11.35316468749999608, 251.6145833367473585, -3.042071309553167513 ) ) ;
#16135=CARTESIAN_POINT ( 'NONE',  ( -8.311093377946834337, 249.8437500034139589, 8.311093377946837890 ) ) ;
#16183=CARTESIAN_POINT ( 'NONE',  ( 0.000000000000000000, 0.000000000000000000, 0.000000000000000000 ) ) ;
#16198=CARTESIAN_POINT ( 'NONE',  ( 11.35316468749999608, 221.6145833367472733, -3.042071309553167069 ) ) ;
#16221=CARTESIAN_POINT ( 'NONE',  ( -6.123233995736766282E-16, 223.7500000000000000, -10.00000000000000000 ) ) ;
#16232=CARTESIAN_POINT ( 'NONE',  ( -10.99999999999999822, 219.6309830641437202, 2.947441116742358425 ) ) ;
#16249=CARTESIAN_POINT ( 'NONE',  ( 5.676582343749997150, 247.5520833367473301, -9.832129032723418760 ) ) ;
#16284=CARTESIAN_POINT ( 'NONE',  ( 3.042071309553163960, 257.4479166700806445, -11.35316468749999785 ) ) ;
#16318=CARTESIAN_POINT ( 'NONE',  ( 1.224646799147353256E-15, 0.000000000000000000, 10.00000000000000000 ) ) ;
#16322=LINE ( 'NONE', #50298, #14732 ) ;
#16335=CARTESIAN_POINT ( 'NONE',  ( -5.000000000000000888, 244.1666666666666572, -8.660254037844387298 ) ) ;
#16343=FACE_OUTER_BOUND ( 'NONE', #56307, .T. ) ;
#16367=EDGE_LOOP ( 'NONE', ( #62929, #68036, #57926, #43379, #32950, #18369, #71092, #38067, #17176, #17301, #70662, #28893, #53237, #28229, #44066, #28085, #11474, #1659, #74097, #71254, #4009, #51067, #28073, #64452 ) ) ;
#16422=CARTESIAN_POINT ( 'NONE',  ( 3.042071309553173286, 255.3645833367473301, 11.35316468749999608 ) ) ;
#16431=DIRECTION ( 'NONE',  ( -0.000000000000000000, -1.000000000000000000, -0.000000000000000000 ) ) ;
#16434=CARTESIAN_POINT ( 'NONE',  ( 1.224646799147353256E-15, 0.000000000000000000, 10.00000000000000000 ) ) ;
#16458=CARTESIAN_POINT ( 'NONE',  ( 5.676582343750005144, 260.8854166700806445, 9.832129032723416984 ) ) ;
#16486=CARTESIAN_POINT ( 'NONE',  ( -5.000000000000000888, 232.2916666734946602, -8.660254037844387298 ) ) ;
#16507=CARTESIAN_POINT ( 'NONE',  ( -11.35316468749999608, 244.1145833367473017, 3.042071309553173730 ) ) ;
#16513=CARTESIAN_POINT ( 'NONE',  ( -3.042071309553159075, 255.2604166700806445, 11.35316468749999963 ) ) ;
#16550=CARTESIAN_POINT ( 'NONE',  ( -10.00000000000000000, 244.7916666666666856, -2.679491924311226292 ) ) ;
#16572=CARTESIAN_POINT ( 'NONE',  ( 5.676582343750005144, 220.5729166700806729, 9.832129032723416984 ) ) ;
#16591=ORIENTED_EDGE ( 'NONE', *, *, #20196, .T. ) ;
#16592=CARTESIAN_POINT ( 'NONE',  ( 9.999999999999998224, 222.7083333333333428, -2.679491924311229401 ) ) ;
#16623=CARTESIAN_POINT ( 'NONE',  ( 9.832129032723420536, 241.3020833367473301, 5.676582343749996262 ) ) ;
#16630=CARTESIAN_POINT ( 'NONE',  ( 1.836970198721029589E-15, 241.2500000000000284, 10.00000000000000000 ) ) ;
#16650=VERTEX_POINT ( 'NONE', #42356 ) ;
#16677=CONICAL_SURFACE ( 'NONE', #64877, 10.00000000000000000, 0.02777063659342106361 ) ;
#16708=CARTESIAN_POINT ( 'NONE',  ( 1.836970198721029589E-15, 236.2500000000000284, 10.00000000000000000 ) ) ;
#16781=CARTESIAN_POINT ( 'NONE',  ( 1.836970198721029589E-15, 249.3750000068279746, 10.00000000000000000 ) ) ;
#16794=CARTESIAN_POINT ( 'NONE',  ( -8.311093377946834337, 239.5312500034140157, 8.311093377946837890 ) ) ;
#16832=CARTESIAN_POINT ( 'NONE',  ( -9.832129032723418760, 243.8020833367473301, -5.676582343749998927 ) ) ;
#16836=AXIS2_PLACEMENT_3D ( 'NONE', #10003, #61309, #49982 ) ;
#16846=VERTEX_POINT ( 'NONE', #43854 ) ;
#16856=VERTEX_POINT ( 'NONE', #3497 ) ;
#16891=CARTESIAN_POINT ( 'NONE',  ( -3.042071309553159075, 244.9479166700806445, 11.35316468749999963 ) ) ;
#16895=CARTESIAN_POINT ( 'NONE',  ( -9.832129032723418760, 258.8020833367473301, -5.676582343749998927 ) ) ;
#16928=DIRECTION ( 'NONE',  ( -0.000000000000000000, -1.000000000000000000, -0.000000000000000000 ) ) ;
#16934=CARTESIAN_POINT ( 'NONE',  ( -6.123233995736766282E-16, 243.7500000000000284, -10.00000000000000000 ) ) ;
#16958=CARTESIAN_POINT ( 'NONE',  ( 10.00000000000000000, 260.6250000068279746, -1.224646799147353256E-15 ) ) ;
#16984=ORIENTED_EDGE ( 'NONE', *, *, #32853, .T. ) ;
#16991=CARTESIAN_POINT ( 'NONE',  ( -4.999999999999992895, 255.8333333333333712, 8.660254037844390851 ) ) ;
#17005=CARTESIAN_POINT ( 'NONE',  ( 9.832129032723416984, 242.1354166700806445, -5.676582343750003368 ) ) ;
#17020=CARTESIAN_POINT ( 'NONE',  ( 7.320508075688771044, 228.1250000000000000, -7.320508075688771932 ) ) ;
#17042=CARTESIAN_POINT ( 'NONE',  ( -9.832129032723418760, 263.4895833367473301, -5.676582343749998927 ) ) ;
#17085=CARTESIAN_POINT ( 'NONE',  ( 10.00000000000000000, 252.5000000000000000, -1.224646799147353256E-15 ) ) ;
#17090=CARTESIAN_POINT ( 'NONE',  ( -7.320508075688770155, 240.6249999999999716, 7.320508075688774596 ) ) ;
#17176=ORIENTED_EDGE ( 'NONE', *, *, #68024, .T. ) ;
#17177=CARTESIAN_POINT ( 'NONE',  ( 11.35316468749999963, 241.1979166700806729, 3.042071309553159519 ) ) ;
#17213=CARTESIAN_POINT ( 'NONE',  ( -3.042071309553166625, 243.1770833367473017, -11.35316468749999608 ) ) ;
#17268=CARTESIAN_POINT ( 'NONE',  ( 11.35316468749999963, 241.4062500034140157, -1.390361679473963556E-15 ) ) ;
#17272=CARTESIAN_POINT ( 'NONE',  ( 8.311093377946834337, 242.3437500034139873, -8.311093377946836114 ) ) ;
#17301=ORIENTED_EDGE ( 'NONE', *, *, #52389, .T. ) ;
#17327=CARTESIAN_POINT ( 'NONE',  ( 8.660254037844389075, 250.2083333401612890, 4.999999999999997335 ) ) ;
#17373=AXIS2_PLACEMENT_3D ( 'NONE', #56623, #38521, #38889 ) ;
#17379=CARTESIAN_POINT ( 'NONE',  ( -8.311093377946836114, 243.5937500034140157, -8.311093377946836114 ) ) ;
#17415=CARTESIAN_POINT ( 'NONE',  ( -6.951808397369817780E-16, 252.6562500034140157, -11.35316468749999963 ) ) ;
#17439=VERTEX_POINT ( 'NONE', #38668 ) ;
#17466=CARTESIAN_POINT ( 'NONE',  ( 8.660254037844389075, 242.0833333333333428, 4.999999999999997335 ) ) ;
#17474=CARTESIAN_POINT ( 'NONE',  ( -8.660254037844385522, 228.5416666734946602, 5.000000000000004441 ) ) ;
#17480=AXIS2_PLACEMENT_3D ( 'NONE', #46674, #68572, #64035 ) ;
#17510=CARTESIAN_POINT ( 'NONE',  ( 0.000000000000000000, 0.000000000000000000, 0.000000000000000000 ) ) ;
#17539=CARTESIAN_POINT ( 'NONE',  ( -6.123233995736766282E-16, 251.8750000068280031, -10.00000000000000000 ) ) ;
#17554=CARTESIAN_POINT ( 'NONE',  ( 11.35316468749999963, 251.1979166700807014, 3.042071309553159519 ) ) ;
#17589=CARTESIAN_POINT ( 'NONE',  ( -6.951808397369817780E-16, 242.9687500034140157, -11.35316468749999963 ) ) ;
#17603=EDGE_LOOP ( 'NONE', ( #8253, #46123, #45958, #21873 ) ) ;
#17641=CARTESIAN_POINT ( 'NONE',  ( -11.35316468749999963, 238.9062500034140157, 0.000000000000000000 ) ) ;
#17644=CARTESIAN_POINT ( 'NONE',  ( 8.311093377946839666, 241.0937500034139873, 8.311093377946829008 ) ) ;
#17702=CARTESIAN_POINT ( 'NONE',  ( -4.999999999999992895, 258.9583333401613459, 8.660254037844390851 ) ) ;
#17705=ORIENTED_EDGE ( 'NONE', *, *, #48975, .T. ) ;
#17745=ADVANCED_FACE ( 'NONE', ( #34987 ), #53061, .F. ) ;
#17754=CARTESIAN_POINT ( 'NONE',  ( 5.676582343749997150, 242.5520833367473301, -9.832129032723418760 ) ) ;
#17770=CARTESIAN_POINT ( 'NONE',  ( -6.123233995736766282E-16, 228.7500000000000000, -10.00000000000000000 ) ) ;
#17791=CARTESIAN_POINT ( 'NONE',  ( 7.320508075688776373, 225.0000000068280315, 7.320508075688767491 ) ) ;
#17792=CARTESIAN_POINT ( 'NONE',  ( -8.311093377946834337, 244.5312500034139589, 8.311093377946837890 ) ) ;
#17798=EDGE_CURVE ( 'NONE', #16650, #6283, #25748, .T. ) ;
#17838=CARTESIAN_POINT ( 'NONE',  ( 8.660254037844389075, 252.0833333333333144, 4.999999999999997335 ) ) ;
#17843=CARTESIAN_POINT ( 'NONE',  ( 2.679491924311225848, 243.5416666666666572, -10.00000000000000000 ) ) ;
#17932=CARTESIAN_POINT ( 'NONE',  ( 3.042071309553173286, 240.3645833367473301, 11.35316468749999608 ) ) ;
#17958=CARTESIAN_POINT ( 'NONE',  ( -6.123233995736766282E-16, 223.7500000000000000, -10.00000000000000000 ) ) ;
#17964=CARTESIAN_POINT ( 'NONE',  ( 3.042071309553163516, 247.7604166700806445, -11.35316468749999785 ) ) ;
#17977=ORIENTED_EDGE ( 'NONE', *, *, #56464, .T. ) ;
#17995=ORIENTED_EDGE ( 'NONE', *, *, #67048, .T. ) ;
#18020=CARTESIAN_POINT ( 'NONE',  ( -11.35316468749999608, 234.1145833367473017, 3.042071309553173730 ) ) ;
#18021=CYLINDRICAL_SURFACE ( 'NONE', #73510, 10.00000000000000000 ) ;
#18023=CARTESIAN_POINT ( 'NONE',  ( 9.832129032723420536, 241.3020833367473301, 5.676582343749996262 ) ) ;
#18027=VERTEX_POINT ( 'NONE', #34064 ) ;
#18079=CARTESIAN_POINT ( 'NONE',  ( -8.660254037844387298, 257.7083333401612890, -4.999999999999999112 ) ) ;
#18089=ADVANCED_FACE ( 'NONE', ( #69860, #18543 ), #1210, .F. ) ;
#18095=CARTESIAN_POINT ( 'NONE',  ( -10.00000000000000000, 220.0000000000000000, 0.000000000000000000 ) ) ;
#18110=( BOUNDED_CURVE ( )  B_SPLINE_CURVE ( 2, ( #27252, #50267, #10289, #55952, #43867, #4262, #43484, #14807, #37848, #73290, #21592, #73655, #66882 ),
 .UNSPECIFIED., .F., .F. ) 
 B_SPLINE_CURVE_WITH_KNOTS ( ( 3, 2, 2, 2, 2, 2, 3 ),
 ( 0.6944444444444444198, 0.7037037037037037202, 0.7129629629629629095, 0.7222222222222222099, 0.7314814814814815103, 0.7407407407407406996, 0.7500000000000000000 ),
 .UNSPECIFIED. ) 
 CURVE ( )  GEOMETRIC_REPRESENTATION_ITEM ( )  RATIONAL_B_SPLINE_CURVE ( ( 1.000000000000000000, 0.9659258262890683122, 1.000000000000000000, 0.9659258262890683122, 1.000000000000000000, 0.9659258262890683122, 1.000000000000000000, 0.9659258262890683122, 1.000000000000000000, 0.9659258262890683122, 1.000000000000000000, 0.9659258262890683122, 1.000000000000000000 ) ) 
 REPRESENTATION_ITEM ( '' )  );
#18129=DIRECTION ( 'NONE',  ( 0.000000000000000000, 0.000000000000000000, -1.000000000000000000 ) ) ;
#18131=CARTESIAN_POINT ( 'NONE',  ( 3.042071309553173286, 230.6770833367473585, 11.35316468749999608 ) ) ;
#18141=ORIENTED_EDGE ( 'NONE', *, *, #61106, .T. ) ;
#18168=CARTESIAN_POINT ( 'NONE',  ( 5.676582343749997150, 242.2395833367473301, -9.832129032723418760 ) ) ;
#18198=VECTOR ( 'NONE', #37463, 1000.000000000000227 ) ;
#18219=CARTESIAN_POINT ( 'NONE',  ( -8.311093377946836114, 263.5937500034140157, -8.311093377946836114 ) ) ;
#18255=DIRECTION ( 'NONE',  ( -0.000000000000000000, -1.000000000000000000, -0.000000000000000000 ) ) ;
#18287=CARTESIAN_POINT ( 'NONE',  ( 8.660254037844385522, 251.0416666734946318, -5.000000000000003553 ) ) ;
#18301=CARTESIAN_POINT ( 'NONE',  ( 3.042071309553173286, 245.3645833367472733, 11.35316468749999608 ) ) ;
#18311=( NAMED_UNIT ( * ) SI_UNIT ( $, .STERADIAN. ) SOLID_ANGLE_UNIT ( ) );
#18336=CARTESIAN_POINT ( 'NONE',  ( -3.042071309553159075, 245.2604166700806729, 11.35316468749999963 ) ) ;
#18367=CARTESIAN_POINT ( 'NONE',  ( -10.00000000000000000, 265.0000000000000000, 0.000000000000000000 ) ) ;
#18369=ORIENTED_EDGE ( 'NONE', *, *, #58332, .T. ) ;
#18392=CARTESIAN_POINT ( 'NONE',  ( 11.35316468749999963, 231.4062500034139873, -1.390361679473963556E-15 ) ) ;
#18395=CARTESIAN_POINT ( 'NONE',  ( -5.676582343749992710, 235.0520833367473301, 9.832129032723422313 ) ) ;
#18423=LINE ( 'NONE', #41800, #35235 ) ;
#18452=CARTESIAN_POINT ( 'NONE',  ( 9.999999999999998224, 255.8333333401613459, -2.679491924311229401 ) ) ;
#18456=( BOUNDED_CURVE ( )  B_SPLINE_CURVE ( 2, ( #1539, #58871, #41145, #58144, #53574, #52463, #47894, #24519, #65622, #47524, #64150, #13552, #70549 ),
 .UNSPECIFIED., .F., .F. ) 
 B_SPLINE_CURVE_WITH_KNOTS ( ( 3, 2, 2, 2, 2, 2, 3 ),
 ( 0.3055555555555551916, 0.3148148148148144365, 0.3240740740740736814, 0.3333333333333329263, 0.3425925925925922821, 0.3518518518518515270, 0.3611111111111107719 ),
 .UNSPECIFIED. ) 
 CURVE ( )  GEOMETRIC_REPRESENTATION_ITEM ( )  RATIONAL_B_SPLINE_CURVE ( ( 1.000000000000001332, 0.9659258262890668689, 1.000000000000000000, 0.9659258262890683122, 1.000000000000000000, 0.9659258262890683122, 1.000000000000000000, 0.9659258262890683122, 1.000000000000000000, 0.9659258262890683122, 1.000000000000000000, 0.9659258262890695335, 0.9999999999999987788 ) ) 
 REPRESENTATION_ITEM ( '' )  );
#18500=CARTESIAN_POINT ( 'NONE',  ( 9.832129032723420536, 231.3020833367473301, 5.676582343749996262 ) ) ;
#18538=CARTESIAN_POINT ( 'NONE',  ( -5.676582343749992710, 244.7395833367473301, 9.832129032723422313 ) ) ;
#18543=FACE_OUTER_BOUND ( 'NONE', #51385, .T. ) ;
#18560=CARTESIAN_POINT ( 'NONE',  ( -2.679491924311383499, 262.0833333401613459, -9.999999999999909406 ) ) ;
#18587=CARTESIAN_POINT ( 'NONE',  ( -9.999999999999998224, 230.2083333333333428, 2.679491924311235618 ) ) ;
#18663=CARTESIAN_POINT ( 'NONE',  ( 7.320508075688771044, 256.2500000068279746, -7.320508075688771932 ) ) ;
#18673=CARTESIAN_POINT ( 'NONE',  ( -9.832129032723415207, 234.3229166700806445, 5.676582343750005144 ) ) ;
#18679=CARTESIAN_POINT ( 'NONE',  ( -5.000000000000000888, 264.1666666666666856, -8.660254037844387298 ) ) ;
#18703=CARTESIAN_POINT ( 'NONE',  ( -10.00000000000000000, 237.9166666734946602, -2.679491924311226292 ) ) ;
#18708=CARTESIAN_POINT ( 'NONE',  ( 3.042071309553163516, 227.7604166700806445, -11.35316468749999785 ) ) ;
#18755=EDGE_CURVE ( 'NONE', #23729, #17439, #11045, .T. ) ;
#18761=CARTESIAN_POINT ( 'NONE',  ( 8.311093377946834337, 227.0312500034140157, -8.311093377946836114 ) ) ;
#18765=CARTESIAN_POINT ( 'NONE',  ( -3.042071309553159075, 240.2604166700806729, 11.35316468749999963 ) ) ;
#18799=CARTESIAN_POINT ( 'NONE',  ( -2.679491924311222295, 224.1666666734946318, 10.00000000000000178 ) ) ;
#18823=CARTESIAN_POINT ( 'NONE',  ( -2.679491924311222295, 254.1666666734946318, 10.00000000000000178 ) ) ;
#18865=DIRECTION ( 'NONE',  ( -0.000000000000000000, -1.000000000000000000, -0.000000000000000000 ) ) ;
#18867=CARTESIAN_POINT ( 'NONE',  ( -8.311093377946836114, 223.5937500034139589, -8.311093377946836114 ) ) ;
#18903=CARTESIAN_POINT ( 'NONE',  ( -11.35316468749999608, 249.1145833367473017, 3.042071309553173730 ) ) ;
#18940=LINE ( 'NONE', #64954, #53085 ) ;
#18952=CARTESIAN_POINT ( 'NONE',  ( 5.000000000000004441, 226.6666666666666856, 8.660254037844385522 ) ) ;
#18960=CARTESIAN_POINT ( 'NONE',  ( 1.836970198721029589E-15, 241.2500000000000284, 10.00000000000000000 ) ) ;
#19012=EDGE_CURVE ( 'NONE', #29523, #73780, #46235, .T. ) ;
#19024=CARTESIAN_POINT ( 'NONE',  ( 10.00000000000000000, 255.6250000068279746, -1.224646799147353256E-15 ) ) ;
#19035=CARTESIAN_POINT ( 'NONE',  ( 11.35316468749999608, 231.6145833367473017, -3.042071309553167069 ) ) ;
#19066=CARTESIAN_POINT ( 'NONE',  ( 7.071067751884405617, 220.0000000000000284, 7.071067871846544506 ) ) ;
#19068=CARTESIAN_POINT ( 'NONE',  ( 5.676582343750005144, 225.8854166700806729, 9.832129032723416984 ) ) ;
#19118=CARTESIAN_POINT ( 'NONE',  ( -5.676582343749992710, 229.7395833367473301, 9.832129032723422313 ) ) ;
#19122=CARTESIAN_POINT ( 'NONE',  ( 9.832129032723416984, 222.1354166700806729, -5.676582343750003368 ) ) ;
#19135=EDGE_LOOP ( 'NONE', ( #67627, #70497, #35638, #40496 ) ) ;
#19181=CARTESIAN_POINT ( 'NONE',  ( 2.679491924311225848, 236.6666666734946602, -10.00000000000000000 ) ) ;
#19230=CARTESIAN_POINT ( 'NONE',  ( 8.311093377946834337, 232.3437500034140157, -8.311093377946836114 ) ) ;
#19237=FACE_OUTER_BOUND ( 'NONE', #29340, .T. ) ;
#19264=CARTESIAN_POINT ( 'NONE',  ( -11.35316468749999963, 238.9062500034140157, 0.000000000000000000 ) ) ;
#19294=ORIENTED_EDGE ( 'NONE', *, *, #47649, .F. ) ;
#19311=CARTESIAN_POINT ( 'NONE',  ( -9.832129032723418760, 263.8020833367473301, -5.676582343749998927 ) ) ;
#19319=CARTESIAN_POINT ( 'NONE',  ( 8.660254037844389075, 242.0833333333333428, 4.999999999999997335 ) ) ;
#19392=CARTESIAN_POINT ( 'NONE',  ( -5.676582343749992710, 234.7395833367473301, 9.832129032723422313 ) ) ;
#19396=CARTESIAN_POINT ( 'NONE',  ( -6.123233995736766282E-16, 246.8750000068280031, -10.00000000000000000 ) ) ;
#19397=CARTESIAN_POINT ( 'NONE',  ( -10.00000000000000000, 260.0000000000000000, 0.000000000000000000 ) ) ;
#19426=ORIENTED_EDGE ( 'NONE', *, *, #12160, .F. ) ;
#19430=CARTESIAN_POINT ( 'NONE',  ( -11.35316468749999785, 234.0104166700806161, -3.042071309553164848 ) ) ;
#19483=CARTESIAN_POINT ( 'NONE',  ( 9.832129032723420536, 230.9895833367473301, 5.676582343749996262 ) ) ;
#19486=CARTESIAN_POINT ( 'NONE',  ( 8.311093377946839666, 221.0937500034139589, 8.311093377946829008 ) ) ;
#19544=CARTESIAN_POINT ( 'NONE',  ( -2.679491924311222295, 234.1666666734946602, 10.00000000000000178 ) ) ;
#19570=CARTESIAN_POINT ( 'NONE',  ( 5.676582343749997150, 262.5520833367473301, -9.832129032723418760 ) ) ;
#19572=ORIENTED_EDGE ( 'NONE', *, *, #22365, .F. ) ;
#19593=CARTESIAN_POINT ( 'NONE',  ( -3.042071309553159075, 235.2604166700806161, 11.35316468749999963 ) ) ;
#19623=( BOUNDED_CURVE ( )  B_SPLINE_CURVE ( 2, ( #48823, #26933, #71830, #43163, #3190, #72206, #49952, #15981, #73340, #61649, #39011, #66548, #14857 ),
 .UNSPECIFIED., .F., .F. ) 
 B_SPLINE_CURVE_WITH_KNOTS ( ( 3, 2, 2, 2, 2, 2, 3 ),
 ( 0.02777777777777718296, 0.03703703703703645211, 0.04629629629629572474, 0.05555555555555498348, 0.06481481481481425611, 0.07407407407407351485, 0.08333333333333278747 ),
 .UNSPECIFIED. ) 
 CURVE ( )  GEOMETRIC_REPRESENTATION_ITEM ( )  RATIONAL_B_SPLINE_CURVE ( ( 1.000000000000002220, 0.9659258262890662028, 1.000000000000000000, 0.9659258262890683122, 1.000000000000000000, 0.9659258262890683122, 1.000000000000000000, 0.9659258262890683122, 1.000000000000000000, 0.9659258262890683122, 1.000000000000000000, 0.9659258262890703106, 0.9999999999999980016 ) ) 
 REPRESENTATION_ITEM ( '' )  );
#19632=CARTESIAN_POINT ( 'NONE',  ( 11.35316468749999608, 236.6145833367473301, -3.042071309553167069 ) ) ;
#19678=AXIS2_PLACEMENT_3D ( 'NONE', #20226, #71536, #32322 ) ;
#19682=CARTESIAN_POINT ( 'NONE',  ( -8.660254037844385522, 230.4166666666666856, 5.000000000000004441 ) ) ;
#19769=CARTESIAN_POINT ( 'NONE',  ( 11.35316468749999608, 236.6145833367473301, -3.042071309553167069 ) ) ;
#19771=CARTESIAN_POINT ( 'NONE',  ( -11.35316468749999963, 264.0625000034140157, 0.000000000000000000 ) ) ;
#19773=CARTESIAN_POINT ( 'NONE',  ( 9.999999999999998224, 262.7083333333333712, -2.679491924311229401 ) ) ;
#19799=CARTESIAN_POINT ( 'NONE',  ( 2.679491924311283579, 221.6666666734946887, -9.999999999999969802 ) ) ;
#19802=CARTESIAN_POINT ( 'NONE',  ( 5.676582343750005144, 235.8854166700806729, 9.832129032723416984 ) ) ;
#19856=CARTESIAN_POINT ( 'NONE',  ( -9.832129032723415207, 219.3229166700806729, 5.676582343750005144 ) ) ;
#19858=CARTESIAN_POINT ( 'NONE',  ( -8.311093377946836114, 228.5937500034139873, -8.311093377946836114 ) ) ;
#19891=CARTESIAN_POINT ( 'NONE',  ( 9.999999999999998224, 232.7083333333333428, -2.679491924311229401 ) ) ;
#19905=VECTOR ( 'NONE', #20515, 1000.000000000000000 ) ;
#19917=CARTESIAN_POINT ( 'NONE',  ( 2.679491924311235174, 239.5833333401612606, 9.999999999999998224 ) ) ;
#19967=CARTESIAN_POINT ( 'NONE',  ( -8.311093377946834337, 219.8437500034139873, 8.311093377946837890 ) ) ;
#19975=CARTESIAN_POINT ( 'NONE',  ( -6.123233995736766282E-16, 248.7500000000000284, -10.00000000000000000 ) ) ;
#20001=CARTESIAN_POINT ( 'NONE',  ( -5.676582343750000703, 233.0729166700806729, -9.832129032723418760 ) ) ;
#20045=CARTESIAN_POINT ( 'NONE',  ( -9.832129032723415207, 249.6354166700806445, 5.676582343750005144 ) ) ;
#20134=ORIENTED_EDGE ( 'NONE', *, *, #45783, .F. ) ;
#20135=CARTESIAN_POINT ( 'NONE',  ( 9.832129032723416984, 231.8229166700806445, -5.676582343750003368 ) ) ;
#20140=CARTESIAN_POINT ( 'NONE',  ( 10.00000000000000000, 252.5000000000000000, -1.224646799147353256E-15 ) ) ;
#20143=CARTESIAN_POINT ( 'NONE',  ( 1.836970198721029589E-15, 239.3750000068279746, 10.00000000000000000 ) ) ;
#20167=CARTESIAN_POINT ( 'NONE',  ( 8.311093377946834337, 237.3437500034139589, -8.311093377946836114 ) ) ;
#20169=EDGE_LOOP ( 'NONE', ( #27135, #53648, #60598, #38125 ) ) ;
#20174=CARTESIAN_POINT ( 'NONE',  ( 1.921951731159528443, 219.9999999999999432, 10.68631426227777226 ) ) ;
#20196=EDGE_CURVE ( 'NONE', #53701, #23527, #18423, .T. ) ;
#20224=CARTESIAN_POINT ( 'NONE',  ( 3.042071309553173286, 230.6770833367473585, 11.35316468749999608 ) ) ;
#20226=CARTESIAN_POINT ( 'NONE',  ( 0.000000000000000000, 0.000000000000000000, 0.000000000000000000 ) ) ;
#20284=CARTESIAN_POINT ( 'NONE',  ( 10.00000000000000178, 235.4166666734946602, 2.679491924311222739 ) ) ;
#20285=CARTESIAN_POINT ( 'NONE',  ( -2.679491924311337314, 252.0833333401613174, -9.999999999999936051 ) ) ;
#20305=CARTESIAN_POINT ( 'NONE',  ( 11.35316468749999963, 256.1979166700806445, 3.042071309553159519 ) ) ;
#20310=CARTESIAN_POINT ( 'NONE',  ( -6.951808397369817780E-16, 262.9687500034140157, -11.35316468749999963 ) ) ;
#20331=FACE_OUTER_BOUND ( 'NONE', #21427, .T. ) ;
#20372=CARTESIAN_POINT ( 'NONE',  ( 8.311093377946839666, 240.7812500034140157, 8.311093377946829008 ) ) ;
#20422=CARTESIAN_POINT ( 'NONE',  ( 0.000000000000000000, 0.000000000000000000, 0.000000000000000000 ) ) ;
#20423=CARTESIAN_POINT ( 'NONE',  ( -5.676582343749992710, 255.0520833367473301, 9.832129032723422313 ) ) ;
#20506=CARTESIAN_POINT ( 'NONE',  ( 11.35316468749999963, 221.1979166700806161, 3.042071309553159519 ) ) ;
#20511=CARTESIAN_POINT ( 'NONE',  ( 7.320508075688776373, 256.8750000000000000, 7.320508075688767491 ) ) ;
#20515=DIRECTION ( 'NONE',  ( -0.000000000000000000, -1.000000000000000000, -0.000000000000000000 ) ) ;
#20570=CARTESIAN_POINT ( 'NONE',  ( 8.660254037844389075, 237.0833333333333428, 4.999999999999997335 ) ) ;
#20598=CARTESIAN_POINT ( 'NONE',  ( -3.042071309553159075, 224.9479166700806445, 11.35316468749999963 ) ) ;
#20601=CARTESIAN_POINT ( 'NONE',  ( -3.042071309553159075, 259.9479166700807014, 11.35316468749999963 ) ) ;
#20666=CARTESIAN_POINT ( 'NONE',  ( 2.679491924311235174, 244.5833333401612606, 9.999999999999998224 ) ) ;
#20667=CARTESIAN_POINT ( 'NONE',  ( -7.320508075688770155, 253.7500000068279462, 7.320508075688774596 ) ) ;
#20687=CARTESIAN_POINT ( 'NONE',  ( -6.951808397369817780E-16, 257.6562500034140157, -11.35316468749999963 ) ) ;
#20713=CARTESIAN_POINT ( 'NONE',  ( -10.00000000000000000, 242.9166666734946318, -2.679491924311226292 ) ) ;
#20755=CARTESIAN_POINT ( 'NONE',  ( 8.311093377946839666, 230.7812500034139589, 8.311093377946829008 ) ) ;
#20804=FACE_OUTER_BOUND ( 'NONE', #49673, .T. ) ;
#20806=CARTESIAN_POINT ( 'NONE',  ( 11.35316468749999963, 256.5104166700807014, 3.042071309553159519 ) ) ;
#20887=EDGE_CURVE ( 'NONE', #9311, #8879, #9283, .T. ) ;
#20892=CARTESIAN_POINT ( 'NONE',  ( 10.00000000000000178, 257.2916666666666856, 2.679491924311222739 ) ) ;
#20977=CARTESIAN_POINT ( 'NONE',  ( -11.35316468749999963, 258.9062500034140157, 0.000000000000000000 ) ) ;
#21013=CARTESIAN_POINT ( 'NONE',  ( -6.951808397369817780E-16, 257.9687500034140157, -11.35316468749999963 ) ) ;
#21025=FACE_OUTER_BOUND ( 'NONE', #47787, .T. ) ;
#21040=CARTESIAN_POINT ( 'NONE',  ( -7.320508075688770155, 228.7500000068279462, 7.320508075688774596 ) ) ;
#21068=CARTESIAN_POINT ( 'NONE',  ( -11.35316468749999785, 254.0104166700806729, -3.042071309553164848 ) ) ;
#21100=EDGE_CURVE ( 'NONE', #71847, #58601, #16322, .T. ) ;
#21129=CARTESIAN_POINT ( 'NONE',  ( -9.832129032723415207, 219.3229166700806729, 5.676582343750005144 ) ) ;
#21159=VERTEX_POINT ( 'NONE', #45380 ) ;
#21178=CARTESIAN_POINT ( 'NONE',  ( 8.311093377946839666, 251.0937500034139873, 8.311093377946829008 ) ) ;
#21216=ADVANCED_FACE ( 'NONE', ( #45754 ), #68395, .F. ) ;
#21232=CARTESIAN_POINT ( 'NONE',  ( -6.123233995736766282E-16, 246.8750000068280031, -10.00000000000000000 ) ) ;
#21260=CARTESIAN_POINT ( 'NONE',  ( 11.35316468749999608, 221.6145833367472733, -3.042071309553167069 ) ) ;
#21265=CARTESIAN_POINT ( 'NONE',  ( -2.679491924311228512, 248.9583333333333712, -9.999999999999998224 ) ) ;
#21273=CARTESIAN_POINT ( 'NONE',  ( 0.000000000000000000, 220.0000000000000284, 11.00000000000000000 ) ) ;
#21350=CARTESIAN_POINT ( 'NONE',  ( -11.35316468749999963, 219.2187500034139873, 0.000000000000000000 ) ) ;
#21371=DIRECTION ( 'NONE',  ( 0.000000000000000000, 0.000000000000000000, -1.000000000000000000 ) ) ;
#21384=CARTESIAN_POINT ( 'NONE',  ( 9.832129032723420536, 256.3020833367473301, 5.676582343749996262 ) ) ;
#21411=CARTESIAN_POINT ( 'NONE',  ( 1.836970198721029589E-15, 229.3750000068279746, 10.00000000000000000 ) ) ;
#21412=CARTESIAN_POINT ( 'NONE',  ( -2.679491924311106832, 254.1666666734946318, 10.00000000000006928 ) ) ;
#21416=EDGE_CURVE ( 'NONE', #72211, #27344, #6865, .T. ) ;
#21420=ORIENTED_EDGE ( 'NONE', *, *, #50752, .F. ) ;
#21427=EDGE_LOOP ( 'NONE', ( #1237, #33964, #45833, #26936, #7044 ) ) ;
#21434=CARTESIAN_POINT ( 'NONE',  ( -7.320508075688770155, 258.7500000068279746, 7.320508075688774596 ) ) ;
#21435=CARTESIAN_POINT ( 'NONE',  ( 2.085542519210945334E-15, 255.1562500034140157, 11.35316468749999963 ) ) ;
#21439=CARTESIAN_POINT ( 'NONE',  ( -6.951808397369817780E-16, 252.9687500034140157, -11.35316468749999963 ) ) ;
#21480=CARTESIAN_POINT ( 'NONE',  ( -4.999999999999992895, 245.8333333333333428, 8.660254037844390851 ) ) ;
#21502=CARTESIAN_POINT ( 'NONE',  ( 3.042071309553163960, 227.4479166700806729, -11.35316468749999785 ) ) ;
#21532=EDGE_LOOP ( 'NONE', ( #50535, #57557, #50001, #31192 ) ) ;
#21551=CARTESIAN_POINT ( 'NONE',  ( 9.832129032723420536, 261.3020833367473301, 5.676582343749996262 ) ) ;
#21592=CARTESIAN_POINT ( 'NONE',  ( 5.000000000000004441, 229.7916666734946602, 8.660254037844385522 ) ) ;
#21632=CARTESIAN_POINT ( 'NONE',  ( -3.042071309553166181, 222.8645833367473301, -11.35316468749999608 ) ) ;
#21637=CARTESIAN_POINT ( 'NONE',  ( -7.320508075688770155, 245.6250000000000000, 7.320508075688774596 ) ) ;
#21673=CARTESIAN_POINT ( 'NONE',  ( 1.836970198721029589E-15, 246.2500000000000284, 10.00000000000000000 ) ) ;
#21692=CARTESIAN_POINT ( 'NONE',  ( 0.000000000000000000, 0.000000000000000000, 0.000000000000000000 ) ) ;
#21718=CARTESIAN_POINT ( 'NONE',  ( 9.832129032723416984, 261.8229166700807014, -5.676582343750003368 ) ) ;
#21753=CARTESIAN_POINT ( 'NONE',  ( -5.676582343750000703, 263.3854166700806445, -9.832129032723418760 ) ) ;
#21763=EDGE_CURVE ( 'NONE', #6788, #6283, #55576, .T. ) ;
#21766=DIRECTION ( 'NONE',  ( 0.000000000000000000, 0.000000000000000000, -1.000000000000000000 ) ) ;
#21779=CARTESIAN_POINT ( 'NONE',  ( -5.000000000000000888, 227.2916666734946602, -8.660254037844387298 ) ) ;
#21800=CARTESIAN_POINT ( 'NONE',  ( 11.35316468749999963, 246.1979166700806445, 3.042071309553159519 ) ) ;
#21802=PRODUCT_CONTEXT ( 'NONE', #48113, 'mechanical' ) ;
#21804=CARTESIAN_POINT ( 'NONE',  ( 11.35316468749999608, 251.9270833367473301, -3.042071309553167069 ) ) ;
#21810=CARTESIAN_POINT ( 'NONE',  ( -11.35316468749999963, 218.9062500034139873, 0.000000000000000000 ) ) ;
#21843=CARTESIAN_POINT ( 'NONE',  ( -2.679491924311358186, 258.9583333333333712, -9.999999999999923617 ) ) ;
#21870=CARTESIAN_POINT ( 'NONE',  ( 8.311093377946834337, 222.0312500034139873, -8.311093377946836114 ) ) ;
#21873=ORIENTED_EDGE ( 'NONE', *, *, #48975, .F. ) ;
#21918=CARTESIAN_POINT ( 'NONE',  ( -6.951808397369817780E-16, 242.9687500034140157, -11.35316468749999963 ) ) ;
#21955=CARTESIAN_POINT ( 'NONE',  ( -5.676582343749992710, 259.7395833367473301, 9.832129032723422313 ) ) ;
#21981=EDGE_CURVE ( 'NONE', #71972, #66887, #13814, .T. ) ;
#22004=CARTESIAN_POINT ( 'NONE',  ( -3.042071309553159075, 219.9479166700806445, 11.35316468749999963 ) ) ;
#22009=CARTESIAN_POINT ( 'NONE',  ( -5.000000000000000888, 234.1666666666666856, -8.660254037844387298 ) ) ;
#22090=CARTESIAN_POINT ( 'NONE',  ( 3.042071309553173286, 260.3645833367473301, 11.35316468749999608 ) ) ;
#22110=CARTESIAN_POINT ( 'NONE',  ( 9.832129032723416984, 222.1354166700806729, -5.676582343750003368 ) ) ;
#22124=CARTESIAN_POINT ( 'NONE',  ( 5.676582343749997150, 252.5520833367473301, -9.832129032723418760 ) ) ;
#22150=CARTESIAN_POINT ( 'NONE',  ( 2.679491924311235174, 229.5833333401612890, 9.999999999999998224 ) ) ;
#22176=CARTESIAN_POINT ( 'NONE',  ( 11.35316468749999963, 241.1979166700806729, 3.042071309553159519 ) ) ;
#22180=CARTESIAN_POINT ( 'NONE',  ( -6.951808397369817780E-16, 257.9687500034140157, -11.35316468749999963 ) ) ;
#22237=CARTESIAN_POINT ( 'NONE',  ( 5.676582343749997150, 222.2395833367473017, -9.832129032723418760 ) ) ;
#22247=ADVANCED_FACE ( 'NONE', ( #66633 ), #55335, .F. ) ;
#22288=CARTESIAN_POINT ( 'NONE',  ( -9.832129032723415207, 244.6354166700806445, 5.676582343750005144 ) ) ;
#22319=FACE_OUTER_BOUND ( 'NONE', #16367, .T. ) ;
#22334=LINE ( 'NONE', #5753, #29332 ) ;
#22365=EDGE_CURVE ( 'NONE', #6788, #27344, #29695, .T. ) ;
#22370=CARTESIAN_POINT ( 'NONE',  ( -4.999999999999992895, 240.8333333333333428, 8.660254037844390851 ) ) ;
#22443=CARTESIAN_POINT ( 'NONE',  ( 7.320508075688771044, 251.2500000068279178, -7.320508075688771932 ) ) ;
#22456=CARTESIAN_POINT ( 'NONE',  ( 9.832129032723420536, 240.9895833367473301, 5.676582343749996262 ) ) ;
#22491=CARTESIAN_POINT ( 'NONE',  ( 8.311093377946839666, 256.0937500034140157, 8.311093377946830785 ) ) ;
#22521=CARTESIAN_POINT ( 'NONE',  ( -10.00000000000000000, 228.1250000068279746, 0.000000000000000000 ) ) ;
#22532=PRODUCT_DEFINITION_FORMATION_WITH_SPECIFIED_SOURCE ( 'ANY', '', #15569, .NOT_KNOWN. ) ;
#22547=CARTESIAN_POINT ( 'NONE',  ( 3.042071309553163516, 247.4479166700806445, -11.35316468749999785 ) ) ;
#22548=FACE_OUTER_BOUND ( 'NONE', #19135, .T. ) ;
#22552=CARTESIAN_POINT ( 'NONE',  ( 9.832129032723420536, 251.3020833367473017, 5.676582343749996262 ) ) ;
#22577=CARTESIAN_POINT ( 'NONE',  ( -10.00000000000000000, 235.0000000000000284, 0.000000000000000000 ) ) ;
#22612=CARTESIAN_POINT ( 'NONE',  ( -5.676582343749992710, 219.7395833367473301, 9.832129032723422313 ) ) ;
#22659=CARTESIAN_POINT ( 'NONE',  ( 0.000000000000000000, 220.0000000000000284, 0.000000000000000000 ) ) ;
#22661=CARTESIAN_POINT ( 'NONE',  ( 8.311093377946839666, 241.0937500034139873, 8.311093377946829008 ) ) ;
#22677=CARTESIAN_POINT ( 'NONE',  ( 4.999999999999997335, 228.3333333333333428, -8.660254037844387298 ) ) ;
#22698=CARTESIAN_POINT ( 'NONE',  ( -8.311093377946834337, 259.5312500034139589, 8.311093377946837890 ) ) ;
#22734=DIRECTION ( 'NONE',  ( 0.000000000000000000, 0.000000000000000000, -1.000000000000000000 ) ) ;
#22748=CARTESIAN_POINT ( 'NONE',  ( -8.660254037844385522, 235.4166666666666572, 5.000000000000004441 ) ) ;
#22765=CARTESIAN_POINT ( 'NONE',  ( 1.836970198721029589E-15, 236.2500000000000284, 10.00000000000000000 ) ) ;
#22784=CARTESIAN_POINT ( 'NONE',  ( 5.000000000000004441, 246.6666666666666856, 8.660254037844385522 ) ) ;
#22816=ORIENTED_EDGE ( 'NONE', *, *, #9654, .F. ) ;
#22832=ADVANCED_FACE ( 'NONE', ( #31848 ), #26167, .F. ) ;
#22837=CARTESIAN_POINT ( 'NONE',  ( 11.35316468749999963, 246.4062500034139873, -1.390361679473963556E-15 ) ) ;
#22848=CARTESIAN_POINT ( 'NONE',  ( 0.000000000000000000, 0.000000000000000000, -10.00000000000000000 ) ) ;
#22869=CARTESIAN_POINT ( 'NONE',  ( -2.679491924311222295, 226.0416666666666288, 10.00000000000000178 ) ) ;
#22876=CARTESIAN_POINT ( 'NONE',  ( 3.042071309553163516, 242.7604166700806729, -11.35316468749999785 ) ) ;
#22905=CARTESIAN_POINT ( 'NONE',  ( -9.999999999999998224, 218.3333333401612606, 2.679491924311235618 ) ) ;
#22934=CARTESIAN_POINT ( 'NONE',  ( 11.35316468749999608, 241.6145833367473585, -3.042071309553167513 ) ) ;
#22938=CARTESIAN_POINT ( 'NONE',  ( 8.311093377946839666, 236.0937500034139589, 8.311093377946829008 ) ) ;
#22946=CARTESIAN_POINT ( 'NONE',  ( 0.000000000000000000, 265.0000000000000000, -19.00000000000003553 ) ) ;
#22973=CYLINDRICAL_SURFACE ( 'NONE', #2514, 10.00000000000000000 ) ;
#22984=AXIS2_PLACEMENT_3D ( 'NONE', #12702, #24759, #13794 ) ;
#22999=CARTESIAN_POINT ( 'NONE',  ( -7.320508075688770155, 248.7500000068279746, 7.320508075688774596 ) ) ;
#23043=CARTESIAN_POINT ( 'NONE',  ( -8.311093377946834337, 244.8437500034140157, 8.311093377946837890 ) ) ;
#23050=CARTESIAN_POINT ( 'NONE',  ( -8.660254037844385522, 240.4166666666666572, 5.000000000000004441 ) ) ;
#23086=ORIENTED_EDGE ( 'NONE', *, *, #1329, .T. ) ;
#23112=CARTESIAN_POINT ( 'NONE',  ( -9.999999999999998224, 220.2083333333333428, 2.679491924311235174 ) ) ;
#23128=CARTESIAN_POINT ( 'NONE',  ( -6.123233995736766282E-16, 243.7500000000000284, -10.00000000000000000 ) ) ;
#23143=DIRECTION ( 'NONE',  ( -0.000000000000000000, -1.000000000000000000, -0.000000000000000000 ) ) ;
#23216=CARTESIAN_POINT ( 'NONE',  ( -11.35316468749999608, 244.1145833367472733, 3.042071309553173730 ) ) ;
#23220=CARTESIAN_POINT ( 'NONE',  ( -10.04299372122919820, 220.0000000000001137, 2.556404203812648213 ) ) ;
#23251=CARTESIAN_POINT ( 'NONE',  ( -11.35316468749999963, 249.2187500034139873, 0.000000000000000000 ) ) ;
#23254=CARTESIAN_POINT ( 'NONE',  ( 0.000000000000000000, 265.0000000000000000, -10.00000000000000000 ) ) ;
#23302=CARTESIAN_POINT ( 'NONE',  ( -8.311093377946834337, 239.5312500034139873, 8.311093377946837890 ) ) ;
#23307=CARTESIAN_POINT ( 'NONE',  ( -6.951808397369817780E-16, 242.9687500034140157, -11.35316468749999963 ) ) ;
#23338=ORIENTED_EDGE ( 'NONE', *, *, #50615, .T. ) ;
#23356=EDGE_LOOP ( 'NONE', ( #15386, #12369, #55095 ) ) ;
#23364=CARTESIAN_POINT ( 'NONE',  ( 2.679491924311225848, 251.6666666734946602, -10.00000000000000000 ) ) ;
#23384=VERTEX_POINT ( 'NONE', #25334 ) ;
#23414=CARTESIAN_POINT ( 'NONE',  ( -11.35316468749999608, 244.4270833367473017, 3.042071309553173730 ) ) ;
#23450=CARTESIAN_POINT ( 'NONE',  ( 9.832129032723420536, 245.9895833367473301, 5.676582343749996262 ) ) ;
#23498=CARTESIAN_POINT ( 'NONE',  ( 4.999999999999997335, 233.3333333333333428, -8.660254037844387298 ) ) ;
#23527=VERTEX_POINT ( 'NONE', #3461 ) ;
#23548=ORIENTED_EDGE ( 'NONE', *, *, #65344, .F. ) ;
#23585=CARTESIAN_POINT ( 'NONE',  ( -3.042071309553166181, 242.8645833367473017, -11.35316468749999608 ) ) ;
#23622=CARTESIAN_POINT ( 'NONE',  ( 8.311093377946834337, 242.3437500034139873, -8.311093377946836114 ) ) ;
#23627=EDGE_CURVE ( 'NONE', #6788, #41315, #26181, .T. ) ;
#23657=ORIENTED_EDGE ( 'NONE', *, *, #65174, .F. ) ;
#23678=CARTESIAN_POINT ( 'NONE',  ( 11.35316468749999963, 236.1979166700806445, 3.042071309553159519 ) ) ;
#23681=CARTESIAN_POINT ( 'NONE',  ( 11.35316468749999963, 241.5104166700806729, 3.042071309553159519 ) ) ;
#23729=VERTEX_POINT ( 'NONE', #5807 ) ;
#23737=CARTESIAN_POINT ( 'NONE',  ( -5.000000000000000888, 247.2916666734946318, -8.660254037844387298 ) ) ;
#23780=CARTESIAN_POINT ( 'NONE',  ( -10.00000000000000000, 233.1250000068279746, 0.000000000000000000 ) ) ;
#23789=CARTESIAN_POINT ( 'NONE',  ( 5.676582343749997150, 227.5520833367473017, -9.832129032723418760 ) ) ;
#23825=CARTESIAN_POINT ( 'NONE',  ( 11.35316468749999963, 251.4062500034139873, -1.390361679473963556E-15 ) ) ;
#23837=ORIENTED_EDGE ( 'NONE', *, *, #42423, .T. ) ;
#23874=CARTESIAN_POINT ( 'NONE',  ( -2.679491924311222295, 226.0416666666666288, 10.00000000000000178 ) ) ;
#23878=ADVANCED_FACE ( 'NONE', ( #59344 ), #2360, .T. ) ;
#23885=EDGE_LOOP ( 'NONE', ( #1021, #41028, #33200, #35605 ) ) ;
#23942=CARTESIAN_POINT ( 'NONE',  ( 7.320508075688776373, 250.0000000068279746, 7.320508075688767491 ) ) ;
#23948=CARTESIAN_POINT ( 'NONE',  ( 7.071067751884405617, 220.0000000000000284, 7.071067871846544506 ) ) ;
#23957=CARTESIAN_POINT ( 'NONE',  ( -11.35316468749999785, 248.6979166700806445, -3.042071309553164848 ) ) ;
#23987=CARTESIAN_POINT ( 'NONE',  ( -5.676582343750000703, 243.3854166700806445, -9.832129032723418760 ) ) ;
#23994=LINE ( 'NONE', #30035, #28740 ) ;
#24006=DIRECTION ( 'NONE',  ( -0.000000000000000000, -1.000000000000000000, -0.000000000000000000 ) ) ;
#24012=CARTESIAN_POINT ( 'NONE',  ( -6.123233995736766282E-16, 246.8750000068280031, -10.00000000000000000 ) ) ;
#24040=CARTESIAN_POINT ( 'NONE',  ( -8.311093377946836114, 238.2812500034139873, -8.311093377946836114 ) ) ;
#24043=CARTESIAN_POINT ( 'NONE',  ( 9.832129032723420536, 236.3020833367473301, 5.676582343749996262 ) ) ;
#24096=DIRECTION ( 'NONE',  ( -0.000000000000000000, -1.000000000000000000, -0.000000000000000000 ) ) ;
#24097=CARTESIAN_POINT ( 'NONE',  ( 4.999999999999997335, 251.4583333401613174, -8.660254037844387298 ) ) ;
#24147=CARTESIAN_POINT ( 'NONE',  ( -3.042071309553166181, 233.1770833367473017, -11.35316468749999608 ) ) ;
#24186=CARTESIAN_POINT ( 'NONE',  ( -5.676582343750000703, 253.0729166700807014, -9.832129032723418760 ) ) ;
#24234=CARTESIAN_POINT ( 'NONE',  ( -4.999999999999992895, 225.8333333333333428, 8.660254037844390851 ) ) ;
#24323=CARTESIAN_POINT ( 'NONE',  ( 3.042071309553173286, 230.3645833367472733, 11.35316468749999608 ) ) ;
#24328=CARTESIAN_POINT ( 'NONE',  ( -2.679491924311228512, 263.9583333333333144, -9.999999999999998224 ) ) ;
#24359=CARTESIAN_POINT ( 'NONE',  ( -8.311093377946836114, 248.5937500034139589, -8.311093377946836114 ) ) ;
#24415=CARTESIAN_POINT ( 'NONE',  ( -9.832129032723415207, 229.3229166700806729, 5.676582343750005144 ) ) ;
#24418=CARTESIAN_POINT ( 'NONE',  ( 11.35316468749999963, 236.5104166700806161, 3.042071309553159519 ) ) ;
#24475=CARTESIAN_POINT ( 'NONE',  ( -7.320508075688771932, 247.5000000068279746, -7.320508075688771932 ) ) ;
#24485=VECTOR ( 'NONE', #64735, 1000.000000000000227 ) ;
#24519=CARTESIAN_POINT ( 'NONE',  ( -10.00000000000000000, 249.7916666666666572, -2.679491924311226292 ) ) ;
#24521=CARTESIAN_POINT ( 'NONE',  ( -5.676582343749992710, 235.0520833367473301, 9.832129032723422313 ) ) ;
#24556=CARTESIAN_POINT ( 'NONE',  ( 11.35316468749999608, 251.6145833367473585, -3.042071309553167069 ) ) ;
#24602=CARTESIAN_POINT ( 'NONE',  ( -9.999999999999998224, 225.2083333333333144, 2.679491924311235618 ) ) ;
#24629=VERTEX_POINT ( 'NONE', #17770 ) ;
#24683=CARTESIAN_POINT ( 'NONE',  ( 3.042071309553173286, 235.3645833367473017, 11.35316468749999608 ) ) ;
#24717=CARTESIAN_POINT ( 'NONE',  ( 4.999999999999997335, 221.4583333401612890, -8.660254037844387298 ) ) ;
#24719=CARTESIAN_POINT ( 'NONE',  ( -3.042071309553159075, 230.2604166700806445, 11.35316468749999963 ) ) ;
#24759=DIRECTION ( 'NONE',  ( -0.000000000000000000, -1.000000000000000000, -0.000000000000000000 ) ) ;
#24765=ORIENTED_EDGE ( 'NONE', *, *, #22365, .T. ) ;
#24771=CARTESIAN_POINT ( 'NONE',  ( 9.832129032723416984, 226.8229166700806729, -5.676582343750003368 ) ) ;
#24774=CARTESIAN_POINT ( 'NONE',  ( -6.951808397369817780E-16, 227.9687500034139873, -11.35316468749999963 ) ) ;
#24832=CARTESIAN_POINT ( 'NONE',  ( -4.999999999999992895, 238.9583333401613174, 8.660254037844390851 ) ) ;
#24873=CARTESIAN_POINT ( 'NONE',  ( -8.660254037844385522, 243.5416666734946318, 5.000000000000004441 ) ) ;
#24877=CARTESIAN_POINT ( 'NONE',  ( -11.35316468749999963, 234.2187500034139873, 0.000000000000000000 ) ) ;
#24888=DIRECTION ( 'NONE',  ( -0.000000000000000000, -1.000000000000000000, -0.000000000000000000 ) ) ;
#24915=CARTESIAN_POINT ( 'NONE',  ( 9.832129032723420536, 230.9895833367473301, 5.676582343749996262 ) ) ;
#24966=CARTESIAN_POINT ( 'NONE',  ( -7.320508075688770155, 220.6250000000000284, 7.320508075688774596 ) ) ;
#25019=( BOUNDED_CURVE ( )  B_SPLINE_CURVE ( 2, ( #53566, #1882, #64143, #65239, #31284, #13543, #23780, #46784, #35483, #2624, #60324, #37327, #2995 ),
 .UNSPECIFIED., .F., .F. ) 
 B_SPLINE_CURVE_WITH_KNOTS ( ( 3, 2, 2, 2, 2, 2, 3 ),
 ( 0.6388888888888887285, 0.6481481481481480289, 0.6574074074074073293, 0.6666666666666665186, 0.6759259259259259300, 0.6851851851851852304, 0.6944444444444444198 ),
 .UNSPECIFIED. ) 
 CURVE ( )  GEOMETRIC_REPRESENTATION_ITEM ( )  RATIONAL_B_SPLINE_CURVE ( ( 1.000000000000000444, 0.9659258262890678681, 1.000000000000000000, 0.9659258262890683122, 1.000000000000000000, 0.9659258262890683122, 1.000000000000000000, 0.9659258262890683122, 1.000000000000000000, 0.9659258262890683122, 1.000000000000000000, 0.9659258262890683122, 1.000000000000000000 ) ) 
 REPRESENTATION_ITEM ( '' )  );
#25033=ORIENTED_EDGE ( 'NONE', *, *, #29161, .T. ) ;
#25047=CARTESIAN_POINT ( 'NONE',  ( -11.35316468749999608, 229.1145833367473301, 3.042071309553173730 ) ) ;
#25072=EDGE_CURVE ( 'NONE', #55545, #26674, #61947, .T. ) ;
#25084=CARTESIAN_POINT ( 'NONE',  ( 2.085542519210945334E-15, 235.4687500034139873, 11.35316468749999963 ) ) ;
#25109=CARTESIAN_POINT ( 'NONE',  ( 2.679491924311139250, 246.6666666734946887, -10.00000000000004796 ) ) ;
#25123=AXIS2_PLACEMENT_3D ( 'NONE', #7463, #53486, #6363 ) ;
#25138=CARTESIAN_POINT ( 'NONE',  ( -11.35316468749999608, 229.1145833367473585, 3.042071309553173730 ) ) ;
#25142=CARTESIAN_POINT ( 'NONE',  ( -11.35316468749999608, 229.4270833367473585, 3.042071309553173730 ) ) ;
#25200=CARTESIAN_POINT ( 'NONE',  ( 2.679491924311071749, 263.5416666666666856, -10.00000000000008704 ) ) ;
#25203=CARTESIAN_POINT ( 'NONE',  ( -8.660254037844387298, 237.7083333401613174, -4.999999999999999112 ) ) ;
#25205=ORIENTED_EDGE ( 'NONE', *, *, #62048, .F. ) ;
#25220=AXIS2_PLACEMENT_3D ( 'NONE', #10460, #38772, #49708 ) ;
#25250=CARTESIAN_POINT ( 'NONE',  ( -11.35316468749999608, 234.4270833367473017, 3.042071309553173730 ) ) ;
#25287=CARTESIAN_POINT ( 'NONE',  ( 9.832129032723420536, 240.9895833367473301, 5.676582343749996262 ) ) ;
#25334=CARTESIAN_POINT ( 'NONE',  ( -6.123233995736766282E-16, 236.8750000068279746, -10.00000000000000000 ) ) ;
#25336=CARTESIAN_POINT ( 'NONE',  ( 4.999999999999997335, 223.3333333333333144, -8.660254037844387298 ) ) ;
#25394=CARTESIAN_POINT ( 'NONE',  ( 0.3346513822855006759, 219.9760043661977420, 11.00000000000000000 ) ) ;
#25422=CARTESIAN_POINT ( 'NONE',  ( 11.35316468749999608, 226.6145833367473301, -3.042071309553167069 ) ) ;
#25430=CARTESIAN_POINT ( 'NONE',  ( 2.679491924311168560, 241.6666666734946602, -10.00000000000003375 ) ) ;
#25457=CARTESIAN_POINT ( 'NONE',  ( 11.35316468749999963, 231.5104166700806445, 3.042071309553159519 ) ) ;
#25482=VECTOR ( 'NONE', #30847, 1000.000000000000000 ) ;
#25510=CARTESIAN_POINT ( 'NONE',  ( 11.35316468749999963, 221.4062500034139873, -1.390361679473963556E-15 ) ) ;
#25513=CARTESIAN_POINT ( 'NONE',  ( 11.35316468749999963, 231.5104166700806445, 3.042071309553159519 ) ) ;
#25572=CARTESIAN_POINT ( 'NONE',  ( 2.679491924311235174, 234.5833333401613174, 9.999999999999998224 ) ) ;
#25585=EDGE_CURVE ( 'NONE', #73780, #15595, #8399, .T. ) ;
#25595=CARTESIAN_POINT ( 'NONE',  ( -11.35316468749999608, 259.1145833367473301, 3.042071309553173730 ) ) ;
#25622=CARTESIAN_POINT ( 'NONE',  ( 11.35316468749999963, 221.5104166700805877, 3.042071309553159519 ) ) ;
#25629=ORIENTED_EDGE ( 'NONE', *, *, #65332, .T. ) ;
#25636=CARTESIAN_POINT ( 'NONE',  ( -11.35316468749999963, 264.0625000034140157, 0.000000000000000000 ) ) ;
#25658=CARTESIAN_POINT ( 'NONE',  ( -9.832129032723418760, 233.4895833367473301, -5.676582343749998927 ) ) ;
#25671=( BOUNDED_CURVE ( )  B_SPLINE_CURVE ( 2, ( #2528, #71917, #71173, #44381, #55715, #28138, #32706 ),
 .UNSPECIFIED., .F., .F. ) 
 B_SPLINE_CURVE_WITH_KNOTS ( ( 3, 2, 2, 3 ),
 ( 0.000000000000000000, 0.009259259259259305583, 0.01851851851851849667, 0.02777777777777780052 ),
 .UNSPECIFIED. ) 
 CURVE ( )  GEOMETRIC_REPRESENTATION_ITEM ( )  RATIONAL_B_SPLINE_CURVE ( ( 1.000000000000000000, 0.9659258262890684232, 1.000000000000000000, 0.9659258262890684232, 1.000000000000000000, 0.9659258262890684232, 1.000000000000000000 ) ) 
 REPRESENTATION_ITEM ( '' )  );
#25704=CARTESIAN_POINT ( 'NONE',  ( -5.676582343750000703, 258.3854166700806445, -9.832129032723418760 ) ) ;
#25748=LINE ( 'NONE', #71776, #18198 ) ;
#25752=ORIENTED_EDGE ( 'NONE', *, *, #9486, .T. ) ;
#25790=ADVANCED_FACE ( 'NONE', ( #74113 ), #51101, .F. ) ;
#25791=CARTESIAN_POINT ( 'NONE',  ( -5.676582343750000703, 233.0729166700806729, -9.832129032723418760 ) ) ;
#25795=CARTESIAN_POINT ( 'NONE',  ( -6.123233995736766282E-16, 258.7500000000000568, -10.00000000000000000 ) ) ;
#25824=CARTESIAN_POINT ( 'NONE',  ( 5.676582343749997150, 237.5520833367473301, -9.832129032723418760 ) ) ;
#25832=CARTESIAN_POINT ( 'NONE',  ( 4.508099642231537807, 219.9999999999999716, 9.452567682505941704 ) ) ;
#25878=CARTESIAN_POINT ( 'NONE',  ( -5.676582343749992710, 230.0520833367473017, 9.832129032723422313 ) ) ;
#25924=EDGE_CURVE ( 'NONE', #56463, #16846, #69573, .T. ) ;
#25942=CARTESIAN_POINT ( 'NONE',  ( 4.999999999999997335, 236.4583333401613174, -8.660254037844387298 ) ) ;
#25960=CARTESIAN_POINT ( 'NONE',  ( -9.832129032723418760, 263.4895833367473301, -5.676582343749998927 ) ) ;
#25962=VERTEX_POINT ( 'NONE', #70314 ) ;
#25963=CARTESIAN_POINT ( 'NONE',  ( 8.311093377946834337, 262.3437500034140157, -8.311093377946836114 ) ) ;
#25995=CARTESIAN_POINT ( 'NONE',  ( 0.000000000000000000, 0.000000000000000000, -10.00000000000000000 ) ) ;
#26024=CARTESIAN_POINT ( 'NONE',  ( 5.676582343749997150, 232.2395833367473301, -9.832129032723418760 ) ) ;
#26076=CARTESIAN_POINT ( 'NONE',  ( 8.311093377946834337, 257.3437500034140157, -8.311093377946836114 ) ) ;
#26167=PLANE ( 'NONE',  #5687 ) ;
#26169=CARTESIAN_POINT ( 'NONE',  ( 8.660254037844389075, 247.0833333333333428, 4.999999999999997335 ) ) ;
#26181=CIRCLE ( 'NONE', #57518, 11.00000000000000000 ) ;
#26199=CARTESIAN_POINT ( 'NONE',  ( -6.951808397369817780E-16, 227.9687500034139873, -11.35316468749999963 ) ) ;
#26220=CARTESIAN_POINT ( 'NONE',  ( 5.000000000000004441, 244.7916666734946318, 8.660254037844385522 ) ) ;
#26221=CARTESIAN_POINT ( 'NONE',  ( 4.999999999999997335, 238.3333333333333428, -8.660254037844387298 ) ) ;
#26252=CARTESIAN_POINT ( 'NONE',  ( -3.042071309553166625, 222.8645833367473301, -11.35316468749999608 ) ) ;
#26255=CARTESIAN_POINT ( 'NONE',  ( 8.311093377946834337, 232.3437500034140157, -8.311093377946836114 ) ) ;
#26281=LINE ( 'NONE', #31963, #8617 ) ;
#26316=CARTESIAN_POINT ( 'NONE',  ( -10.00000000000000000, 232.9166666734946602, -2.679491924311226292 ) ) ;
#26323=VERTEX_POINT ( 'NONE', #69394 ) ;
#26337=CARTESIAN_POINT ( 'NONE',  ( -6.123233995736766282E-16, 256.8750000068279746, -10.00000000000000000 ) ) ;
#26338=CARTESIAN_POINT ( 'NONE',  ( 8.311093377946839666, 260.7812500034140157, 8.311093377946830785 ) ) ;
#26342=CARTESIAN_POINT ( 'NONE',  ( 8.311093377946839666, 261.0937500034140157, 8.311093377946829008 ) ) ;
#26392=DIRECTION ( 'NONE',  ( -0.000000000000000000, -1.000000000000000000, -0.000000000000000000 ) ) ;
#26399=CARTESIAN_POINT ( 'NONE',  ( -11.35316468749999608, 229.1145833367473301, 3.042071309553173730 ) ) ;
#26453=CARTESIAN_POINT ( 'NONE',  ( 2.085542519210945334E-15, 255.4687500034140157, 11.35316468749999963 ) ) ;
#26482=ORIENTED_EDGE ( 'NONE', *, *, #52389, .F. ) ;
#26539=CARTESIAN_POINT ( 'NONE',  ( -5.676582343749992710, 224.7395833367473301, 9.832129032723422313 ) ) ;
#26544=CARTESIAN_POINT ( 'NONE',  ( 5.000000000000004441, 251.6666666666667140, 8.660254037844385522 ) ) ;
#26612=EDGE_CURVE ( 'NONE', #8879, #44513, #5557, .T. ) ;
#26635=CARTESIAN_POINT ( 'NONE',  ( 5.676582343749997150, 257.2395833367473301, -9.832129032723418760 ) ) ;
#26652=ORIENTED_EDGE ( 'NONE', *, *, #7694, .T. ) ;
#26670=CARTESIAN_POINT ( 'NONE',  ( -7.320508075688771932, 222.5000000068279746, -7.320508075688771932 ) ) ;
#26671=CARTESIAN_POINT ( 'NONE',  ( 9.832129032723416984, 262.1354166700806445, -5.676582343750003368 ) ) ;
#26674=VERTEX_POINT ( 'NONE', #73105 ) ;
#26685=CYLINDRICAL_SURFACE ( 'NONE', #25220, 10.00000000000000000 ) ;
#26701=CARTESIAN_POINT ( 'NONE',  ( -6.123233995736766282E-16, 221.8750000068279746, -10.00000000000000000 ) ) ;
#26722=CARTESIAN_POINT ( 'NONE',  ( -8.660254037844385522, 258.5416666734946602, 5.000000000000004441 ) ) ;
#26723=CARTESIAN_POINT ( 'NONE',  ( 9.832129032723420536, 255.9895833367473301, 5.676582343749996262 ) ) ;
#26727=CARTESIAN_POINT ( 'NONE',  ( 8.311093377946839666, 251.0937500034139873, 8.311093377946829008 ) ) ;
#26790=CARTESIAN_POINT ( 'NONE',  ( 11.35316468749999963, 226.4062500034139873, -1.390361679473963556E-15 ) ) ;
#26841=CARTESIAN_POINT ( 'NONE',  ( -8.311093377946834337, 259.8437500034140157, 8.311093377946837890 ) ) ;
#26892=CARTESIAN_POINT ( 'NONE',  ( -10.00000000000000000, 247.9166666734946318, -2.679491924311226292 ) ) ;
#26910=DIRECTION ( 'NONE',  ( -0.000000000000000000, -1.000000000000000000, -0.000000000000000000 ) ) ;
#26923=CARTESIAN_POINT ( 'NONE',  ( -8.311093377946836114, 223.2812500034140157, -8.311093377946836114 ) ) ;
#26927=CARTESIAN_POINT ( 'NONE',  ( 5.000000000000004441, 256.6666666666666288, 8.660254037844385522 ) ) ;
#26933=CARTESIAN_POINT ( 'NONE',  ( 2.679491924311071749, 261.6666666734946602, -10.00000000000008704 ) ) ;
#26934=PLANE ( 'NONE',  #36875 ) ;
#26936=ORIENTED_EDGE ( 'NONE', *, *, #42716, .T. ) ;
#26966=FACE_OUTER_BOUND ( 'NONE', #7402, .T. ) ;
#26970=CARTESIAN_POINT ( 'NONE',  ( 1.836970198721029589E-15, 256.2500000000000568, 10.00000000000000000 ) ) ;
#26981=CARTESIAN_POINT ( 'NONE',  ( 10.00000000000000000, 237.5000000000000284, -1.224646799147353256E-15 ) ) ;
#27015=CARTESIAN_POINT ( 'NONE',  ( -11.35316468749999608, 259.1145833367473301, 3.042071309553173730 ) ) ;
#27019=CARTESIAN_POINT ( 'NONE',  ( 0.000000000000000000, 0.000000000000000000, 0.000000000000000000 ) ) ;
#27049=CARTESIAN_POINT ( 'NONE',  ( -10.00000000000000000, 223.1250000068279746, 0.000000000000000000 ) ) ;
#27051=CARTESIAN_POINT ( 'NONE',  ( 3.042071309553173286, 260.6770833367473301, 11.35316468749999608 ) ) ;
#27077=CARTESIAN_POINT ( 'NONE',  ( 2.679491924311225848, 221.6666666734946602, -10.00000000000000000 ) ) ;
#27098=CARTESIAN_POINT ( 'NONE',  ( -11.35316468749999785, 253.6979166700806729, -3.042071309553164848 ) ) ;
#27102=CARTESIAN_POINT ( 'NONE',  ( 8.311093377946834337, 257.3437500034140157, -8.311093377946836114 ) ) ;
#27135=ORIENTED_EDGE ( 'NONE', *, *, #58612, .F. ) ;
#27159=CARTESIAN_POINT ( 'NONE',  ( 4.999999999999997335, 261.4583333401613459, -8.660254037844387298 ) ) ;
#27182=CARTESIAN_POINT ( 'NONE',  ( 10.00000000000000178, 222.2916666666666572, 2.679491924311222739 ) ) ;
#27208=CARTESIAN_POINT ( 'NONE',  ( -11.35316468749999963, 254.2187500034139873, 0.000000000000000000 ) ) ;
#27242=CARTESIAN_POINT ( 'NONE',  ( -5.676582343749992710, 254.7395833367473301, 9.832129032723422313 ) ) ;
#27252=CARTESIAN_POINT ( 'NONE',  ( -6.123233995736766282E-16, 231.8750000068279746, -10.00000000000000000 ) ) ;
#27291=CARTESIAN_POINT ( 'NONE',  ( -6.951808397369817780E-16, 222.6562500034139873, -11.35316468749999963 ) ) ;
#27296=CARTESIAN_POINT ( 'NONE',  ( 1.836970198721029589E-15, 256.2500000000000568, 10.00000000000000000 ) ) ;
#27344=VERTEX_POINT ( 'NONE', #18095 ) ;
#27379=CARTESIAN_POINT ( 'NONE',  ( 11.35316468749999608, 256.6145833367473301, -3.042071309553167069 ) ) ;
#27380=CLOSED_SHELL ( 'NONE', ( #23878, #30621, #42476, #42452, #22247, #49183, #55320, #14553, #37623, #69191, #15165, #60003, #42103, #29055, #29098, #4459, #28483, #28388, #11030, #51900, #17745, #25790, #70244, #21216, #18089, #8762, #33748, #71550, #31883, #62913, #35206, #22832, #56522, #47121, #31909 ) ) ;
#27415=CARTESIAN_POINT ( 'NONE',  ( 2.085542519210945334E-15, 260.4687500034140157, 11.35316468749999963 ) ) ;
#27427=FACE_OUTER_BOUND ( 'NONE', #20169, .T. ) ;
#27439=CARTESIAN_POINT ( 'NONE',  ( -8.660254037844385522, 223.5416666734946602, 5.000000000000004441 ) ) ;
#27464=CARTESIAN_POINT ( 'NONE',  ( 8.311093377946834337, 247.0312500034139589, -8.311093377946836114 ) ) ;
#27469=CARTESIAN_POINT ( 'NONE',  ( 2.085542519210945334E-15, 255.4687500034140157, 11.35316468749999963 ) ) ;
#27511=CARTESIAN_POINT ( 'NONE',  ( -7.320508075688771932, 244.3750000000000000, -7.320508075688771932 ) ) ;
#27532=CARTESIAN_POINT ( 'NONE',  ( -2.679491924311222295, 259.1666666734946602, 10.00000000000000178 ) ) ;
#27584=CARTESIAN_POINT ( 'NONE',  ( -5.676582343750000703, 248.3854166700806445, -9.832129032723418760 ) ) ;
#27598=CARTESIAN_POINT ( 'NONE',  ( 7.320508075688776373, 226.8750000000000000, 7.320508075688767491 ) ) ;
#27620=CARTESIAN_POINT ( 'NONE',  ( 9.832129032723416984, 261.8229166700807014, -5.676582343750003368 ) ) ;
#27673=CARTESIAN_POINT ( 'NONE',  ( -6.123233995736766282E-16, 253.7500000000000284, -10.00000000000000000 ) ) ;
#27701=CARTESIAN_POINT ( 'NONE',  ( -5.676582343749992710, 220.0520833367473301, 9.832129032723422313 ) ) ;
#27713=VECTOR ( 'NONE', #50662, 1000.000000000000000 ) ;
#27724=CARTESIAN_POINT ( 'NONE',  ( 9.999999999999998224, 237.7083333333333144, -2.679491924311229401 ) ) ;
#27755=CARTESIAN_POINT ( 'NONE',  ( -11.35316468749999608, 254.1145833367473585, 3.042071309553173730 ) ) ;
#27791=CARTESIAN_POINT ( 'NONE',  ( 3.042071309553163516, 252.7604166700806445, -11.35316468749999785 ) ) ;
#27823=CARTESIAN_POINT ( 'NONE',  ( -4.999999999999992895, 223.9583333401612890, 8.660254037844390851 ) ) ;
#27832=VECTOR ( 'NONE', #30485, 1000.000000000000000 ) ;
#27838=ORIENTED_EDGE ( 'NONE', *, *, #2670, .F. ) ;
#27847=CARTESIAN_POINT ( 'NONE',  ( 9.832129032723416984, 241.8229166700806445, -5.676582343750003368 ) ) ;
#27851=CARTESIAN_POINT ( 'NONE',  ( 3.042071309553163960, 247.7604166700806161, -11.35316468749999785 ) ) ;
#27911=CARTESIAN_POINT ( 'NONE',  ( -11.35316468749999608, 224.1145833367473301, 3.042071309553173730 ) ) ;
#27951=CARTESIAN_POINT ( 'NONE',  ( -6.123233995736766282E-16, 253.7500000000000284, -10.00000000000000000 ) ) ;
#27966=CARTESIAN_POINT ( 'NONE',  ( -11.35316468749999608, 239.4270833367473301, 3.042071309553173730 ) ) ;
#27970=EDGE_CURVE ( 'NONE', #25962, #7137, #14352, .T. ) ;
#28048=CARTESIAN_POINT ( 'NONE',  ( 8.660254037844389075, 232.0833333333333428, 4.999999999999997335 ) ) ;
#28073=ORIENTED_EDGE ( 'NONE', *, *, #52180, .F. ) ;
#28085=ORIENTED_EDGE ( 'NONE', *, *, #57635, .T. ) ;
#28107=DIRECTION ( 'NONE',  ( -0.000000000000000000, -1.000000000000000000, -0.000000000000000000 ) ) ;
#28130=CARTESIAN_POINT ( 'NONE',  ( 11.35316468749999608, 261.6145833367473301, -3.042071309553167069 ) ) ;
#28138=CARTESIAN_POINT ( 'NONE',  ( -2.947441116742341105, 219.7440169426842544, 11.00000000000000355 ) ) ;
#28166=CARTESIAN_POINT ( 'NONE',  ( -11.35316468749999963, 259.2187500034140157, 0.000000000000000000 ) ) ;
#28194=CARTESIAN_POINT ( 'NONE',  ( 8.660254037844389075, 230.2083333401612890, 4.999999999999997335 ) ) ;
#28220=CARTESIAN_POINT ( 'NONE',  ( 5.676582343750005144, 250.5729166700807014, 9.832129032723416984 ) ) ;
#28225=CARTESIAN_POINT ( 'NONE',  ( 9.832129032723416984, 247.1354166700806445, -5.676582343750003368 ) ) ;
#28229=ORIENTED_EDGE ( 'NONE', *, *, #41835, .T. ) ;
#28250=CARTESIAN_POINT ( 'NONE',  ( -6.123233995736766282E-16, 233.7500000000000000, -10.00000000000000000 ) ) ;
#28273=STYLED_ITEM('',(#74692),#66799);
#28287=CARTESIAN_POINT ( 'NONE',  ( -8.660254037844387298, 262.7083333401612890, -4.999999999999999112 ) ) ;
#28335=CARTESIAN_POINT ( 'NONE',  ( -5.676582343749992710, 240.0520833367473301, 9.832129032723422313 ) ) ;
#28348=CARTESIAN_POINT ( 'NONE',  ( -6.123233995736766282E-16, 228.7500000000000000, -10.00000000000000000 ) ) ;
#28385=DIRECTION ( 'NONE',  ( -0.000000000000000000, -1.000000000000000000, -0.000000000000000000 ) ) ;
#28388=ADVANCED_FACE ( 'NONE', ( #27427 ), #26685, .F. ) ;
#28421=CARTESIAN_POINT ( 'NONE',  ( 10.00000000000000178, 242.2916666666666288, 2.679491924311222739 ) ) ;
#28483=ADVANCED_FACE ( 'NONE', ( #21025 ), #8969, .F. ) ;
#28504=CARTESIAN_POINT ( 'NONE',  ( 9.832129032723420536, 245.9895833367473301, 5.676582343749996262 ) ) ;
#28512=( NAMED_UNIT ( * ) PLANE_ANGLE_UNIT ( ) SI_UNIT ( $, .RADIAN. ) );
#28538=CARTESIAN_POINT ( 'NONE',  ( -5.676582343750000703, 238.3854166700806445, -9.832129032723418760 ) ) ;
#28577=ORIENTED_EDGE ( 'NONE', *, *, #70513, .T. ) ;
#28592=CARTESIAN_POINT ( 'NONE',  ( -3.042071309553166625, 242.8645833367473301, -11.35316468749999608 ) ) ;
#28597=CARTESIAN_POINT ( 'NONE',  ( -9.832129032723418760, 233.8020833367473301, -5.676582343749998927 ) ) ;
#28620=CARTESIAN_POINT ( 'NONE',  ( -2.679491924311228512, 233.9583333333333428, -9.999999999999998224 ) ) ;
#28637=DIRECTION ( 'NONE',  ( -0.000000000000000000, -1.000000000000000000, -0.000000000000000000 ) ) ;
#28653=CARTESIAN_POINT ( 'NONE',  ( 8.660254037844385522, 256.0416666734946602, -5.000000000000003553 ) ) ;
#28701=CARTESIAN_POINT ( 'NONE',  ( 8.311093377946839666, 246.0937500034139873, 8.311093377946829008 ) ) ;
#28736=CARTESIAN_POINT ( 'NONE',  ( -3.042071309553166181, 262.8645833367473301, -11.35316468749999608 ) ) ;
#28740=VECTOR ( 'NONE', #35701, 1000.000000000000000 ) ;
#28753=DIRECTION ( 'NONE',  ( -0.000000000000000000, -1.000000000000000000, -0.000000000000000000 ) ) ;
#28773=DIRECTION ( 'NONE',  ( -0.8660254037844389297, -0.4999999999999994449, 0.000000000000000000 ) ) ;
#28783=CARTESIAN_POINT ( 'NONE',  ( 8.660254037844385522, 252.9166666666666856, -5.000000000000003553 ) ) ;
#28789=CARTESIAN_POINT ( 'NONE',  ( 8.660254037844385522, 242.9166666666666572, -5.000000000000003553 ) ) ;
#28874=CARTESIAN_POINT ( 'NONE',  ( 3.042071309553163960, 242.4479166700806729, -11.35316468749999785 ) ) ;
#28878=CARTESIAN_POINT ( 'NONE',  ( -9.036584110083673238, 219.9999999999999716, 5.919388431620439484 ) ) ;
#28893=ORIENTED_EDGE ( 'NONE', *, *, #60070, .T. ) ;
#28906=CARTESIAN_POINT ( 'NONE',  ( -2.679491924311171225, 223.9583333333333144, -10.00000000000003197 ) ) ;
#28914=CARTESIAN_POINT ( 'NONE',  ( -8.311093377946834337, 244.8437500034139873, 8.311093377946837890 ) ) ;
#28966=CARTESIAN_POINT ( 'NONE',  ( 9.832129032723420536, 245.9895833367473301, 5.676582343749996262 ) ) ;
#28970=CARTESIAN_POINT ( 'NONE',  ( -11.35316468749999608, 244.4270833367473017, 3.042071309553173730 ) ) ;
#29027=CARTESIAN_POINT ( 'NONE',  ( 0.000000000000000000, 0.000000000000000000, 0.000000000000000000 ) ) ;
#29028=CARTESIAN_POINT ( 'NONE',  ( 7.320508075688776373, 250.0000000068279746, 7.320508075688767491 ) ) ;
#29055=ADVANCED_FACE ( 'NONE', ( #73370 ), #38680, .F. ) ;
#29082=CARTESIAN_POINT ( 'NONE',  ( 2.085542519210945334E-15, 245.4687500034140157, 11.35316468749999963 ) ) ;
#29098=ADVANCED_FACE ( 'NONE', ( #26966 ), #49613, .F. ) ;
#29119=CARTESIAN_POINT ( 'NONE',  ( -11.35316468749999963, 253.9062500034139873, 0.000000000000000000 ) ) ;
#29144=CARTESIAN_POINT ( 'NONE',  ( -8.660254037844387298, 262.7083333401612890, -4.999999999999999112 ) ) ;
#29161=EDGE_CURVE ( 'NONE', #5036, #15595, #68139, .T. ) ;
#29165=ORIENTED_EDGE ( 'NONE', *, *, #42912, .T. ) ;
#29172=CARTESIAN_POINT ( 'NONE',  ( 7.320508075688776373, 241.8749999999999716, 7.320508075688767491 ) ) ;
#29180=CARTESIAN_POINT ( 'NONE',  ( -2.679491924311228512, 227.0833333401612890, -9.999999999999998224 ) ) ;
#29199=VERTEX_POINT ( 'NONE', #34574 ) ;
#29233=DIRECTION ( 'NONE',  ( 0.000000000000000000, 0.000000000000000000, -1.000000000000000000 ) ) ;
#29257=CARTESIAN_POINT ( 'NONE',  ( 2.085542519210945334E-15, 245.1562500034140157, 11.35316468749999963 ) ) ;
#29294=CARTESIAN_POINT ( 'NONE',  ( -11.35316468749999608, 249.4270833367473017, 3.042071309553173730 ) ) ;
#29332=VECTOR ( 'NONE', #28753, 1000.000000000000000 ) ;
#29340=EDGE_LOOP ( 'NONE', ( #65378, #63294, #1583, #65423 ) ) ;
#29349=CARTESIAN_POINT ( 'NONE',  ( 2.085542519210945334E-15, 230.1562500034139873, 11.35316468749999963 ) ) ;
#29354=CARTESIAN_POINT ( 'NONE',  ( -5.676582343749992710, 245.0520833367473301, 9.832129032723422313 ) ) ;
#29357=( BOUNDED_CURVE ( )  B_SPLINE_CURVE ( 2, ( #36700, #48372, #71376, #42713, #37066, #60066, #8388, #31401, #71751, #56668, #32542, #61573, #9893 ),
 .UNSPECIFIED., .F., .F. ) 
 B_SPLINE_CURVE_WITH_KNOTS ( ( 3, 2, 2, 2, 2, 2, 3 ),
 ( 0.7500000000000000000, 0.7592592592592593004, 0.7685185185185184897, 0.7777777777777777901, 0.7870370370370370905, 0.7962962962962962798, 0.8055555555555555802 ),
 .UNSPECIFIED. ) 
 CURVE ( )  GEOMETRIC_REPRESENTATION_ITEM ( )  RATIONAL_B_SPLINE_CURVE ( ( 1.000000000000000000, 0.9659258262890683122, 1.000000000000000000, 0.9659258262890683122, 1.000000000000000000, 0.9659258262890683122, 1.000000000000000000, 0.9659258262890683122, 1.000000000000000000, 0.9659258262890683122, 1.000000000000000000, 0.9659258262890683122, 1.000000000000000000 ) ) 
 REPRESENTATION_ITEM ( '' )  );
#29409=CARTESIAN_POINT ( 'NONE',  ( 7.320508075688776373, 255.0000000068279746, 7.320508075688767491 ) ) ;
#29456=CARTESIAN_POINT ( 'NONE',  ( 8.311093377946834337, 222.3437500034139589, -8.311093377946836114 ) ) ;
#29463=CARTESIAN_POINT ( 'NONE',  ( -8.660254037844387298, 239.5833333333333428, -4.999999999999999112 ) ) ;
#29492=CARTESIAN_POINT ( 'NONE',  ( -11.35316468749999785, 253.6979166700807014, -3.042071309553164848 ) ) ;
#29523=VERTEX_POINT ( 'NONE', #36777 ) ;
#29525=CARTESIAN_POINT ( 'NONE',  ( -7.320508075688770155, 220.6250000000000284, 7.320508075688774596 ) ) ;
#29539=CARTESIAN_POINT ( 'NONE',  ( -7.320508075688771932, 239.3749999999999716, -7.320508075688771932 ) ) ;
#29587=ORIENTED_EDGE ( 'NONE', *, *, #63145, .F. ) ;
#29625=CARTESIAN_POINT ( 'NONE',  ( -8.311093377946836114, 248.2812500034139873, -8.311093377946836114 ) ) ;
#29656=CARTESIAN_POINT ( 'NONE',  ( -5.676582343749992710, 240.0520833367473301, 9.832129032723422313 ) ) ;
#29695=B_SPLINE_CURVE_WITH_KNOTS ( 'NONE', 3,
 ( #10786, #62830, #51146, #45854, #28878, #45479, #51898, #16058, #69247, #239, #23220, #73784, #68497, #40201, #39826, #68871 ),
 .UNSPECIFIED., .F., .F.,
 ( 4, 2, 2, 2, 2, 2, 2, 4 ),
 ( 0.002858817767436716648, 0.003816970720266378483, 0.004775123673096039884, 0.005733276625925702585, 0.006691429578755363553, 0.008607735484414683752, 0.009565888437244344719, 0.01052404139007400395 ),
 .UNSPECIFIED. ) ;
#29706=EDGE_CURVE ( 'NONE', #29523, #5036, #19623, .T. ) ;
#29714=CARTESIAN_POINT ( 'NONE',  ( 3.042071309553173286, 235.3645833367473017, 11.35316468749999608 ) ) ;
#29717=CARTESIAN_POINT ( 'NONE',  ( -11.35316468749999785, 239.0104166700806161, -3.042071309553164848 ) ) ;
#29727=DIRECTION ( 'NONE',  ( -0.000000000000000000, -1.000000000000000000, -0.000000000000000000 ) ) ;
#29770=CARTESIAN_POINT ( 'NONE',  ( 9.999999999999998224, 250.8333333401613459, -2.679491924311229401 ) ) ;
#29785=EDGE_CURVE ( 'NONE', #5866, #8328, #64887, .T. ) ;
#29807=AXIS2_PLACEMENT_3D ( 'NONE', #47999, #58250, #30662 ) ;
#29823=CARTESIAN_POINT ( 'NONE',  ( -5.676582343750000703, 233.3854166700806729, -9.832129032723418760 ) ) ;
#29861=CARTESIAN_POINT ( 'NONE',  ( -11.35316468749999963, 248.9062500034139873, 0.000000000000000000 ) ) ;
#29881=ORIENTED_EDGE ( 'NONE', *, *, #52927, .F. ) ;
#29908=CARTESIAN_POINT ( 'NONE',  ( 7.320508075688776373, 226.8749999999999716, 7.320508075688767491 ) ) ;
#29916=CARTESIAN_POINT ( 'NONE',  ( -7.320508075688770155, 228.7500000068279746, 7.320508075688774596 ) ) ;
#29935=VERTEX_POINT ( 'NONE', #42237 ) ;
#29994=CARTESIAN_POINT ( 'NONE',  ( 8.311093377946839666, 250.7812500034139873, 8.311093377946829008 ) ) ;
#29999=CARTESIAN_POINT ( 'NONE',  ( 7.320508075688771044, 258.1250000000000000, -7.320508075688771932 ) ) ;
#30025=CARTESIAN_POINT ( 'NONE',  ( -6.123233995736766282E-16, 221.8750000068279746, -10.00000000000000000 ) ) ;
#30028=CARTESIAN_POINT ( 'NONE',  ( -11.35316468749999785, 239.0104166700806445, -3.042071309553164848 ) ) ;
#30035=CARTESIAN_POINT ( 'NONE',  ( 1.224646799147353256E-15, 0.000000000000000000, 10.00000000000000000 ) ) ;
#30059=CARTESIAN_POINT ( 'NONE',  ( -6.123233995736766282E-16, 263.7500000000000568, -10.00000000000000178 ) ) ;
#30061=ORIENTED_EDGE ( 'NONE', *, *, #63840, .F. ) ;
#30080=CARTESIAN_POINT ( 'NONE',  ( -3.042071309553159075, 234.9479166700806445, 11.35316468749999963 ) ) ;
#30083=CARTESIAN_POINT ( 'NONE',  ( -8.311093377946834337, 234.8437500034139305, 8.311093377946837890 ) ) ;
#30142=CARTESIAN_POINT ( 'NONE',  ( -9.999999999999998224, 253.3333333401613174, 2.679491924311235618 ) ) ;
#30166=LINE ( 'NONE', #74052, #27713 ) ;
#30190=CARTESIAN_POINT ( 'NONE',  ( -8.311093377946834337, 229.8437500034140157, 8.311093377946837890 ) ) ;
#30226=CARTESIAN_POINT ( 'NONE',  ( -3.042071309553159075, 249.9479166700806729, 11.35316468749999963 ) ) ;
#30277=CARTESIAN_POINT ( 'NONE',  ( -10.00000000000000000, 225.0000000000000000, 0.000000000000000000 ) ) ;
#30361=CARTESIAN_POINT ( 'NONE',  ( 11.35316468749999963, 236.1979166700806445, 3.042071309553159519 ) ) ;
#30367=CARTESIAN_POINT ( 'NONE',  ( -2.679491924311222295, 261.0416666666666856, 10.00000000000000178 ) ) ;
#30396=CARTESIAN_POINT ( 'NONE',  ( -3.042071309553166625, 228.1770833367473301, -11.35316468749999608 ) ) ;
#30404=DIRECTION ( 'NONE',  ( 0.000000000000000000, -0.9996144206527183274, -0.02776706724035331308 ) ) ;
#30411=CARTESIAN_POINT ( 'NONE',  ( 2.679491924311096174, 258.5416666666666856, -10.00000000000007283 ) ) ;
#30452=CARTESIAN_POINT ( 'NONE',  ( -11.35316468749999963, 228.9062500034139873, 0.000000000000000000 ) ) ;
#30456=CARTESIAN_POINT ( 'NONE',  ( -11.35316468749999785, 224.0104166700806161, -3.042071309553164848 ) ) ;
#30485=DIRECTION ( 'NONE',  ( -0.000000000000000000, -1.000000000000000000, -0.000000000000000000 ) ) ;
#30486=CARTESIAN_POINT ( 'NONE',  ( 2.679491924311234730, 231.4583333333333428, 9.999999999999998224 ) ) ;
#30510=CARTESIAN_POINT ( 'NONE',  ( -2.679491924311228512, 242.0833333401612606, -9.999999999999998224 ) ) ;
#30521=VECTOR ( 'NONE', #30404, 1000.000000000000000 ) ;
#30537=CARTESIAN_POINT ( 'NONE',  ( 3.042071309553163960, 262.7604166700806445, -11.35316468749999785 ) ) ;
#30560=CARTESIAN_POINT ( 'NONE',  ( -6.951808397369817780E-16, 222.9687500034139873, -11.35316468749999963 ) ) ;
#30594=CARTESIAN_POINT ( 'NONE',  ( 10.00000000000000178, 225.4166666734946602, 2.679491924311222739 ) ) ;
#30595=CARTESIAN_POINT ( 'NONE',  ( 8.311093377946834337, 252.0312500034139589, -8.311093377946836114 ) ) ;
#30621=ADVANCED_FACE ( 'NONE', ( #36706 ), #59718, .F. ) ;
#30644=CARTESIAN_POINT ( 'NONE',  ( 3.042071309553163960, 262.7604166700806445, -11.35316468749999785 ) ) ;
#30662=DIRECTION ( 'NONE',  ( 0.000000000000000000, 0.000000000000000000, -1.000000000000000000 ) ) ;
#30727=CARTESIAN_POINT ( 'NONE',  ( 11.35316468749999963, 226.4062500034139873, -1.390361679473963556E-15 ) ) ;
#30732=CARTESIAN_POINT ( 'NONE',  ( 8.660254037844385522, 262.9166666666666856, -5.000000000000003553 ) ) ;
#30737=CARTESIAN_POINT ( 'NONE',  ( 1.347111479062088405E-15, 0.000000000000000000, 11.00000000000000000 ) ) ;
#30744=ORIENTED_EDGE ( 'NONE', *, *, #45264, .F. ) ;
#30761=CARTESIAN_POINT ( 'NONE',  ( -5.676582343749992710, 225.0520833367473017, 9.832129032723422313 ) ) ;
#30812=CARTESIAN_POINT ( 'NONE',  ( 5.676582343749997150, 227.2395833367473301, -9.832129032723418760 ) ) ;
#30816=CARTESIAN_POINT ( 'NONE',  ( 11.35316468749999963, 221.5104166700805877, 3.042071309553159519 ) ) ;
#30847=DIRECTION ( 'NONE',  ( -0.000000000000000000, -1.000000000000000000, -0.000000000000000000 ) ) ;
#30850=CARTESIAN_POINT ( 'NONE',  ( 7.320508075688771044, 233.1250000000000284, -7.320508075688771932 ) ) ;
#30877=CARTESIAN_POINT ( 'NONE',  ( 5.000000000000004441, 244.7916666734946318, 8.660254037844385522 ) ) ;
#30900=CARTESIAN_POINT ( 'NONE',  ( 9.832129032723416984, 262.1354166700806445, -5.676582343750003368 ) ) ;
#30921=CARTESIAN_POINT ( 'NONE',  ( -8.311093377946836114, 233.5937500034139305, -8.311093377946836114 ) ) ;
#30933=EDGE_CURVE ( 'NONE', #35109, #53701, #48227, .T. ) ;
#30958=CARTESIAN_POINT ( 'NONE',  ( 5.000000000000004441, 224.7916666734946602, 8.660254037844385522 ) ) ;
#30959=CARTESIAN_POINT ( 'NONE',  ( -5.676582343750000703, 228.0729166700806729, -9.832129032723418760 ) ) ;
#31007=CARTESIAN_POINT ( 'NONE',  ( 4.999999999999997335, 228.3333333333333428, -8.660254037844387298 ) ) ;
#31015=CARTESIAN_POINT ( 'NONE',  ( 8.660254037844385522, 242.9166666666666572, -5.000000000000003553 ) ) ;
#31088=CARTESIAN_POINT ( 'NONE',  ( 3.042071309553163960, 227.4479166700806729, -11.35316468749999785 ) ) ;
#31089=AXIS2_PLACEMENT_3D ( 'NONE', #59240, #65990, #31672 ) ;
#31093=CARTESIAN_POINT ( 'NONE',  ( -10.00000000000000000, 259.7916666666666288, -2.679491924311226292 ) ) ;
#31125=CARTESIAN_POINT ( 'NONE',  ( -8.311093377946834337, 224.8437500034139589, 8.311093377946837890 ) ) ;
#31184=CARTESIAN_POINT ( 'NONE',  ( 11.35316468749999963, 221.1979166700806161, 3.042071309553159519 ) ) ;
#31187=CARTESIAN_POINT ( 'NONE',  ( -5.676582343749992710, 225.0520833367473017, 9.832129032723422313 ) ) ;
#31192=ORIENTED_EDGE ( 'NONE', *, *, #18755, .F. ) ;
#31220=CARTESIAN_POINT ( 'NONE',  ( 1.224646799147353256E-15, 0.000000000000000000, 10.00000000000000000 ) ) ;
#31247=CARTESIAN_POINT ( 'NONE',  ( -6.123233995736766282E-16, 236.8750000068279746, -10.00000000000000000 ) ) ;
#31284=CARTESIAN_POINT ( 'NONE',  ( -8.660254037844385522, 233.5416666734946318, 5.000000000000004441 ) ) ;
#31314=VECTOR ( 'NONE', #26910, 1000.000000000000000 ) ;
#31330=CARTESIAN_POINT ( 'NONE',  ( 9.832129032723416984, 231.8229166700806445, -5.676582343750003368 ) ) ;
#31364=ORIENTED_EDGE ( 'NONE', *, *, #52180, .T. ) ;
#31383=CARTESIAN_POINT ( 'NONE',  ( -6.951808397369817780E-16, 257.9687500034140157, -11.35316468749999963 ) ) ;
#31391=CARTESIAN_POINT ( 'NONE',  ( 2.679491924311292905, 241.4583333333333712, 9.999999999999968026 ) ) ;
#31401=CARTESIAN_POINT ( 'NONE',  ( -10.00000000000000000, 229.7916666666666572, -2.679491924311226292 ) ) ;
#31409=FACE_OUTER_BOUND ( 'NONE', #2155, .T. ) ;
#31473=CARTESIAN_POINT ( 'NONE',  ( -3.042071309553166181, 232.8645833367473017, -11.35316468749999608 ) ) ;
#31478=CARTESIAN_POINT ( 'NONE',  ( 5.000000000000004441, 261.6666666666666856, 8.660254037844385522 ) ) ;
#31507=CARTESIAN_POINT ( 'NONE',  ( 5.676582343749997150, 232.5520833367473301, -9.832129032723418760 ) ) ;
#31529=CARTESIAN_POINT ( 'NONE',  ( 8.660254037844389075, 245.2083333401613174, 4.999999999999997335 ) ) ;
#31563=CARTESIAN_POINT ( 'NONE',  ( -3.042071309553159075, 220.2604166700806161, 11.35316468749999963 ) ) ;
#31623=CARTESIAN_POINT ( 'NONE',  ( -2.679491924311222295, 239.1666666734946034, 10.00000000000000178 ) ) ;
#31646=CARTESIAN_POINT ( 'NONE',  ( -3.042071309553159075, 259.9479166700806445, 11.35316468749999963 ) ) ;
#31654=ORIENTED_EDGE ( 'NONE', *, *, #39451, .T. ) ;
#31672=DIRECTION ( 'NONE',  ( 0.000000000000000000, 0.000000000000000000, -1.000000000000000000 ) ) ;
#31711=CARTESIAN_POINT ( 'NONE',  ( 5.676582343750005144, 235.5729166700806729, 9.832129032723416984 ) ) ;
#31732=CONICAL_SURFACE ( 'NONE', #37775, 10.00000000000000000, 0.02777063659342106361 ) ;
#31741=EDGE_LOOP ( 'NONE', ( #50034, #71031, #73326, #19294 ) ) ;
#31760=CARTESIAN_POINT ( 'NONE',  ( -11.35316468749999785, 249.0104166700806445, -3.042071309553164848 ) ) ;
#31790=ORIENTED_EDGE ( 'NONE', *, *, #26612, .F. ) ;
#31804=DIRECTION ( 'NONE',  ( 0.000000000000000000, 0.000000000000000000, -1.000000000000000000 ) ) ;
#31823=CARTESIAN_POINT ( 'NONE',  ( 2.326828918379973337E-15, 0.000000000000000000, 19.00000000000001776 ) ) ;
#31843=CARTESIAN_POINT ( 'NONE',  ( -10.00000000000000000, 255.0000000000000000, 0.000000000000000000 ) ) ;
#31848=FACE_OUTER_BOUND ( 'NONE', #23885, .T. ) ;
#31850=CARTESIAN_POINT ( 'NONE',  ( -6.123233995736766282E-16, 248.7500000000000284, -10.00000000000000000 ) ) ;
#31879=CARTESIAN_POINT ( 'NONE',  ( 9.832129032723416984, 237.1354166700806445, -5.676582343750003368 ) ) ;
#31883=ADVANCED_FACE ( 'NONE', ( #45346, #61587 ), #57431, .F. ) ;
#31894=CARTESIAN_POINT ( 'NONE',  ( 5.000000000000004441, 256.6666666666666288, 8.660254037844385522 ) ) ;
#31903=CARTESIAN_POINT ( 'NONE',  ( 4.999999999999997335, 246.4583333401613174, -8.660254037844387298 ) ) ;
#31909=ADVANCED_FACE ( 'NONE', ( #22319 ), #55337, .T. ) ;
#31932=CARTESIAN_POINT ( 'NONE',  ( 9.832129032723416984, 221.8229166700806729, -5.676582343750003368 ) ) ;
#31935=CARTESIAN_POINT ( 'NONE',  ( -9.832129032723418760, 228.8020833367473301, -5.676582343749998927 ) ) ;
#31963=CARTESIAN_POINT ( 'NONE',  ( -10.67658234375000070, 263.5156250051209668, 0.000000000000000000 ) ) ;
#32001=CARTESIAN_POINT ( 'NONE',  ( -7.320508075688770155, 233.7500000068279462, 7.320508075688774596 ) ) ;
#32020=CARTESIAN_POINT ( 'NONE',  ( -7.320508075688771932, 257.5000000068279746, -7.320508075688771932 ) ) ;
#32021=CARTESIAN_POINT ( 'NONE',  ( -9.832129032723415207, 254.3229166700806729, 5.676582343750005144 ) ) ;
#32025=CARTESIAN_POINT ( 'NONE',  ( 9.832129032723420536, 261.3020833367473301, 5.676582343749996262 ) ) ;
#32080=CARTESIAN_POINT ( 'NONE',  ( 0.000000000000000000, 0.000000000000000000, 0.000000000000000000 ) ) ;
#32086=CARTESIAN_POINT ( 'NONE',  ( -11.35316468749999963, 233.9062500034139873, 0.000000000000000000 ) ) ;
#32138=CARTESIAN_POINT ( 'NONE',  ( 3.042071309553163960, 252.7604166700806445, -11.35316468749999785 ) ) ;
#32185=ORIENTED_EDGE ( 'NONE', *, *, #10764, .F. ) ;
#32187=EDGE_CURVE ( 'NONE', #43392, #71847, #2119, .T. ) ;
#32193=CARTESIAN_POINT ( 'NONE',  ( -7.320508075688771932, 247.5000000068279746, -7.320508075688771932 ) ) ;
#32225=CARTESIAN_POINT ( 'NONE',  ( -9.832129032723415207, 224.3229166700806729, 5.676582343750005144 ) ) ;
#32230=CARTESIAN_POINT ( 'NONE',  ( 2.679491924311235174, 256.4583333333333712, 9.999999999999998224 ) ) ;
#32262=CARTESIAN_POINT ( 'NONE',  ( 2.085542519210945334E-15, 220.4687500034139873, 11.35316468749999963 ) ) ;
#32314=CARTESIAN_POINT ( 'NONE',  ( 0.000000000000000000, 0.000000000000000000, 0.000000000000000000 ) ) ;
#32315=CARTESIAN_POINT ( 'NONE',  ( 3.042071309553173286, 220.3645833367473017, 11.35316468749999608 ) ) ;
#32320=CARTESIAN_POINT ( 'NONE',  ( 9.832129032723416984, 251.8229166700806729, -5.676582343750003368 ) ) ;
#32322=DIRECTION ( 'NONE',  ( 0.000000000000000000, 0.000000000000000000, -1.000000000000000000 ) ) ;
#32353=CARTESIAN_POINT ( 'NONE',  ( 9.832129032723420536, 251.3020833367473017, 5.676582343749996262 ) ) ;
#32355=EDGE_LOOP ( 'NONE', ( #70010, #17995, #25752, #44673, #48777, #45891, #23837 ) ) ;
#32379=CARTESIAN_POINT ( 'NONE',  ( 2.679491924311225848, 231.6666666734946318, -10.00000000000000000 ) ) ;
#32400=CARTESIAN_POINT ( 'NONE',  ( -3.042071309553166625, 257.8645833367473301, -11.35316468749999608 ) ) ;
#32405=CARTESIAN_POINT ( 'NONE',  ( -5.676582343749992710, 255.0520833367473301, 9.832129032723422313 ) ) ;
#32440=VERTEX_POINT ( 'NONE', #38694 ) ;
#32457=CYLINDRICAL_SURFACE ( 'NONE', #59320, 10.00000000000000000 ) ;
#32469=CARTESIAN_POINT ( 'NONE',  ( -9.832129032723415207, 239.3229166700806445, 5.676582343750005144 ) ) ;
#32522=CARTESIAN_POINT ( 'NONE',  ( 9.832129032723420536, 256.3020833367473301, 5.676582343749996262 ) ) ;
#32542=CARTESIAN_POINT ( 'NONE',  ( -5.000000000000000888, 229.1666666666666856, -8.660254037844387298 ) ) ;
#32613=CARTESIAN_POINT ( 'NONE',  ( -2.679491924311228512, 253.9583333333333428, -9.999999999999998224 ) ) ;
#32667=CARTESIAN_POINT ( 'NONE',  ( 7.320508075688771044, 238.1249999999999716, -7.320508075688771932 ) ) ;
#32696=CARTESIAN_POINT ( 'NONE',  ( -11.35316468749999963, 218.9062500034139873, 0.000000000000000000 ) ) ;
#32699=CARTESIAN_POINT ( 'NONE',  ( -3.042071309553159075, 254.9479166700806729, 11.35316468749999963 ) ) ;
#32706=CARTESIAN_POINT ( 'NONE',  ( 2.020667218593132706E-15, 219.9523502760175973, 11.00000000000000000 ) ) ;
#32732=CARTESIAN_POINT ( 'NONE',  ( -4.999999999999992895, 223.9583333401612890, 8.660254037844390851 ) ) ;
#32733=CARTESIAN_POINT ( 'NONE',  ( -3.042071309553166625, 258.1770833367473301, -11.35316468749999608 ) ) ;
#32759=CARTESIAN_POINT ( 'NONE',  ( 1.836970198721029589E-15, 219.3750000068279746, 10.00000000000000000 ) ) ;
#32760=CARTESIAN_POINT ( 'NONE',  ( -4.999999999999992895, 253.9583333401613174, 8.660254037844390851 ) ) ;
#32782=CARTESIAN_POINT ( 'NONE',  ( -11.35316468749999608, 254.1145833367473585, 3.042071309553173730 ) ) ;
#32786=CARTESIAN_POINT ( 'NONE',  ( -5.676582343750000703, 253.3854166700806445, -9.832129032723418760 ) ) ;
#32810=CARTESIAN_POINT ( 'NONE',  ( 1.836970198721029589E-15, 236.2500000000000284, 10.00000000000000000 ) ) ;
#32825=CARTESIAN_POINT ( 'NONE',  ( 1.836970198721029589E-15, 246.2500000000000284, 10.00000000000000000 ) ) ;
#32848=CARTESIAN_POINT ( 'NONE',  ( 9.832129032723416984, 226.8229166700806729, -5.676582343750003368 ) ) ;
#32853=EDGE_CURVE ( 'NONE', #46305, #26674, #66845, .T. ) ;
#32875=( LENGTH_UNIT ( ) NAMED_UNIT ( * ) SI_UNIT ( .MILLI., .METRE. ) );
#32885=CARTESIAN_POINT ( 'NONE',  ( -10.99999999999999822, 219.4226497308103774, 0.000000000000000000 ) ) ;
#32901=DIRECTION ( 'NONE',  ( -0.000000000000000000, -1.000000000000000000, -0.000000000000000000 ) ) ;
#32903=CARTESIAN_POINT ( 'NONE',  ( -3.042071309553159075, 250.2604166700806445, 11.35316468749999963 ) ) ;
#32938=CARTESIAN_POINT ( 'NONE',  ( -11.35316468749999963, 258.9062500034140157, 0.000000000000000000 ) ) ;
#32950=ORIENTED_EDGE ( 'NONE', *, *, #29706, .T. ) ;
#32992=CARTESIAN_POINT ( 'NONE',  ( 2.679491924311225848, 253.5416666666666572, -10.00000000000000000 ) ) ;
#33023=CARTESIAN_POINT ( 'NONE',  ( 3.042071309553163516, 222.7604166700806445, -11.35316468749999785 ) ) ;
#33033=VERTEX_POINT ( 'NONE', #61569 ) ;
#33080=CARTESIAN_POINT ( 'NONE',  ( 3.042071309553163960, 257.4479166700806445, -11.35316468749999785 ) ) ;
#33115=CARTESIAN_POINT ( 'NONE',  ( -6.123233995736766282E-16, 221.8750000068279746, -10.00000000000000000 ) ) ;
#33117=CARTESIAN_POINT ( 'NONE',  ( -5.676582343750000703, 253.3854166700806445, -9.832129032723418760 ) ) ;
#33143=CARTESIAN_POINT ( 'NONE',  ( -10.00000000000000000, 222.9166666734946602, -2.679491924311226292 ) ) ;
#33162=CARTESIAN_POINT ( 'NONE',  ( 1.836970198721029589E-15, 259.3750000068280315, 10.00000000000000000 ) ) ;
#33163=CARTESIAN_POINT ( 'NONE',  ( 5.676582343750005144, 260.5729166700806445, 9.832129032723416984 ) ) ;
#33168=CARTESIAN_POINT ( 'NONE',  ( -11.35316468749999608, 254.4270833367473585, 3.042071309553173730 ) ) ;
#33185=EDGE_LOOP ( 'NONE', ( #1899, #642, #16591, #19426 ) ) ;
#33200=ORIENTED_EDGE ( 'NONE', *, *, #32187, .F. ) ;
#33224=CARTESIAN_POINT ( 'NONE',  ( 3.042071309553163960, 222.4479166700806729, -11.35316468749999785 ) ) ;
#33260=EDGE_CURVE ( 'NONE', #24629, #52326, #39461, .T. ) ;
#33272=CARTESIAN_POINT ( 'NONE',  ( 8.311093377946834337, 237.3437500034139589, -8.311093377946836114 ) ) ;
#33307=DIRECTION ( 'NONE',  ( 0.000000000000000000, -1.000000000000000000, -0.000000000000000000 ) ) ;
#33323=CARTESIAN_POINT ( 'NONE',  ( -7.320508075688770155, 248.7500000068279746, 7.320508075688774596 ) ) ;
#33352=CARTESIAN_POINT ( 'NONE',  ( 2.085542519210945334E-15, 220.1562500034139873, 11.35316468749999963 ) ) ;
#33357=CARTESIAN_POINT ( 'NONE',  ( -9.999999999999998224, 245.2083333333333428, 2.679491924311235618 ) ) ;
#33387=CARTESIAN_POINT ( 'NONE',  ( -3.042071309553166625, 223.1770833367473017, -11.35316468749999608 ) ) ;
#33444=CARTESIAN_POINT ( 'NONE',  ( 8.311093377946839666, 260.7812500034140157, 8.311093377946829008 ) ) ;
#33460=CARTESIAN_POINT ( 'NONE',  ( -6.123233995736766282E-16, 241.8750000068280031, -10.00000000000000000 ) ) ;
#33479=CARTESIAN_POINT ( 'NONE',  ( 5.676582343750005144, 255.8854166700806445, 9.832129032723416984 ) ) ;
#33506=CARTESIAN_POINT ( 'NONE',  ( -10.00000000000000000, 223.1250000068279746, 0.000000000000000000 ) ) ;
#33532=CARTESIAN_POINT ( 'NONE',  ( -8.311093377946834337, 249.5312500034139873, 8.311093377946837890 ) ) ;
#33536=CARTESIAN_POINT ( 'NONE',  ( -8.311093377946834337, 254.8437500034139873, 8.311093377946837890 ) ) ;
#33595=CARTESIAN_POINT ( 'NONE',  ( -8.311093377946834337, 224.5312500034140157, 8.311093377946837890 ) ) ;
#33631=CARTESIAN_POINT ( 'NONE',  ( -2.679491924311106832, 256.0416666666666856, 10.00000000000006928 ) ) ;
#33643=CARTESIAN_POINT ( 'NONE',  ( 11.35316468749999963, 241.7187500034139873, -1.390361679473963556E-15 ) ) ;
#33681=CARTESIAN_POINT ( 'NONE',  ( 8.311093377946834337, 257.0312500034139020, -8.311093377946836114 ) ) ;
#33722=AXIS2_PLACEMENT_3D ( 'NONE', #61681, #14890, #9633 ) ;
#33727=CARTESIAN_POINT ( 'NONE',  ( 1.836970198721029589E-15, 251.2500000000000284, 10.00000000000000000 ) ) ;
#33732=CARTESIAN_POINT ( 'NONE',  ( -10.00000000000000000, 234.7916666666666856, -2.679491924311226292 ) ) ;
#33748=ADVANCED_FACE ( 'NONE', ( #70865, #35443 ), #58454, .F. ) ;
#33761=CARTESIAN_POINT ( 'NONE',  ( -11.35316468749999785, 224.0104166700806161, -3.042071309553164848 ) ) ;
#33818=CIRCLE ( 'NONE', #1297, 11.00000000000000000 ) ;
#33819=CARTESIAN_POINT ( 'NONE',  ( -8.311093377946836114, 253.2812500034139873, -8.311093377946836114 ) ) ;
#33839=CARTESIAN_POINT ( 'NONE',  ( 2.085542519210945334E-15, 220.4687500034139873, 11.35316468749999963 ) ) ;
#33853=CARTESIAN_POINT ( 'NONE',  ( 9.832129032723416984, 257.1354166700806445, -5.676582343750003368 ) ) ;
#33881=CARTESIAN_POINT ( 'NONE',  ( -6.123233995736766282E-16, 226.8750000068279746, -10.00000000000000000 ) ) ;
#33906=CARTESIAN_POINT ( 'NONE',  ( 0.000000000000000000, 265.0000000000000000, 0.000000000000000000 ) ) ;
#33908=CARTESIAN_POINT ( 'NONE',  ( 11.35316468749999608, 246.6145833367473017, -3.042071309553167513 ) ) ;
#33911=CARTESIAN_POINT ( 'NONE',  ( -5.676582343750000703, 258.3854166700806445, -9.832129032723418760 ) ) ;
#33947=CARTESIAN_POINT ( 'NONE',  ( -6.123233995736766282E-16, 258.7500000000000568, -10.00000000000000000 ) ) ;
#33964=ORIENTED_EDGE ( 'NONE', *, *, #15384, .T. ) ;
#33974=CARTESIAN_POINT ( 'NONE',  ( 2.085542519210945334E-15, 220.1562500034139873, 11.35316468749999963 ) ) ;
#33996=CARTESIAN_POINT ( 'NONE',  ( 1.836970198721029589E-15, 221.2500000000000000, 10.00000000000000000 ) ) ;
#34023=CARTESIAN_POINT ( 'NONE',  ( 2.085542519210945334E-15, 240.4687500034139873, 11.35316468749999963 ) ) ;
#34059=CARTESIAN_POINT ( 'NONE',  ( 11.35316468749999608, 261.6145833367473301, -3.042071309553167069 ) ) ;
#34064=CARTESIAN_POINT ( 'NONE',  ( -6.123233995736766282E-16, 253.7500000000000284, -10.00000000000000000 ) ) ;
#34080=CARTESIAN_POINT ( 'NONE',  ( 1.836970198721029589E-15, 246.2500000000000284, 10.00000000000000000 ) ) ;
#34082=VECTOR ( 'NONE', #40443, 1000.000000000000000 ) ;
#34088=VERTEX_POINT ( 'NONE', #56136 ) ;
#34092=CARTESIAN_POINT ( 'NONE',  ( 0.000000000000000000, 0.000000000000000000, 0.000000000000000000 ) ) ;
#34106=CARTESIAN_POINT ( 'NONE',  ( 2.679491924311235174, 231.4583333333333428, 9.999999999999998224 ) ) ;
#34185=CARTESIAN_POINT ( 'NONE',  ( -11.35316468749999963, 238.9062500034140157, 0.000000000000000000 ) ) ;
#34222=CARTESIAN_POINT ( 'NONE',  ( -5.676582343750000703, 248.3854166700806445, -9.832129032723418760 ) ) ;
#34265=CYLINDRICAL_SURFACE ( 'NONE', #17480, 11.00000000000000000 ) ;
#34277=CARTESIAN_POINT ( 'NONE',  ( 8.311093377946839666, 250.7812500034140157, 8.311093377946830785 ) ) ;
#34281=CARTESIAN_POINT ( 'NONE',  ( -11.35316468749999963, 244.2187500034140157, 0.000000000000000000 ) ) ;
#34321=EDGE_CURVE ( 'NONE', #46305, #32440, #65009, .T. ) ;
#34344=CARTESIAN_POINT ( 'NONE',  ( 11.35316468749999963, 226.1979166700806729, 3.042071309553159519 ) ) ;
#34393=CARTESIAN_POINT ( 'NONE',  ( -9.832129032723418760, 238.8020833367473301, -5.676582343749998927 ) ) ;
#34429=CARTESIAN_POINT ( 'NONE',  ( 2.085542519210945334E-15, 255.1562500034140157, 11.35316468749999963 ) ) ;
#34459=DIRECTION ( 'NONE',  ( 1.000000000000000000, 0.000000000000000000, 0.000000000000000000 ) ) ;
#34479=CARTESIAN_POINT ( 'NONE',  ( 8.660254037844385522, 237.9166666666666572, -5.000000000000003553 ) ) ;
#34523=DIRECTION ( 'NONE',  ( 0.000000000000000000, 0.000000000000000000, -1.000000000000000000 ) ) ;
#34550=CARTESIAN_POINT ( 'NONE',  ( 2.679491924311117934, 251.6666666734946887, -10.00000000000006217 ) ) ;
#34563=CARTESIAN_POINT ( 'NONE',  ( -5.676582343750000703, 243.0729166700806445, -9.832129032723418760 ) ) ;
#34574=CARTESIAN_POINT ( 'NONE',  ( -11.35316468749999963, 263.9062500034140157, 0.000000000000000000 ) ) ;
#34595=CARTESIAN_POINT ( 'NONE',  ( 11.35316468749999963, 241.7187500034139873, -1.390361679473963556E-15 ) ) ;
#34652=CARTESIAN_POINT ( 'NONE',  ( 5.676582343750005144, 240.5729166700806445, 9.832129032723416984 ) ) ;
#34657=CARTESIAN_POINT ( 'NONE',  ( 8.311093377946834337, 237.3437500034139589, -8.311093377946836114 ) ) ;
#34711=CARTESIAN_POINT ( 'NONE',  ( -6.123233995736766282E-16, 256.8750000068279746, -10.00000000000000000 ) ) ;
#34767=CARTESIAN_POINT ( 'NONE',  ( 11.35316468749999963, 236.5104166700806161, 3.042071309553159519 ) ) ;
#34775=CARTESIAN_POINT ( 'NONE',  ( 1.224646799147353256E-15, 0.000000000000000000, 10.00000000000000000 ) ) ;
#34781=CARTESIAN_POINT ( 'NONE',  ( 9.999999999999998224, 227.7083333333333144, -2.679491924311229401 ) ) ;
#34802=CARTESIAN_POINT ( 'NONE',  ( 11.35316468749999608, 246.6145833367472733, -3.042071309553167069 ) ) ;
#34852=CARTESIAN_POINT ( 'NONE',  ( -10.00000000000000000, 240.0000000000000284, 0.000000000000000000 ) ) ;
#34935=CARTESIAN_POINT ( 'NONE',  ( 3.042071309553163960, 247.4479166700806445, -11.35316468749999785 ) ) ;
#34967=CARTESIAN_POINT ( 'NONE',  ( -9.832129032723418760, 248.8020833367473301, -5.676582343749998927 ) ) ;
#34987=FACE_OUTER_BOUND ( 'NONE', #65104, .T. ) ;
#35011=CIRCLE ( 'NONE', #22984, 10.00000000000000000 ) ;
#35023=CARTESIAN_POINT ( 'NONE',  ( 11.35316468749999963, 231.1979166700806445, 3.042071309553159519 ) ) ;
#35026=CARTESIAN_POINT ( 'NONE',  ( -3.042071309553159075, 245.2604166700806729, 11.35316468749999963 ) ) ;
#35038=FACE_OUTER_BOUND ( 'NONE', #50217, .T. ) ;
#35048=CARTESIAN_POINT ( 'NONE',  ( -7.320508075688770155, 235.6250000000000000, 7.320508075688774596 ) ) ;
#35080=CARTESIAN_POINT ( 'NONE',  ( -7.320508075688770155, 253.7500000068279462, 7.320508075688774596 ) ) ;
#35109=VERTEX_POINT ( 'NONE', #47438 ) ;
#35110=ORIENTED_EDGE ( 'NONE', *, *, #1965, .T. ) ;
#35130=CARTESIAN_POINT ( 'NONE',  ( -11.35316468749999963, 229.2187500034139873, 0.000000000000000000 ) ) ;
#35167=CARTESIAN_POINT ( 'NONE',  ( 9.832129032723416984, 251.8229166700806729, -5.676582343750003368 ) ) ;
#35206=ADVANCED_FACE ( 'NONE', ( #35038 ), #41423, .F. ) ;
#35215=CARTESIAN_POINT ( 'NONE',  ( -4.999999999999992895, 235.8333333333333428, 8.660254037844390851 ) ) ;
#35223=CARTESIAN_POINT ( 'NONE',  ( -2.679491924311222295, 229.1666666734946034, 10.00000000000000178 ) ) ;
#35235=VECTOR ( 'NONE', #41438, 1000.000000000000000 ) ;
#35300=CARTESIAN_POINT ( 'NONE',  ( -9.832129032723415207, 249.3229166700806729, 5.676582343750005144 ) ) ;
#35337=CARTESIAN_POINT ( 'NONE',  ( 11.35316468749999963, 246.7187500034139873, -1.390361679473963556E-15 ) ) ;
#35386=DIRECTION ( 'NONE',  ( 0.000000000000000000, 0.000000000000000000, -1.000000000000000000 ) ) ;
#35389=CARTESIAN_POINT ( 'NONE',  ( -9.832129032723418760, 228.4895833367473585, -5.676582343749998927 ) ) ;
#35393=CARTESIAN_POINT ( 'NONE',  ( -6.951808397369817780E-16, 237.9687500034139873, -11.35316468749999963 ) ) ;
#35406=EDGE_LOOP ( 'NONE', ( #31790, #69984, #29165, #4481 ) ) ;
#35443=FACE_BOUND ( 'NONE', #1327, .T. ) ;
#35446=DIRECTION ( 'NONE',  ( 0.000000000000000000, 0.000000000000000000, -1.000000000000000000 ) ) ;
#35447=CARTESIAN_POINT ( 'NONE',  ( 2.679491924311225848, 246.6666666734946602, -10.00000000000000000 ) ) ;
#35461=EDGE_LOOP ( 'NONE', ( #23338, #14628, #29587, #43999 ) ) ;
#35465=LINE ( 'NONE', #42581, #63907 ) ;
#35483=CARTESIAN_POINT ( 'NONE',  ( -8.660254037844387298, 232.7083333401613174, -4.999999999999999112 ) ) ;
#35492=CARTESIAN_POINT ( 'NONE',  ( -11.35316468749999785, 229.0104166700806445, -3.042071309553164848 ) ) ;
#35529=CARTESIAN_POINT ( 'NONE',  ( 9.832129032723416984, 241.8229166700806445, -5.676582343750003368 ) ) ;
#35577=CARTESIAN_POINT ( 'NONE',  ( 10.00000000000000000, 222.5000000000000000, -1.224646799147353256E-15 ) ) ;
#35605=ORIENTED_EDGE ( 'NONE', *, *, #7880, .F. ) ;
#35638=ORIENTED_EDGE ( 'NONE', *, *, #56056, .T. ) ;
#35651=CARTESIAN_POINT ( 'NONE',  ( 2.679491924311096174, 256.6666666734946602, -10.00000000000007283 ) ) ;
#35661=CARTESIAN_POINT ( 'NONE',  ( -5.676582343750000703, 248.0729166700806729, -9.832129032723418760 ) ) ;
#35666=CARTESIAN_POINT ( 'NONE',  ( -8.660254037844387298, 259.5833333333333144, -4.999999999999999112 ) ) ;
#35688=CARTESIAN_POINT ( 'NONE',  ( -5.000000000000000888, 237.2916666734946318, -8.660254037844387298 ) ) ;
#35694=CARTESIAN_POINT ( 'NONE',  ( -11.35316468749999963, 239.2187500034139873, 0.000000000000000000 ) ) ;
#35701=DIRECTION ( 'NONE',  ( -0.000000000000000000, -1.000000000000000000, -0.000000000000000000 ) ) ;
#35724=CARTESIAN_POINT ( 'NONE',  ( -2.679491924311383499, 263.9583333333334281, -9.999999999999909406 ) ) ;
#35747=CARTESIAN_POINT ( 'NONE',  ( -5.676582343750000703, 228.0729166700806729, -9.832129032723418760 ) ) ;
#35752=CARTESIAN_POINT ( 'NONE',  ( -11.35316468749999608, 234.4270833367473017, 3.042071309553173730 ) ) ;
#35763=CARTESIAN_POINT ( 'NONE',  ( 0.000000000000000000, 265.0000000000000000, 0.000000000000000000 ) ) ;
#35804=DIRECTION ( 'NONE',  ( 0.000000000000000000, -1.000000000000000000, -0.000000000000000000 ) ) ;
#35810=CARTESIAN_POINT ( 'NONE',  ( 7.320508075688771044, 256.2500000068279746, -7.320508075688771932 ) ) ;
#35850=( BOUNDED_CURVE ( )  B_SPLINE_CURVE ( 2, ( #525, #35223, #57865, #29916, #17474, #11822, #1983, #41241, #63500, #41606, #6171, #29180, #896 ),
 .UNSPECIFIED., .F., .F. ) 
 B_SPLINE_CURVE_WITH_KNOTS ( ( 3, 2, 2, 2, 2, 2, 3 ),
 ( 0.7500000000000000000, 0.7592592592592593004, 0.7685185185185184897, 0.7777777777777777901, 0.7870370370370370905, 0.7962962962962962798, 0.8055555555555555802 ),
 .UNSPECIFIED. ) 
 CURVE ( )  GEOMETRIC_REPRESENTATION_ITEM ( )  RATIONAL_B_SPLINE_CURVE ( ( 1.000000000000000000, 0.9659258262890683122, 1.000000000000000000, 0.9659258262890683122, 1.000000000000000000, 0.9659258262890683122, 1.000000000000000000, 0.9659258262890683122, 1.000000000000000000, 0.9659258262890683122, 1.000000000000000000, 0.9659258262890683122, 1.000000000000000000 ) ) 
 REPRESENTATION_ITEM ( '' )  );
#35858=CARTESIAN_POINT ( 'NONE',  ( 5.676582343750005144, 230.8854166700806729, 9.832129032723416984 ) ) ;
#35896=CARTESIAN_POINT ( 'NONE',  ( 3.042071309553163960, 247.4479166700806445, -11.35316468749999785 ) ) ;
#35943=CARTESIAN_POINT ( 'NONE',  ( 2.679491924311235174, 226.4583333333333144, 9.999999999999998224 ) ) ;
#35952=CARTESIAN_POINT ( 'NONE',  ( 1.347111479062088405E-15, 45.00000000000000000, 11.00000000000000000 ) ) ;
#36019=CARTESIAN_POINT ( 'NONE',  ( 9.999999999999998224, 255.8333333401613459, -2.679491924311229401 ) ) ;
#36029=CARTESIAN_POINT ( 'NONE',  ( 8.311093377946834337, 232.0312500034139873, -8.311093377946836114 ) ) ;
#36035=CARTESIAN_POINT ( 'NONE',  ( 4.999999999999997335, 263.3333333333333712, -8.660254037844387298 ) ) ;
#36063=CARTESIAN_POINT ( 'NONE',  ( 9.832129032723416984, 227.1354166700806729, -5.676582343750003368 ) ) ;
#36092=CARTESIAN_POINT ( 'NONE',  ( -8.660254037844387298, 264.5833333333333144, -4.999999999999999112 ) ) ;
#36114=CARTESIAN_POINT ( 'NONE',  ( 8.311093377946834337, 232.0312500034139873, -8.311093377946836114 ) ) ;
#36118=CARTESIAN_POINT ( 'NONE',  ( 11.35316468749999963, 226.5104166700806445, 3.042071309553159519 ) ) ;
#36174=CARTESIAN_POINT ( 'NONE',  ( 7.320508075688771044, 241.2500000068279178, -7.320508075688771932 ) ) ;
#36225=CARTESIAN_POINT ( 'NONE',  ( -11.35316468749999963, 224.2187500034139873, 0.000000000000000000 ) ) ;
#36263=CARTESIAN_POINT ( 'NONE',  ( -9.832129032723418760, 248.4895833367473301, -5.676582343749998927 ) ) ;
#36312=CARTESIAN_POINT ( 'NONE',  ( 5.000000000000004441, 221.6666666666666856, 8.660254037844385522 ) ) ;
#36384=CARTESIAN_POINT ( 'NONE',  ( 1.836970198721029589E-15, 254.3750000068280031, 10.00000000000000000 ) ) ;
#36394=CARTESIAN_POINT ( 'NONE',  ( -6.951808397369817780E-16, 232.6562500034139873, -11.35316468749999963 ) ) ;
#36411=CARTESIAN_POINT ( 'NONE',  ( 1.836970198721029589E-15, 261.2500000000000568, 10.00000000000000000 ) ) ;
#36430=CARTESIAN_POINT ( 'NONE',  ( 9.832129032723420536, 226.3020833367473301, 5.676582343749996262 ) ) ;
#36483=CARTESIAN_POINT ( 'NONE',  ( 8.311093377946839666, 225.7812500034140157, 8.311093377946830785 ) ) ;
#36486=ORIENTED_EDGE ( 'NONE', *, *, #62144, .T. ) ;
#36487=CARTESIAN_POINT ( 'NONE',  ( 11.35316468749999963, 221.7187500034139873, -1.390361679473963556E-15 ) ) ;
#36545=CARTESIAN_POINT ( 'NONE',  ( 8.660254037844389075, 235.2083333401613174, 4.999999999999997335 ) ) ;
#36592=CARTESIAN_POINT ( 'NONE',  ( -8.311093377946834337, 224.8437500034139589, 8.311093377946837890 ) ) ;
#36621=DIRECTION ( 'NONE',  ( -0.000000000000000000, -1.000000000000000000, -0.000000000000000000 ) ) ;
#36632=CARTESIAN_POINT ( 'NONE',  ( -9.832129032723418760, 238.4895833367473301, -5.676582343749998927 ) ) ;
#36680=CARTESIAN_POINT ( 'NONE',  ( -4.999999999999992895, 220.8333333333333428, 8.660254037844390851 ) ) ;
#36689=CARTESIAN_POINT ( 'NONE',  ( 4.999999999999997335, 243.3333333333333428, -8.660254037844387298 ) ) ;
#36700=CARTESIAN_POINT ( 'NONE',  ( 1.836970198721029589E-15, 231.2500000000000000, 10.00000000000000000 ) ) ;
#36706=FACE_OUTER_BOUND ( 'NONE', #32355, .T. ) ;
#36718=( BOUNDED_CURVE ( )  B_SPLINE_CURVE ( 2, ( #16221, #39260, #68295, #10961, #39631, #16592, #67188, #27182, #62258, #74325, #62630, #15486, #33996 ),
 .UNSPECIFIED., .F., .F. ) 
 B_SPLINE_CURVE_WITH_KNOTS ( ( 3, 2, 2, 2, 2, 2, 3 ),
 ( 0.9166666666666668517, 0.9259259259259261521, 0.9351851851851854525, 0.9444444444444445308, 0.9537037037037038312, 0.9629629629629630205, 0.9722222222222223209 ),
 .UNSPECIFIED. ) 
 CURVE ( )  GEOMETRIC_REPRESENTATION_ITEM ( )  RATIONAL_B_SPLINE_CURVE ( ( 0.9999999999999992228, 0.9659258262890690894, 1.000000000000000000, 0.9659258262890683122, 1.000000000000000000, 0.9659258262890683122, 1.000000000000000000, 0.9659258262890683122, 1.000000000000000000, 0.9659258262890683122, 1.000000000000000000, 0.9659258262890678681, 1.000000000000000444 ) ) 
 REPRESENTATION_ITEM ( '' )  );
#36765=CARTESIAN_POINT ( 'NONE',  ( 2.085542519210945334E-15, 230.1562500034139873, 11.35316468749999963 ) ) ;
#36769=CARTESIAN_POINT ( 'NONE',  ( 7.320508075688771044, 263.1249999999999432, -7.320508075688771932 ) ) ;
#36777=CARTESIAN_POINT ( 'NONE',  ( -6.123233995736766282E-16, 261.8750000068280315, -10.00000000000000000 ) ) ;
#36798=CARTESIAN_POINT ( 'NONE',  ( 2.085542519210945334E-15, 225.4687500034139873, 11.35316468749999963 ) ) ;
#36800=ORIENTED_EDGE ( 'NONE', *, *, #65344, .T. ) ;
#36853=CARTESIAN_POINT ( 'NONE',  ( -6.951808397369817780E-16, 222.6562500034139873, -11.35316468749999963 ) ) ;
#36856=CARTESIAN_POINT ( 'NONE',  ( 8.311093377946839666, 226.0937500034140157, 8.311093377946829008 ) ) ;
#36875=AXIS2_PLACEMENT_3D ( 'NONE', #21273, #49953, #61650 ) ;
#36910=CARTESIAN_POINT ( 'NONE',  ( 7.320508075688776373, 261.8750000000000000, 7.320508075688767491 ) ) ;
#36914=CARTESIAN_POINT ( 'NONE',  ( -7.320508075688771932, 232.5000000068279462, -7.320508075688771932 ) ) ;
#36937=DIRECTION ( 'NONE',  ( -0.000000000000000000, -1.000000000000000000, -0.000000000000000000 ) ) ;
#36997=CARTESIAN_POINT ( 'NONE',  ( -3.042071309553159075, 234.9479166700806445, 11.35316468749999963 ) ) ;
#37000=EDGE_CURVE ( 'NONE', #23729, #46331, #6350, .T. ) ;
#37045=CARTESIAN_POINT ( 'NONE',  ( 8.660254037844389075, 222.0833333333333428, 4.999999999999997335 ) ) ;
#37066=CARTESIAN_POINT ( 'NONE',  ( -8.660254037844385522, 230.4166666666666856, 5.000000000000004441 ) ) ;
#37131=CARTESIAN_POINT ( 'NONE',  ( 2.085542519210945334E-15, 225.1562500034139873, 11.35316468749999963 ) ) ;
#37165=CARTESIAN_POINT ( 'NONE',  ( 8.001991528333338266, 220.1059721264024347, 6.140144111190926957 ) ) ;
#37167=CARTESIAN_POINT ( 'NONE',  ( 8.311093377946834337, 227.3437500034140157, -8.311093377946836114 ) ) ;
#37182=CARTESIAN_POINT ( 'NONE',  ( 10.00000000000000000, 257.5000000000000000, -1.224646799147353256E-15 ) ) ;
#37226=CARTESIAN_POINT ( 'NONE',  ( -6.951808397369817780E-16, 232.9687500034139873, -11.35316468749999963 ) ) ;
#37282=ORIENTED_EDGE ( 'NONE', *, *, #32853, .F. ) ;
#37289=CARTESIAN_POINT ( 'NONE',  ( -2.679491924311222295, 244.1666666734946318, 10.00000000000000178 ) ) ;
#37307=CARTESIAN_POINT ( 'NONE',  ( 3.042071309553163516, 262.4479166700805877, -11.35316468749999785 ) ) ;
#37327=CARTESIAN_POINT ( 'NONE',  ( -2.679491924311228512, 232.0833333401613174, -9.999999999999998224 ) ) ;
#37370=CARTESIAN_POINT ( 'NONE',  ( 8.311093377946834337, 237.0312500034140157, -8.311093377946836114 ) ) ;
#37423=CARTESIAN_POINT ( 'NONE',  ( 5.676582343750005144, 250.8854166700806729, 9.832129032723416984 ) ) ;
#37463=DIRECTION ( 'NONE',  ( 0.8660254037844389297, 0.4999999999999994449, -0.000000000000000000 ) ) ;
#37510=CARTESIAN_POINT ( 'NONE',  ( -11.35316468749999785, 228.6979166700806729, -3.042071309553164848 ) ) ;
#37515=CARTESIAN_POINT ( 'NONE',  ( -10.00000000000000000, 244.7916666666666856, -2.679491924311226292 ) ) ;
#37538=FACE_OUTER_BOUND ( 'NONE', #43581, .T. ) ;
#37544=CARTESIAN_POINT ( 'NONE',  ( 8.311093377946839666, 231.0937500034139873, 8.311093377946830785 ) ) ;
#37596=CARTESIAN_POINT ( 'NONE',  ( -9.832129032723418760, 223.4895833367473301, -5.676582343749998927 ) ) ;
#37601=CARTESIAN_POINT ( 'NONE',  ( 2.085542519210945334E-15, 230.4687500034139873, 11.35316468749999963 ) ) ;
#37623=ADVANCED_FACE ( 'NONE', ( #53527 ), #12412, .F. ) ;
#37639=CARTESIAN_POINT ( 'NONE',  ( 1.836970198721029589E-15, 231.2500000000000000, 10.00000000000000000 ) ) ;
#37665=CARTESIAN_POINT ( 'NONE',  ( 10.00000000000000000, 240.6250000068279746, -1.224646799147353256E-15 ) ) ;
#37686=CARTESIAN_POINT ( 'NONE',  ( -10.00000000000000000, 257.9166666734946602, -2.679491924311226292 ) ) ;
#37687=CARTESIAN_POINT ( 'NONE',  ( -8.311093377946836114, 258.2812500034140157, -8.311093377946836114 ) ) ;
#37690=CARTESIAN_POINT ( 'NONE',  ( 11.35316468749999963, 261.7187500034140157, -1.390361679473963556E-15 ) ) ;
#37710=CYLINDRICAL_SURFACE ( 'NONE', #31089, 10.00000000000000000 ) ;
#37729=CARTESIAN_POINT ( 'NONE',  ( -10.00000000000000000, 260.0000000000000000, 0.000000000000000000 ) ) ;
#37751=CARTESIAN_POINT ( 'NONE',  ( 11.35316468749999608, 231.6145833367473017, -3.042071309553167069 ) ) ;
#37775=AXIS2_PLACEMENT_3D ( 'NONE', #1647, #47274, #59719 ) ;
#37779=CARTESIAN_POINT ( 'NONE',  ( 7.320508075688776373, 235.0000000068279746, 7.320508075688767491 ) ) ;
#37802=CARTESIAN_POINT ( 'NONE',  ( 9.832129032723416984, 257.1354166700806445, -5.676582343750003368 ) ) ;
#37848=CARTESIAN_POINT ( 'NONE',  ( 8.660254037844389075, 230.2083333401612890, 4.999999999999997335 ) ) ;
#37885=CARTESIAN_POINT ( 'NONE',  ( 9.832129032723416984, 221.8229166700806729, -5.676582343750003368 ) ) ;
#37890=CARTESIAN_POINT ( 'NONE',  ( -8.660254037844385522, 250.4166666666666856, 5.000000000000004441 ) ) ;
#37950=ORIENTED_EDGE ( 'NONE', *, *, #17798, .T. ) ;
#37973=CARTESIAN_POINT ( 'NONE',  ( -8.311093377946834337, 219.5312500034139873, 8.311093377946837890 ) ) ;
#37976=CARTESIAN_POINT ( 'NONE',  ( -5.676582343749992710, 254.7395833367473301, 9.832129032723422313 ) ) ;
#38009=CARTESIAN_POINT ( 'NONE',  ( 3.042071309553173286, 255.6770833367473301, 11.35316468749999608 ) ) ;
#38036=CARTESIAN_POINT ( 'NONE',  ( 9.999999999999998224, 230.8333333401612890, -2.679491924311229401 ) ) ;
#38059=CARTESIAN_POINT ( 'NONE',  ( 5.676582343749997150, 252.2395833367473301, -9.832129032723418760 ) ) ;
#38067=ORIENTED_EDGE ( 'NONE', *, *, #26612, .T. ) ;
#38123=CARTESIAN_POINT ( 'NONE',  ( -3.042071309553166181, 237.8645833367473301, -11.35316468749999608 ) ) ;
#38125=ORIENTED_EDGE ( 'NONE', *, *, #10764, .T. ) ;
#38174=CARTESIAN_POINT ( 'NONE',  ( 9.832129032723416984, 262.1354166700806445, -5.676582343750003368 ) ) ;
#38248=( BOUNDED_CURVE ( )  B_SPLINE_CURVE ( 2, ( #46115, #69133, #29144, #494, #40461, #18560, #862 ),
 .UNSPECIFIED., .F., .F. ) 
 B_SPLINE_CURVE_WITH_KNOTS ( ( 3, 2, 2, 3 ),
 ( 0.000000000000000000, 0.009259259259259060987, 0.01851851851851812197, 0.02777777777777718296 ),
 .UNSPECIFIED. ) 
 CURVE ( )  GEOMETRIC_REPRESENTATION_ITEM ( )  RATIONAL_B_SPLINE_CURVE ( ( 1.000000000000000000, 0.9659258262890683122, 1.000000000000000000, 0.9659258262890683122, 1.000000000000000000, 0.9659258262890705327, 0.9999999999999977796 ) ) 
 REPRESENTATION_ITEM ( '' )  );
#38261=CARTESIAN_POINT ( 'NONE',  ( -5.000000000000000888, 254.1666666666666572, -8.660254037844387298 ) ) ;
#38299=CARTESIAN_POINT ( 'NONE',  ( 0.6686838642329748783, 220.0000000000000284, 10.97965672913483814 ) ) ;
#38345=CARTESIAN_POINT ( 'NONE',  ( 2.085542519210945334E-15, 260.1562500034140157, 11.35316468749999963 ) ) ;
#38381=CARTESIAN_POINT ( 'NONE',  ( 2.085542519210945334E-15, 255.4687500034140157, 11.35316468749999963 ) ) ;
#38410=CARTESIAN_POINT ( 'NONE',  ( 8.660254037844385522, 231.0416666734946318, -5.000000000000003553 ) ) ;
#38414=AXIS2_PLACEMENT_3D ( 'NONE', #22659, #18865, #18129 ) ;
#38432=CARTESIAN_POINT ( 'NONE',  ( 11.35316468749999608, 261.6145833367473301, -3.042071309553167513 ) ) ;
#38436=CARTESIAN_POINT ( 'NONE',  ( -3.042071309553166181, 248.1770833367472733, -11.35316468749999608 ) ) ;
#38497=CARTESIAN_POINT ( 'NONE',  ( 8.660254037844389075, 260.2083333401612890, 4.999999999999997335 ) ) ;
#38521=DIRECTION ( 'NONE',  ( -0.000000000000000000, -1.000000000000000000, -0.000000000000000000 ) ) ;
#38531=ORIENTED_EDGE ( 'NONE', *, *, #27970, .T. ) ;
#38553=CARTESIAN_POINT ( 'NONE',  ( 11.35316468749999963, 261.7187500034140157, -1.390361679473963556E-15 ) ) ;
#38587=DIRECTION ( 'NONE',  ( 0.000000000000000000, 0.000000000000000000, -1.000000000000000000 ) ) ;
#38589=EDGE_LOOP ( 'NONE', ( #69083, #71564 ) ) ;
#38610=( BOUNDED_CURVE ( )  B_SPLINE_CURVE ( 2, ( #16630, #69453, #51722, #71, #23050, #46061, #63783, #6460, #29463, #70199, #71281, #1547, #48276 ),
 .UNSPECIFIED., .F., .F. ) 
 B_SPLINE_CURVE_WITH_KNOTS ( ( 3, 2, 2, 2, 2, 2, 3 ),
 ( 0.5277777777777775681, 0.5370370370370368684, 0.5462962962962960578, 0.5555555555555553582, 0.5648148148148145475, 0.5740740740740738479, 0.5833333333333331483 ),
 .UNSPECIFIED. ) 
 CURVE ( )  GEOMETRIC_REPRESENTATION_ITEM ( )  RATIONAL_B_SPLINE_CURVE ( ( 1.000000000000000888, 0.9659258262890675351, 1.000000000000000000, 0.9659258262890683122, 1.000000000000000000, 0.9659258262890683122, 1.000000000000000000, 0.9659258262890683122, 1.000000000000000000, 0.9659258262890683122, 1.000000000000000000, 0.9659258262890690894, 0.9999999999999992228 ) ) 
 REPRESENTATION_ITEM ( '' )  );
#38639=CARTESIAN_POINT ( 'NONE',  ( 1.836970198721029589E-15, 224.3750000068279746, 10.00000000000000000 ) ) ;
#38640=CARTESIAN_POINT ( 'NONE',  ( 7.320508075688776373, 246.8750000000000284, 7.320508075688767491 ) ) ;
#38668=CARTESIAN_POINT ( 'NONE',  ( -6.123233995736766282E-16, 223.7500000000000000, -10.00000000000000000 ) ) ;
#38680=CYLINDRICAL_SURFACE ( 'NONE', #33722, 10.00000000000000000 ) ;
#38694=CARTESIAN_POINT ( 'NONE',  ( 1.836970198721029589E-15, 244.3750000068280031, 10.00000000000000000 ) ) ;
#38728=CARTESIAN_POINT ( 'NONE',  ( -11.35316468749999963, 263.9062500034140157, 0.000000000000000000 ) ) ;
#38761=CARTESIAN_POINT ( 'NONE',  ( -6.951808397369817780E-16, 262.9687500034140157, -11.35316468749999963 ) ) ;
#38772=DIRECTION ( 'NONE',  ( -0.000000000000000000, -1.000000000000000000, -0.000000000000000000 ) ) ;
#38784=CARTESIAN_POINT ( 'NONE',  ( 5.000000000000004441, 224.7916666734946602, 8.660254037844385522 ) ) ;
#38788=VECTOR ( 'NONE', #16431, 1000.000000000000000 ) ;
#38807=CARTESIAN_POINT ( 'NONE',  ( -5.676582343750000703, 263.0729166700806445, -9.832129032723418760 ) ) ;
#38812=CARTESIAN_POINT ( 'NONE',  ( -8.311093377946836114, 258.5937500034140157, -8.311093377946836114 ) ) ;
#38867=CARTESIAN_POINT ( 'NONE',  ( -6.951808397369817780E-16, 222.6562500034139873, -11.35316468749999963 ) ) ;
#38889=DIRECTION ( 'NONE',  ( 0.000000000000000000, 0.000000000000000000, -1.000000000000000000 ) ) ;
#38918=CARTESIAN_POINT ( 'NONE',  ( -11.35316468749999963, 259.2187500034140157, 0.000000000000000000 ) ) ;
#38938=( BOUNDED_CURVE ( )  B_SPLINE_CURVE ( 2, ( #44258, #15936, #9174, #33323, #43875, #72922, #61232, #26892, #15197, #32193, #55584, #68003, #21232 ),
 .UNSPECIFIED., .F., .F. ) 
 B_SPLINE_CURVE_WITH_KNOTS ( ( 3, 2, 2, 2, 2, 2, 3 ),
 ( 0.3055555555555558023, 0.3148148148148149361, 0.3240740740740741255, 0.3333333333333332593, 0.3425925925925924487, 0.3518518518518516380, 0.3611111111111107719 ),
 .UNSPECIFIED. ) 
 CURVE ( )  GEOMETRIC_REPRESENTATION_ITEM ( )  RATIONAL_B_SPLINE_CURVE ( ( 0.9999999999999992228, 0.9659258262890690894, 1.000000000000000000, 0.9659258262890683122, 1.000000000000000000, 0.9659258262890683122, 1.000000000000000000, 0.9659258262890683122, 1.000000000000000000, 0.9659258262890683122, 1.000000000000000000, 0.9659258262890695335, 0.9999999999999987788 ) ) 
 REPRESENTATION_ITEM ( '' )  );
#38951=CARTESIAN_POINT ( 'NONE',  ( 3.042071309553173286, 255.3645833367473301, 11.35316468749999608 ) ) ;
#38970=EDGE_CURVE ( 'NONE', #23384, #41296, #69872, .T. ) ;
#39003=CARTESIAN_POINT ( 'NONE',  ( 4.999999999999997335, 248.3333333333333428, -8.660254037844387298 ) ) ;
#39011=CARTESIAN_POINT ( 'NONE',  ( 5.000000000000004441, 259.7916666734946034, 8.660254037844385522 ) ) ;
#39054=( BOUNDED_CURVE ( )  B_SPLINE_CURVE ( 2, ( #32810, #10155, #4135, #35048, #46342, #5250, #22577, #56934, #11643, #68611, #68242, #28620, #28250 ),
 .UNSPECIFIED., .F., .T. ) 
 B_SPLINE_CURVE_WITH_KNOTS ( ( 3, 2, 2, 2, 2, 2, 3 ),
 ( 0.6388888888888887285, 0.6481481481481480289, 0.6574074074074073293, 0.6666666666666665186, 0.6759259259259259300, 0.6851851851851852304, 0.6944444444444444198 ),
 .UNSPECIFIED. ) 
 CURVE ( )  GEOMETRIC_REPRESENTATION_ITEM ( )  RATIONAL_B_SPLINE_CURVE ( ( 1.000000000000000444, 0.9659258262890678681, 1.000000000000000000, 0.9659258262890683122, 1.000000000000000000, 0.9659258262890683122, 1.000000000000000000, 0.9659258262890683122, 1.000000000000000000, 0.9659258262890683122, 1.000000000000000000, 0.9659258262890683122, 1.000000000000000000 ) ) 
 REPRESENTATION_ITEM ( '' )  );
#39087=CARTESIAN_POINT ( 'NONE',  ( -9.832129032723418760, 258.4895833367473301, -5.676582343749998927 ) ) ;
#39121=CARTESIAN_POINT ( 'NONE',  ( -6.951808397369817780E-16, 252.9687500034140157, -11.35316468749999963 ) ) ;
#39148=CARTESIAN_POINT ( 'NONE',  ( 4.999999999999997335, 231.4583333401613174, -8.660254037844387298 ) ) ;
#39149=CARTESIAN_POINT ( 'NONE',  ( -7.320508075688771932, 252.5000000068279178, -7.320508075688771932 ) ) ;
#39170=CARTESIAN_POINT ( 'NONE',  ( -5.676582343749992710, 244.7395833367473301, 9.832129032723422313 ) ) ;
#39173=VERTEX_POINT ( 'NONE', #56626 ) ;
#39174=CARTESIAN_POINT ( 'NONE',  ( -9.832129032723415207, 249.6354166700806445, 5.676582343750005144 ) ) ;
#39199=CARTESIAN_POINT ( 'NONE',  ( -10.00000000000000000, 263.1250000068279746, 0.000000000000000000 ) ) ;
#39237=CARTESIAN_POINT ( 'NONE',  ( 11.35316468749999963, 221.4062500034139873, -1.390361679473963556E-15 ) ) ;
#39260=CARTESIAN_POINT ( 'NONE',  ( 2.679491924311283579, 223.5416666666666856, -9.999999999999969802 ) ) ;
#39287=CARTESIAN_POINT ( 'NONE',  ( 9.832129032723416984, 247.1354166700806445, -5.676582343750003368 ) ) ;
#39306=CARTESIAN_POINT ( 'NONE',  ( 10.00000000000000178, 227.2916666666666288, 2.679491924311222739 ) ) ;
#39324=CARTESIAN_POINT ( 'NONE',  ( 8.311093377946839666, 255.7812500034139589, 8.311093377946829008 ) ) ;
#39354=DIRECTION ( 'NONE',  ( -0.000000000000000000, -1.000000000000000000, -0.000000000000000000 ) ) ;
#39373=CARTESIAN_POINT ( 'NONE',  ( 10.00000000000000178, 232.2916666666666856, 2.679491924311222739 ) ) ;
#39402=CARTESIAN_POINT ( 'NONE',  ( 9.832129032723416984, 222.1354166700806729, -5.676582343750003368 ) ) ;
#39409=CARTESIAN_POINT ( 'NONE',  ( 4.999999999999997335, 248.3333333333333428, -8.660254037844387298 ) ) ;
#39437=ORIENTED_EDGE ( 'NONE', *, *, #2105, .F. ) ;
#39451=EDGE_CURVE ( 'NONE', #29199, #53500, #57918, .T. ) ;
#39454=ORIENTED_EDGE ( 'NONE', *, *, #65308, .T. ) ;
#39455=CARTESIAN_POINT ( 'NONE',  ( -11.35316468749999785, 253.6979166700807014, -3.042071309553164848 ) ) ;
#39461=( BOUNDED_CURVE ( )  B_SPLINE_CURVE ( 2, ( #28348, #68342, #22677, #17020, #40044, #34781, #50986, #39306, #63048, #27598, #5716, #80, #69087 ),
 .UNSPECIFIED., .F., .F. ) 
 B_SPLINE_CURVE_WITH_KNOTS ( ( 3, 2, 2, 2, 2, 2, 3 ),
 ( 0.8055555555555555802, 0.8148148148148147696, 0.8240740740740740700, 0.8333333333333333703, 0.8425925925925925597, 0.8518518518518518601, 0.8611111111111111605 ),
 .UNSPECIFIED. ) 
 CURVE ( )  GEOMETRIC_REPRESENTATION_ITEM ( )  RATIONAL_B_SPLINE_CURVE ( ( 1.000000000000000000, 0.9659258262890683122, 1.000000000000000000, 0.9659258262890683122, 1.000000000000000000, 0.9659258262890683122, 1.000000000000000000, 0.9659258262890683122, 1.000000000000000000, 0.9659258262890683122, 1.000000000000000000, 0.9659258262890683122, 1.000000000000000000 ) ) 
 REPRESENTATION_ITEM ( '' )  );
#39495=CARTESIAN_POINT ( 'NONE',  ( 11.35316468749999608, 251.9270833367473585, -3.042071309553167513 ) ) ;
#39498=CARTESIAN_POINT ( 'NONE',  ( -10.00000000000000000, 265.0000000000000000, 0.000000000000000000 ) ) ;
#39523=CARTESIAN_POINT ( 'NONE',  ( 8.660254037844385522, 221.0416666734946602, -5.000000000000003553 ) ) ;
#39545=DIRECTION ( 'NONE',  ( -0.000000000000000000, -1.000000000000000000, -0.000000000000000000 ) ) ;
#39548=CARTESIAN_POINT ( 'NONE',  ( -3.042071309553159075, 239.9479166700806729, 11.35316468749999963 ) ) ;
#39552=CARTESIAN_POINT ( 'NONE',  ( 5.676582343749997150, 247.5520833367473301, -9.832129032723418760 ) ) ;
#39609=CARTESIAN_POINT ( 'NONE',  ( 8.311093377946839666, 225.7812500034140157, 8.311093377946829008 ) ) ;
#39631=CARTESIAN_POINT ( 'NONE',  ( 8.660254037844385522, 222.9166666666666856, -5.000000000000003553 ) ) ;
#39646=CARTESIAN_POINT ( 'NONE',  ( -2.679491924311337314, 253.9583333333333997, -9.999999999999936051 ) ) ;
#39658=CARTESIAN_POINT ( 'NONE',  ( 11.35316468749999608, 246.9270833367472733, -3.042071309553167069 ) ) ;
#39689=CARTESIAN_POINT ( 'NONE',  ( -6.951808397369817780E-16, 262.6562500034140157, -11.35316468749999963 ) ) ;
#39738=CARTESIAN_POINT ( 'NONE',  ( -10.00000000000000000, 235.0000000000000284, 0.000000000000000000 ) ) ;
#39820=CARTESIAN_POINT ( 'NONE',  ( 1.836970198721029589E-15, 259.3750000068280315, 10.00000000000000000 ) ) ;
#39823=CARTESIAN_POINT ( 'NONE',  ( -8.311093377946834337, 249.5312500034139873, 8.311093377946837890 ) ) ;
#39826=CARTESIAN_POINT ( 'NONE',  ( -10.04313107478231260, 220.0000000000000284, 0.3202752235055294494 ) ) ;
#39855=ORIENTED_EDGE ( 'NONE', *, *, #27970, .F. ) ;
#39859=CARTESIAN_POINT ( 'NONE',  ( -8.311093377946836114, 243.5937500034139873, -8.311093377946836114 ) ) ;
#39914=CARTESIAN_POINT ( 'NONE',  ( 2.085542519210945334E-15, 250.1562500034140157, 11.35316468749999963 ) ) ;
#39919=CARTESIAN_POINT ( 'NONE',  ( -9.832129032723418760, 253.8020833367473017, -5.676582343749998927 ) ) ;
#39981=CARTESIAN_POINT ( 'NONE',  ( 10.00000000000000178, 260.4166666734946034, 2.679491924311222739 ) ) ;
#40018=CARTESIAN_POINT ( 'NONE',  ( -7.320508075688770155, 255.6250000000000000, 7.320508075688774596 ) ) ;
#40031=CARTESIAN_POINT ( 'NONE',  ( -9.832129032723415207, 239.6354166700806445, 5.676582343750005144 ) ) ;
#40044=CARTESIAN_POINT ( 'NONE',  ( 8.660254037844385522, 227.9166666666666856, -5.000000000000003553 ) ) ;
#40066=CARTESIAN_POINT ( 'NONE',  ( 11.35316468749999963, 256.4062500034140157, -1.390361679473963556E-15 ) ) ;
#40112=CARTESIAN_POINT ( 'NONE',  ( 10.00000000000000000, 237.5000000000000284, -1.224646799147353256E-15 ) ) ;
#40198=CARTESIAN_POINT ( 'NONE',  ( -8.311093377946834337, 244.5312500034139589, 8.311093377946837890 ) ) ;
#40201=CARTESIAN_POINT ( 'NONE',  ( -10.07107371533886386, 220.0000000000001705, 0.6428371030747326298 ) ) ;
#40232=CARTESIAN_POINT ( 'NONE',  ( -9.832129032723415207, 244.6354166700806445, 5.676582343750005144 ) ) ;
#40287=CARTESIAN_POINT ( 'NONE',  ( 9.832129032723420536, 240.9895833367473301, 5.676582343749996262 ) ) ;
#40291=CARTESIAN_POINT ( 'NONE',  ( 9.832129032723416984, 242.1354166700806445, -5.676582343750003368 ) ) ;
#40302=AXIS2_PLACEMENT_3D ( 'NONE', #49174, #48058, #8443 ) ;
#40348=CARTESIAN_POINT ( 'NONE',  ( -8.660254037844385522, 253.5416666734946602, 5.000000000000004441 ) ) ;
#40403=CARTESIAN_POINT ( 'NONE',  ( 11.35316468749999608, 241.9270833367473301, -3.042071309553167069 ) ) ;
#40437=CARTESIAN_POINT ( 'NONE',  ( -11.35316468749999608, 254.1145833367473585, 3.042071309553173730 ) ) ;
#40443=DIRECTION ( 'NONE',  ( -0.000000000000000000, 1.000000000000000000, -0.000000000000000000 ) ) ;
#40461=CARTESIAN_POINT ( 'NONE',  ( -5.000000000000000888, 262.2916666734946034, -8.660254037844387298 ) ) ;
#40486=CARTESIAN_POINT ( 'NONE',  ( -9.999999999999998224, 240.2083333333333144, 2.679491924311235618 ) ) ;
#40496=ORIENTED_EDGE ( 'NONE', *, *, #45264, .T. ) ;
#40571=CARTESIAN_POINT ( 'NONE',  ( 3.042071309553173286, 250.3645833367473301, 11.35316468749999608 ) ) ;
#40607=CARTESIAN_POINT ( 'NONE',  ( -11.35316468749999785, 249.0104166700806445, -3.042071309553164848 ) ) ;
#40651=ORIENTED_EDGE ( 'NONE', *, *, #38970, .F. ) ;
#40654=EDGE_CURVE ( 'NONE', #16856, #23729, #35850, .T. ) ;
#40660=CARTESIAN_POINT ( 'NONE',  ( -11.35316468749999785, 248.6979166700806445, -3.042071309553164848 ) ) ;
#40664=CARTESIAN_POINT ( 'NONE',  ( -8.311093377946836114, 233.5937500034139305, -8.311093377946836114 ) ) ;
#40719=CARTESIAN_POINT ( 'NONE',  ( 10.00000000000000000, 250.6250000068279746, -1.224646799147353256E-15 ) ) ;
#40769=CARTESIAN_POINT ( 'NONE',  ( -8.311093377946834337, 239.8437500034139873, 8.311093377946837890 ) ) ;
#40776=DIRECTION ( 'NONE',  ( 3.400485001760801611E-18, -0.9996144206527183274, 0.02776706724035331308 ) ) ;
#40805=CARTESIAN_POINT ( 'NONE',  ( -9.832129032723415207, 244.3229166700806445, 5.676582343750005144 ) ) ;
#40851=ORIENTED_EDGE ( 'NONE', *, *, #56695, .T. ) ;
#40859=CARTESIAN_POINT ( 'NONE',  ( -2.679491924311228512, 233.9583333333333712, -9.999999999999998224 ) ) ;
#40932=CARTESIAN_POINT ( 'NONE',  ( 10.00000000000000000, 250.6250000068279746, -1.224646799147353256E-15 ) ) ;
#40947=CARTESIAN_POINT ( 'NONE',  ( -3.042071309553159075, 249.9479166700806729, 11.35316468749999963 ) ) ;
#40977=CARTESIAN_POINT ( 'NONE',  ( -8.660254037844385522, 225.4166666666666856, 5.000000000000004441 ) ) ;
#40982=CARTESIAN_POINT ( 'NONE',  ( -3.042071309553159075, 240.2604166700806729, 11.35316468749999963 ) ) ;
#40986=VECTOR ( 'NONE', #63402, 1000.000000000000000 ) ;
#41006=ORIENTED_EDGE ( 'NONE', *, *, #18755, .T. ) ;
#41028=ORIENTED_EDGE ( 'NONE', *, *, #21100, .F. ) ;
#41038=CARTESIAN_POINT ( 'NONE',  ( -11.35316468749999963, 233.9062500034139873, 0.000000000000000000 ) ) ;
#41041=CARTESIAN_POINT ( 'NONE',  ( -3.042071309553166181, 238.1770833367473301, -11.35316468749999608 ) ) ;
#41095=CARTESIAN_POINT ( 'NONE',  ( -2.679491924311228512, 257.0833333401612890, -9.999999999999998224 ) ) ;
#41145=CARTESIAN_POINT ( 'NONE',  ( -4.999999999999992895, 250.8333333333333428, 8.660254037844390851 ) ) ;
#41147=CARTESIAN_POINT ( 'NONE',  ( -5.676582343749992710, 230.0520833367473017, 9.832129032723422313 ) ) ;
#41183=CARTESIAN_POINT ( 'NONE',  ( 5.676582343749997150, 247.2395833367473301, -9.832129032723418760 ) ) ;
#41232=CARTESIAN_POINT ( 'NONE',  ( -8.660254037844387298, 224.5833333333333712, -4.999999999999999112 ) ) ;
#41241=CARTESIAN_POINT ( 'NONE',  ( -10.00000000000000000, 227.9166666734946034, -2.679491924311226292 ) ) ;
#41272=CARTESIAN_POINT ( 'NONE',  ( 0.000000000000000000, 0.000000000000000000, -10.00000000000000000 ) ) ;
#41296=VERTEX_POINT ( 'NONE', #11735 ) ;
#41301=EDGE_CURVE ( 'NONE', #3433, #5951, #13195, .T. ) ;
#41315=VERTEX_POINT ( 'NONE', #52110 ) ;
#41317=CARTESIAN_POINT ( 'NONE',  ( 11.35316468749999963, 241.4062500034140157, -1.390361679473963556E-15 ) ) ;
#41344=CARTESIAN_POINT ( 'NONE',  ( -7.320508075688770155, 238.7500000068279462, 7.320508075688774596 ) ) ;
#41351=CARTESIAN_POINT ( 'NONE',  ( -9.832129032723415207, 239.6354166700806445, 5.676582343750005144 ) ) ;
#41381=CARTESIAN_POINT ( 'NONE',  ( -5.000000000000000888, 264.1666666666666856, -8.660254037844387298 ) ) ;
#41404=CARTESIAN_POINT ( 'NONE',  ( 8.311093377946839666, 230.7812500034139589, 8.311093377946830785 ) ) ;
#41409=CARTESIAN_POINT ( 'NONE',  ( 11.35316468749999608, 236.9270833367473017, -3.042071309553167069 ) ) ;
#41423=PLANE ( 'NONE',  #25123 ) ;
#41438=DIRECTION ( 'NONE',  ( -0.000000000000000000, -1.000000000000000000, -0.000000000000000000 ) ) ;
#41465=CARTESIAN_POINT ( 'NONE',  ( -10.00000000000000000, 252.9166666734946602, -2.679491924311226292 ) ) ;
#41509=CARTESIAN_POINT ( 'NONE',  ( -3.042071309553166181, 228.1770833367473301, -11.35316468749999608 ) ) ;
#41546=CARTESIAN_POINT ( 'NONE',  ( -11.35316468749999785, 243.6979166700806445, -3.042071309553164848 ) ) ;
#41570=ORIENTED_EDGE ( 'NONE', *, *, #48376, .F. ) ;
#41598=CARTESIAN_POINT ( 'NONE',  ( -10.00000000000000000, 220.0000000000000000, 0.000000000000000000 ) ) ;
#41606=CARTESIAN_POINT ( 'NONE',  ( -7.320508075688771932, 227.5000000068279462, -7.320508075688771932 ) ) ;
#41683=CARTESIAN_POINT ( 'NONE',  ( -8.311093377946834337, 234.5312500034139589, 8.311093377946837890 ) ) ;
#41688=CARTESIAN_POINT ( 'NONE',  ( 2.679491924311235174, 261.4583333333332575, 9.999999999999998224 ) ) ;
#41716=CARTESIAN_POINT ( 'NONE',  ( 9.832129032723420536, 236.3020833367473301, 5.676582343749996262 ) ) ;
#41768=CARTESIAN_POINT ( 'NONE',  ( -8.311093377946834337, 229.5312500034139589, 8.311093377946837890 ) ) ;
#41772=CARTESIAN_POINT ( 'NONE',  ( 2.085542519210945334E-15, 225.4687500034139873, 11.35316468749999963 ) ) ;
#41800=CARTESIAN_POINT ( 'NONE',  ( 0.000000000000000000, 0.000000000000000000, -19.00000000000001776 ) ) ;
#41826=CARTESIAN_POINT ( 'NONE',  ( -7.320508075688770155, 258.7500000068279746, 7.320508075688774596 ) ) ;
#41835=EDGE_CURVE ( 'NONE', #39173, #23384, #56583, .T. ) ;
#41873=CARTESIAN_POINT ( 'NONE',  ( -5.676582343750000703, 223.3854166700806729, -9.832129032723418760 ) ) ;
#41898=DIRECTION ( 'NONE',  ( -0.000000000000000000, -1.000000000000000000, -0.000000000000000000 ) ) ;
#41910=CARTESIAN_POINT ( 'NONE',  ( -8.311093377946836114, 243.2812500034139589, -8.311093377946836114 ) ) ;
#41943=CARTESIAN_POINT ( 'NONE',  ( 1.836970198721029589E-15, 221.2500000000000000, 10.00000000000000178 ) ) ;
#41956=CARTESIAN_POINT ( 'NONE',  ( -3.042071309553166181, 263.1770833367473301, -11.35316468749999608 ) ) ;
#42040=CARTESIAN_POINT ( 'NONE',  ( -5.676582343750000703, 238.0729166700806445, -9.832129032723418760 ) ) ;
#42066=CARTESIAN_POINT ( 'NONE',  ( -2.679491924311165008, 239.1666666734946602, 10.00000000000003553 ) ) ;
#42071=CARTESIAN_POINT ( 'NONE',  ( 3.042071309553173286, 225.6770833367473017, 11.35316468749999608 ) ) ;
#42103=ADVANCED_FACE ( 'NONE', ( #37538 ), #3961, .F. ) ;
#42123=CARTESIAN_POINT ( 'NONE',  ( 11.35316468749999963, 226.1979166700806445, 3.042071309553159519 ) ) ;
#42127=CARTESIAN_POINT ( 'NONE',  ( 11.35316468749999608, 221.9270833367473017, -3.042071309553167069 ) ) ;
#42158=CARTESIAN_POINT ( 'NONE',  ( 5.000000000000004441, 231.6666666666666856, 8.660254037844385522 ) ) ;
#42183=CARTESIAN_POINT ( 'NONE',  ( 8.660254037844385522, 236.0416666734946318, -5.000000000000003553 ) ) ;
#42192=AXIS2_PLACEMENT_3D ( 'NONE', #68719, #58172, #73639 ) ;
#42212=CARTESIAN_POINT ( 'NONE',  ( -3.042071309553159075, 260.2604166700805877, 11.35316468749999963 ) ) ;
#42236=CARTESIAN_POINT ( 'NONE',  ( 11.35316468749999963, 231.5104166700806445, 3.042071309553159519 ) ) ;
#42237=CARTESIAN_POINT ( 'NONE',  ( -6.123233995736766282E-16, 233.7500000000000000, -10.00000000000000000 ) ) ;
#42276=CARTESIAN_POINT ( 'NONE',  ( 9.832129032723416984, 236.8229166700806445, -5.676582343750003368 ) ) ;
#42322=CARTESIAN_POINT ( 'NONE',  ( 10.00000000000000178, 222.2916666666666856, 2.679491924311222739 ) ) ;
#42356=CARTESIAN_POINT ( 'NONE',  ( -11.35316468749999963, 219.2187500034139873, 0.000000000000000000 ) ) ;
#42378=CARTESIAN_POINT ( 'NONE',  ( 0.6686838642329748783, 220.0000000000000284, 10.97965672913483814 ) ) ;
#42396=ORIENTED_EDGE ( 'NONE', *, *, #41301, .T. ) ;
#42406=CARTESIAN_POINT ( 'NONE',  ( -11.35316468749999785, 233.6979166700806161, -3.042071309553164848 ) ) ;
#42423=EDGE_CURVE ( 'NONE', #6283, #66955, #55156, .T. ) ;
#42441=CARTESIAN_POINT ( 'NONE',  ( 2.085542519210945334E-15, 230.4687500034139873, 11.35316468749999963 ) ) ;
#42452=ADVANCED_FACE ( 'NONE', ( #66078 ), #56269, .F. ) ;
#42468=CARTESIAN_POINT ( 'NONE',  ( 10.00000000000000000, 245.6250000068279746, -1.224646799147353256E-15 ) ) ;
#42476=ADVANCED_FACE ( 'NONE', ( #20804 ), #16677, .F. ) ;
#42482=ORIENTED_EDGE ( 'NONE', *, *, #1965, .F. ) ;
#42493=AXIS2_PLACEMENT_3D ( 'NONE', #21692, #44718, #61698 ) ;
#42498=CARTESIAN_POINT ( 'NONE',  ( -6.951808397369817780E-16, 237.6562500034140157, -11.35316468749999963 ) ) ;
#42501=CARTESIAN_POINT ( 'NONE',  ( 5.676582343750005144, 220.8854166700806445, 9.832129032723416984 ) ) ;
#42562=CARTESIAN_POINT ( 'NONE',  ( -10.00000000000000000, 233.1250000068279746, 0.000000000000000000 ) ) ;
#42581=CARTESIAN_POINT ( 'NONE',  ( 1.224646799147353256E-15, 0.000000000000000000, 10.00000000000000000 ) ) ;
#42618=DIRECTION ( 'NONE',  ( 0.000000000000000000, 0.000000000000000000, -1.000000000000000000 ) ) ;
#42646=CARTESIAN_POINT ( 'NONE',  ( 9.832129032723420536, 235.9895833367473301, 5.676582343749996262 ) ) ;
#42682=DIRECTION ( 'NONE',  ( 0.000000000000000000, 0.000000000000000000, -1.000000000000000000 ) ) ;
#42692=CARTESIAN_POINT ( 'NONE',  ( -8.660254037844385522, 225.4166666666666856, 5.000000000000004441 ) ) ;
#42713=CARTESIAN_POINT ( 'NONE',  ( -7.320508075688770155, 230.6250000000000284, 7.320508075688774596 ) ) ;
#42716=EDGE_CURVE ( 'NONE', #27344, #16846, #69696, .T. ) ;
#42777=CARTESIAN_POINT ( 'NONE',  ( -8.311093377946836114, 233.2812500034139589, -8.311093377946836114 ) ) ;
#42781=CARTESIAN_POINT ( 'NONE',  ( -5.000000000000000888, 259.1666666666666288, -8.660254037844387298 ) ) ;
#42806=CARTESIAN_POINT ( 'NONE',  ( 8.660254037844389075, 220.2083333401613174, 4.999999999999997335 ) ) ;
#42808=CARTESIAN_POINT ( 'NONE',  ( -9.832129032723415207, 234.6354166700806445, 5.676582343750005144 ) ) ;
#42860=CARTESIAN_POINT ( 'NONE',  ( -5.676582343750000703, 223.0729166700806729, -9.832129032723418760 ) ) ;
#42864=CARTESIAN_POINT ( 'NONE',  ( -11.35316468749999963, 224.2187500034139873, 0.000000000000000000 ) ) ;
#42895=CARTESIAN_POINT ( 'NONE',  ( 0.000000000000000000, 0.000000000000000000, -10.00000000000000000 ) ) ;
#42912=EDGE_CURVE ( 'NONE', #50547, #14535, #18456, .T. ) ;
#42925=CARTESIAN_POINT ( 'NONE',  ( -10.00000000000000000, 242.9166666734946318, -2.679491924311226292 ) ) ;
#42946=CARTESIAN_POINT ( 'NONE',  ( -11.35316468749999963, 263.9062500034140157, 0.000000000000000000 ) ) ;
#43011=CARTESIAN_POINT ( 'NONE',  ( -6.951808397369817780E-16, 232.6562500034139873, -11.35316468749999963 ) ) ;
#43037=SHAPE_REPRESENTATION_RELATIONSHIP ( 'NONE' , 'NONE' ,  #4585, #47122 ) ;
#43063=CARTESIAN_POINT ( 'NONE',  ( -8.311093377946834337, 254.8437500034139873, 8.311093377946837890 ) ) ;
#43150=CARTESIAN_POINT ( 'NONE',  ( 9.832129032723416984, 226.8229166700806729, -5.676582343750003368 ) ) ;
#43156=CARTESIAN_POINT ( 'NONE',  ( -10.00000000000000000, 250.0000000000000000, 0.000000000000000000 ) ) ;
#43163=CARTESIAN_POINT ( 'NONE',  ( 7.320508075688771044, 261.2500000068279178, -7.320508075688771932 ) ) ;
#43185=CARTESIAN_POINT ( 'NONE',  ( -3.042071309553159075, 235.2604166700806161, 11.35316468749999963 ) ) ;
#43198=CARTESIAN_POINT ( 'NONE',  ( 9.999999999999998224, 257.7083333333333712, -2.679491924311229401 ) ) ;
#43242=CARTESIAN_POINT ( 'NONE',  ( -3.042071309553159075, 230.2604166700806445, 11.35316468749999963 ) ) ;
#43277=CARTESIAN_POINT ( 'NONE',  ( 7.320508075688776373, 231.8750000000000000, 7.320508075688767491 ) ) ;
#43305=CARTESIAN_POINT ( 'NONE',  ( -4.999999999999992895, 233.9583333401613174, 8.660254037844390851 ) ) ;
#43324=CARTESIAN_POINT ( 'NONE',  ( 11.35316468749999963, 256.4062500034140157, -1.390361679473963556E-15 ) ) ;
#43327=CARTESIAN_POINT ( 'NONE',  ( 11.35316468749999608, 261.9270833367472733, -3.042071309553167069 ) ) ;
#43379=ORIENTED_EDGE ( 'NONE', *, *, #1017, .T. ) ;
#43389=CARTESIAN_POINT ( 'NONE',  ( -8.311093377946836114, 233.2812500034139589, -8.311093377946836114 ) ) ;
#43392=VERTEX_POINT ( 'NONE', #39199 ) ;
#43413=CARTESIAN_POINT ( 'NONE',  ( 8.660254037844385522, 236.0416666734946318, -5.000000000000003553 ) ) ;
#43438=DIRECTION ( 'NONE',  ( -0.000000000000000000, -1.000000000000000000, -0.000000000000000000 ) ) ;
#43439=CARTESIAN_POINT ( 'NONE',  ( 11.35316468749999608, 261.9270833367472733, -3.042071309553167069 ) ) ;
#43484=CARTESIAN_POINT ( 'NONE',  ( 10.00000000000000000, 230.6250000068279746, -1.224646799147353256E-15 ) ) ;
#43521=CARTESIAN_POINT ( 'NONE',  ( -9.832129032723418760, 223.4895833367473301, -5.676582343749998927 ) ) ;
#43526=CARTESIAN_POINT ( 'NONE',  ( -10.00000000000000000, 249.7916666666666572, -2.679491924311226292 ) ) ;
#43581=EDGE_LOOP ( 'NONE', ( #56866, #30061, #44403, #73395 ) ) ;
#43618=CARTESIAN_POINT ( 'NONE',  ( -5.676582343750000703, 253.0729166700807014, -9.832129032723418760 ) ) ;
#43650=ORIENTED_EDGE ( 'NONE', *, *, #58161, .F. ) ;
#43684=CARTESIAN_POINT ( 'NONE',  ( 10.00000000000000178, 245.4166666734946318, 2.679491924311222739 ) ) ;
#43706=CARTESIAN_POINT ( 'NONE',  ( -11.35316468749999963, 253.9062500034139873, 0.000000000000000000 ) ) ;
#43729=CARTESIAN_POINT ( 'NONE',  ( -2.679491924311287132, 242.0833333401613174, -9.999999999999968026 ) ) ;
#43748=CARTESIAN_POINT ( 'NONE',  ( -7.320508075688770155, 260.6249999999999432, 7.320508075688774596 ) ) ;
#43770=CARTESIAN_POINT ( 'NONE',  ( -11.35316468749999963, 228.9062500034139873, 0.000000000000000000 ) ) ;
#43800=( NAMED_UNIT ( * ) PLANE_ANGLE_UNIT ( ) SI_UNIT ( $, .RADIAN. ) );
#43825=CARTESIAN_POINT ( 'NONE',  ( -11.35316468749999608, 259.4270833367472164, 3.042071309553173730 ) ) ;
#43854=CARTESIAN_POINT ( 'NONE',  ( 0.000000000000000000, 220.0000000000000284, -10.00000000000000000 ) ) ;
#43867=CARTESIAN_POINT ( 'NONE',  ( 8.660254037844385522, 231.0416666734946318, -5.000000000000003553 ) ) ;
#43875=CARTESIAN_POINT ( 'NONE',  ( -8.660254037844385522, 248.5416666734946318, 5.000000000000004441 ) ) ;
#43902=VECTOR ( 'NONE', #153, 1000.000000000000000 ) ;
#43914=CARTESIAN_POINT ( 'NONE',  ( -7.320508075688770155, 255.6250000000000000, 7.320508075688774596 ) ) ;
#43944=CARTESIAN_POINT ( 'NONE',  ( -5.676582343750000703, 223.3854166700806729, -9.832129032723418760 ) ) ;
#43997=CARTESIAN_POINT ( 'NONE',  ( -11.35316468749999785, 223.6979166700806445, -3.042071309553164848 ) ) ;
#43999=ORIENTED_EDGE ( 'NONE', *, *, #20196, .F. ) ;
#44002=CARTESIAN_POINT ( 'NONE',  ( -3.042071309553166181, 252.8645833367473301, -11.35316468749999608 ) ) ;
#44037=CARTESIAN_POINT ( 'NONE',  ( -11.35316468749999608, 254.4270833367473585, 3.042071309553173730 ) ) ;
#44064=CARTESIAN_POINT ( 'NONE',  ( 10.00000000000000178, 230.4166666734946034, 2.679491924311222739 ) ) ;
#44066=ORIENTED_EDGE ( 'NONE', *, *, #38970, .T. ) ;
#44081=PRODUCT_DEFINITION ( 'UNKNOWN', '', #22532, #62901 ) ;
#44082=FACE_OUTER_BOUND ( 'NONE', #52049, .T. ) ;
#44087=CARTESIAN_POINT ( 'NONE',  ( 11.35316468749999963, 261.1979166700807014, 3.042071309553159519 ) ) ;
#44092=CARTESIAN_POINT ( 'NONE',  ( -8.311093377946836114, 253.5937500034140157, -8.311093377946836114 ) ) ;
#44149=CARTESIAN_POINT ( 'NONE',  ( -11.35316468749999608, 219.1145833367473017, 3.042071309553173730 ) ) ;
#44176=CARTESIAN_POINT ( 'NONE',  ( 7.320508075688771044, 236.2500000068279746, -7.320508075688771932 ) ) ;
#44177=( NAMED_UNIT ( * ) SI_UNIT ( $, .STERADIAN. ) SOLID_ANGLE_UNIT ( ) );
#44201=CARTESIAN_POINT ( 'NONE',  ( -11.00000000000000000, 0.000000000000000000, 0.000000000000000000 ) ) ;
#44203=CARTESIAN_POINT ( 'NONE',  ( -11.35316468749999785, 259.0104166700807014, -3.042071309553164848 ) ) ;
#44258=CARTESIAN_POINT ( 'NONE',  ( 1.836970198721029589E-15, 249.3750000068279746, 10.00000000000000000 ) ) ;
#44284=CARTESIAN_POINT ( 'NONE',  ( 5.676582343750005144, 220.5729166700806729, 9.832129032723416984 ) ) ;
#44289=CARTESIAN_POINT ( 'NONE',  ( 9.999999999999998224, 247.7083333333333428, -2.679491924311229401 ) ) ;
#44332=CARTESIAN_POINT ( 'NONE',  ( 7.320508075688776373, 256.8750000000000000, 7.320508075688767491 ) ) ;
#44366=AXIS2_PLACEMENT_3D ( 'NONE', #70140, #35804, #6761 ) ;
#44374=CARTESIAN_POINT ( 'NONE',  ( -5.676582343750000703, 263.0729166700806445, -9.832129032723418760 ) ) ;
#44381=CARTESIAN_POINT ( 'NONE',  ( -8.052558883257647793, 219.3273502760175973, 8.052558883257653122 ) ) ;
#44403=ORIENTED_EDGE ( 'NONE', *, *, #21981, .T. ) ;
#44406=CARTESIAN_POINT ( 'NONE',  ( 1.836970198721029589E-15, 256.2500000000000568, 10.00000000000000000 ) ) ;
#44407=CARTESIAN_POINT ( 'NONE',  ( 8.311093377946834337, 257.3437500034139589, -8.311093377946836114 ) ) ;
#44434=CARTESIAN_POINT ( 'NONE',  ( -2.679491924311228512, 232.0833333401613174, -9.999999999999998224 ) ) ;
#44458=CARTESIAN_POINT ( 'NONE',  ( 3.042071309553163516, 257.4479166700806445, -11.35316468749999785 ) ) ;
#44462=CARTESIAN_POINT ( 'NONE',  ( -11.35316468749999963, 259.2187500034140157, 0.000000000000000000 ) ) ;
#44500=CARTESIAN_POINT ( 'NONE',  ( -5.000000000000000888, 259.1666666666666288, -8.660254037844387298 ) ) ;
#44501=CARTESIAN_POINT ( 'NONE',  ( -5.000000000000000888, 244.1666666666666572, -8.660254037844387298 ) ) ;
#44513=VERTEX_POINT ( 'NONE', #60645 ) ;
#44521=CARTESIAN_POINT ( 'NONE',  ( -5.000000000000000888, 262.2916666734946034, -8.660254037844387298 ) ) ;
#44577=CARTESIAN_POINT ( 'NONE',  ( -11.35316468749999608, 254.4270833367473585, 3.042071309553173730 ) ) ;
#44610=CARTESIAN_POINT ( 'NONE',  ( -8.311093377946836114, 258.2812500034140157, -8.311093377946836114 ) ) ;
#44662=CARTESIAN_POINT ( 'NONE',  ( -10.00000000000000000, 254.7916666666666856, -2.679491924311226292 ) ) ;
#44673=ORIENTED_EDGE ( 'NONE', *, *, #65308, .F. ) ;
#44690=CARTESIAN_POINT ( 'NONE',  ( -8.311093377946836114, 223.5937500034139589, -8.311093377946836114 ) ) ;
#44718=DIRECTION ( 'NONE',  ( -0.000000000000000000, -1.000000000000000000, -0.000000000000000000 ) ) ;
#44746=CARTESIAN_POINT ( 'NONE',  ( 5.676582343750005144, 255.5729166700806445, 9.832129032723416984 ) ) ;
#44780=CARTESIAN_POINT ( 'NONE',  ( -10.00000000000000000, 222.9166666734946318, -2.679491924311226292 ) ) ;
#44781=CARTESIAN_POINT ( 'NONE',  ( -9.832129032723415207, 259.6354166700806445, 5.676582343750005144 ) ) ;
#44806=CARTESIAN_POINT ( 'NONE',  ( 4.999999999999997335, 226.4583333401612890, -8.660254037844387298 ) ) ;
#44831=CARTESIAN_POINT ( 'NONE',  ( 8.311093377946839666, 245.7812500034139589, 8.311093377946830785 ) ) ;
#44837=CARTESIAN_POINT ( 'NONE',  ( 5.676582343750005144, 250.8854166700806729, 9.832129032723416984 ) ) ;
#44876=CARTESIAN_POINT ( 'NONE',  ( -2.679491924311287132, 243.9583333333333712, -9.999999999999968026 ) ) ;
#44898=CARTESIAN_POINT ( 'NONE',  ( 9.999999999999998224, 260.8333333401612890, -2.679491924311229401 ) ) ;
#44931=CARTESIAN_POINT ( 'NONE',  ( -8.967304722683161700, 219.9183361721456720, 6.468172613360420264 ) ) ;
#44942=EDGE_CURVE ( 'NONE', #11938, #33033, #63768, .T. ) ;
#44949=CARTESIAN_POINT ( 'NONE',  ( 5.676582343750005144, 245.8854166700806445, 9.832129032723416984 ) ) ;
#45030=CARTESIAN_POINT ( 'NONE',  ( -9.832129032723415207, 219.3229166700806729, 5.676582343750005144 ) ) ;
#45036=CARTESIAN_POINT ( 'NONE',  ( -6.123233995736766282E-16, 233.7500000000000000, -10.00000000000000000 ) ) ;
#45114=CARTESIAN_POINT ( 'NONE',  ( 11.35316468749999963, 261.1979166700807014, 3.042071309553159519 ) ) ;
#45134=CARTESIAN_POINT ( 'NONE',  ( 11.35316468749999608, 221.9270833367473017, -3.042071309553167069 ) ) ;
#45149=CARTESIAN_POINT ( 'NONE',  ( 8.311093377946834337, 252.3437500034139589, -8.311093377946836114 ) ) ;
#45177=CARTESIAN_POINT ( 'NONE',  ( -6.123233995736766282E-16, 231.8750000068279746, -10.00000000000000000 ) ) ;
#45200=CARTESIAN_POINT ( 'NONE',  ( -8.311093377946836114, 248.2812500034139589, -8.311093377946836114 ) ) ;
#45204=CARTESIAN_POINT ( 'NONE',  ( 3.042071309553173286, 255.6770833367473301, 11.35316468749999608 ) ) ;
#45251=CARTESIAN_POINT ( 'NONE',  ( 2.020667218593132706E-15, 219.9523502760175973, 11.00000000000000000 ) ) ;
#45264=EDGE_CURVE ( 'NONE', #14535, #55545, #6553, .T. ) ;
#45266=CARTESIAN_POINT ( 'NONE',  ( -3.042071309553166181, 227.8645833367473301, -11.35316468749999608 ) ) ;
#45311=CARTESIAN_POINT ( 'NONE',  ( 8.311093377946834337, 242.3437500034139873, -8.311093377946836114 ) ) ;
#45344=CARTESIAN_POINT ( 'NONE',  ( 4.999999999999997335, 226.4583333401612890, -8.660254037844387298 ) ) ;
#45346=FACE_OUTER_BOUND ( 'NONE', #15099, .T. ) ;
#45348=ORIENTED_EDGE ( 'NONE', *, *, #61106, .F. ) ;
#45380=CARTESIAN_POINT ( 'NONE',  ( 1.836970198721029589E-15, 231.2500000000000000, 10.00000000000000000 ) ) ;
#45392=CARTESIAN_POINT ( 'NONE',  ( 2.679491924311225848, 238.5416666666666288, -10.00000000000000000 ) ) ;
#45436=DIRECTION ( 'NONE',  ( -0.000000000000000000, -1.000000000000000000, -0.000000000000000000 ) ) ;
#45476=CARTESIAN_POINT ( 'NONE',  ( -8.311093377946836114, 243.2812500034139589, -8.311093377946836114 ) ) ;
#45479=CARTESIAN_POINT ( 'NONE',  ( -9.300015335314476772, 220.0000000000000000, 5.337650171418015788 ) ) ;
#45513=CARTESIAN_POINT ( 'NONE',  ( -9.832129032723418760, 258.8020833367473301, -5.676582343749998927 ) ) ;
#45541=CARTESIAN_POINT ( 'NONE',  ( -10.00000000000000000, 227.9166666734946034, -2.679491924311226292 ) ) ;
#45557=AXIS2_PLACEMENT_3D ( 'NONE', #72983, #60538, #8864 ) ;
#45569=CARTESIAN_POINT ( 'NONE',  ( -9.832129032723415207, 244.3229166700806445, 5.676582343750005144 ) ) ;
#45574=CARTESIAN_POINT ( 'NONE',  ( 5.676582343749997150, 252.5520833367473301, -9.832129032723418760 ) ) ;
#45615=CARTESIAN_POINT ( 'NONE',  ( 0.000000000000000000, 45.00000000000000000, 0.000000000000000000 ) ) ;
#45633=CARTESIAN_POINT ( 'NONE',  ( -5.676582343750000703, 223.0729166700806729, -9.832129032723418760 ) ) ;
#45680=CARTESIAN_POINT ( 'NONE',  ( 3.042071309553173286, 240.6770833367473301, 11.35316468749999608 ) ) ;
#45717=CARTESIAN_POINT ( 'NONE',  ( 9.832129032723416984, 256.8229166700806445, -5.676582343750003368 ) ) ;
#45754=FACE_OUTER_BOUND ( 'NONE', #68604, .T. ) ;
#45769=CARTESIAN_POINT ( 'NONE',  ( 10.00000000000000000, 242.5000000000000284, -1.224646799147353256E-15 ) ) ;
#45783=EDGE_CURVE ( 'NONE', #66887, #6411, #47946, .T. ) ;
#45833=ORIENTED_EDGE ( 'NONE', *, *, #21416, .T. ) ;
#45851=CARTESIAN_POINT ( 'NONE',  ( -9.832129032723418760, 243.4895833367473301, -5.676582343749998927 ) ) ;
#45854=CARTESIAN_POINT ( 'NONE',  ( -8.892166665161244765, 220.0000000000000284, 6.204661273877360550 ) ) ;
#45882=CARTESIAN_POINT ( 'NONE',  ( -4.999999999999992895, 225.8333333333333428, 8.660254037844390851 ) ) ;
#45889=CARTESIAN_POINT ( 'NONE',  ( -6.951808397369817780E-16, 237.9687500034139873, -11.35316468749999963 ) ) ;
#45891=ORIENTED_EDGE ( 'NONE', *, *, #21763, .T. ) ;
#45945=CARTESIAN_POINT ( 'NONE',  ( -11.35316468749999608, 249.1145833367473017, 3.042071309553173730 ) ) ;
#45948=CARTESIAN_POINT ( 'NONE',  ( 3.042071309553173286, 245.6770833367473017, 11.35316468749999608 ) ) ;
#45950=ORIENTED_EDGE ( 'NONE', *, *, #29161, .F. ) ;
#45958=ORIENTED_EDGE ( 'NONE', *, *, #10394, .T. ) ;
#45979=CARTESIAN_POINT ( 'NONE',  ( 0.000000000000000000, 0.000000000000000000, 0.000000000000000000 ) ) ;
#46005=CARTESIAN_POINT ( 'NONE',  ( -10.00000000000000000, 248.1250000068279746, 0.000000000000000000 ) ) ;
#46054=CARTESIAN_POINT ( 'NONE',  ( -11.35316468749999963, 244.2187500034140157, 0.000000000000000000 ) ) ;
#46061=CARTESIAN_POINT ( 'NONE',  ( -9.999999999999998224, 240.2083333333333144, 2.679491924311235174 ) ) ;
#46088=CARTESIAN_POINT ( 'NONE',  ( -9.832129032723415207, 254.3229166700806729, 5.676582343750005144 ) ) ;
#46115=CARTESIAN_POINT ( 'NONE',  ( -10.00000000000000000, 263.1250000068279746, 0.000000000000000000 ) ) ;
#46123=ORIENTED_EDGE ( 'NONE', *, *, #58161, .T. ) ;
#46140=CARTESIAN_POINT ( 'NONE',  ( -7.320508075688770155, 235.6250000000000000, 7.320508075688774596 ) ) ;
#46227=CARTESIAN_POINT ( 'NONE',  ( 5.676582343750005144, 250.5729166700807014, 9.832129032723416984 ) ) ;
#46235=LINE ( 'NONE', #22848, #38788 ) ;
#46247=AXIS2_PLACEMENT_3D ( 'NONE', #63552, #28107, #29233 ) ;
#46259=CARTESIAN_POINT ( 'NONE',  ( 9.832129032723416984, 247.1354166700806445, -5.676582343750003368 ) ) ;
#46305=VERTEX_POINT ( 'NONE', #19396 ) ;
#46316=CARTESIAN_POINT ( 'NONE',  ( -9.832129032723415207, 239.3229166700806445, 5.676582343750005144 ) ) ;
#46320=CARTESIAN_POINT ( 'NONE',  ( 11.35316468749999963, 246.5104166700806161, 3.042071309553159519 ) ) ;
#46331=VERTEX_POINT ( 'NONE', #38639 ) ;
#46342=CARTESIAN_POINT ( 'NONE',  ( -8.660254037844385522, 235.4166666666666572, 5.000000000000004441 ) ) ;
#46378=CARTESIAN_POINT ( 'NONE',  ( 8.660254037844389075, 255.2083333401612890, 4.999999999999997335 ) ) ;
#46429=CARTESIAN_POINT ( 'NONE',  ( -6.951808397369817780E-16, 247.9687500034140157, -11.35316468749999963 ) ) ;
#46462=CARTESIAN_POINT ( 'NONE',  ( 2.085542519210945334E-15, 245.1562500034140157, 11.35316468749999963 ) ) ;
#46506=CARTESIAN_POINT ( 'NONE',  ( 7.320508075688776373, 251.8750000000000284, 7.320508075688767491 ) ) ;
#46512=CARTESIAN_POINT ( 'NONE',  ( 4.999999999999997335, 238.3333333333333428, -8.660254037844387298 ) ) ;
#46574=UNCERTAINTY_MEASURE_WITH_UNIT (LENGTH_MEASURE( 1.000000000000000082E-05 ), #67017, 'distance_accuracy_value', 'NONE');
#46595=CARTESIAN_POINT ( 'NONE',  ( 8.311093377946839666, 240.7812500034140157, 8.311093377946829008 ) ) ;
#46631=CARTESIAN_POINT ( 'NONE',  ( 5.676582343750005144, 250.8854166700806729, 9.832129032723416984 ) ) ;
#46660=CARTESIAN_POINT ( 'NONE',  ( -4.999999999999992895, 218.9583333401613174, 8.660254037844390851 ) ) ;
#46670=ORIENTED_EDGE ( 'NONE', *, *, #7694, .F. ) ;
#46674=CARTESIAN_POINT ( 'NONE',  ( 0.000000000000000000, 0.000000000000000000, 0.000000000000000000 ) ) ;
#46683=CARTESIAN_POINT ( 'NONE',  ( 9.832129032723416984, 231.8229166700806445, -5.676582343750003368 ) ) ;
#46687=CARTESIAN_POINT ( 'NONE',  ( 2.085542519210945334E-15, 245.4687500034140157, 11.35316468749999963 ) ) ;
#46742=CARTESIAN_POINT ( 'NONE',  ( -2.679491924311228512, 252.0833333401612606, -9.999999999999998224 ) ) ;
#46784=CARTESIAN_POINT ( 'NONE',  ( -10.00000000000000000, 232.9166666734946318, -2.679491924311226292 ) ) ;
#46793=CARTESIAN_POINT ( 'NONE',  ( 8.311093377946834337, 227.3437500034140157, -8.311093377946836114 ) ) ;
#46794=CARTESIAN_POINT ( 'NONE',  ( 0.000000000000000000, 0.000000000000000000, -10.00000000000000000 ) ) ;
#46830=CARTESIAN_POINT ( 'NONE',  ( -6.951808397369817780E-16, 242.6562500034140157, -11.35316468749999963 ) ) ;
#46884=CARTESIAN_POINT ( 'NONE',  ( 7.320508075688776373, 221.8750000000000284, 7.320508075688767491 ) ) ;
#46910=ORIENTED_EDGE ( 'NONE', *, *, #19012, .T. ) ;
#46949=CARTESIAN_POINT ( 'NONE',  ( 9.999999999999998224, 250.8333333401613459, -2.679491924311229401 ) ) ;
#46964=CARTESIAN_POINT ( 'NONE',  ( -11.35316468749999608, 249.1145833367473017, 3.042071309553173730 ) ) ;
#46996=CARTESIAN_POINT ( 'NONE',  ( 5.676582343749997150, 242.5520833367473301, -9.832129032723418760 ) ) ;
#47000=VECTOR ( 'NONE', #618, 1000.000000000000000 ) ;
#47044=AXIS2_PLACEMENT_3D ( 'NONE', #53218, #24888, #42618 ) ;
#47050=CARTESIAN_POINT ( 'NONE',  ( 2.085542519210945334E-15, 235.1562500034140157, 11.35316468749999963 ) ) ;
#47053=CARTESIAN_POINT ( 'NONE',  ( 3.042071309553173286, 235.6770833367473017, 11.35316468749999608 ) ) ;
#47107=CARTESIAN_POINT ( 'NONE',  ( -4.999999999999992895, 253.9583333401613174, 8.660254037844390851 ) ) ;
#47121=ADVANCED_FACE ( 'NONE', ( #54122 ), #71075, .T. ) ;
#47122=ADVANCED_BREP_SHAPE_REPRESENTATION ( '', ( #66799, #57354 ), #47738 ) ;
#47159=CARTESIAN_POINT ( 'NONE',  ( -9.832129032723415207, 229.6354166700806729, 5.676582343750005144 ) ) ;
#47199=CARTESIAN_POINT ( 'NONE',  ( -8.311093377946834337, 249.5312500034139873, 8.311093377946837890 ) ) ;
#47248=CARTESIAN_POINT ( 'NONE',  ( -7.320508075688771932, 229.3749999999999716, -7.320508075688771932 ) ) ;
#47272=CARTESIAN_POINT ( 'NONE',  ( 0.000000000000000000, 0.000000000000000000, 0.000000000000000000 ) ) ;
#47274=DIRECTION ( 'NONE',  ( -0.000000000000000000, -1.000000000000000000, -0.000000000000000000 ) ) ;
#47324=ORIENTED_EDGE ( 'NONE', *, *, #5284, .T. ) ;
#47325=CARTESIAN_POINT ( 'NONE',  ( 4.999999999999997335, 256.4583333401613459, -8.660254037844387298 ) ) ;
#47334=CARTESIAN_POINT ( 'NONE',  ( 8.311093377946834337, 237.0312500034140157, -8.311093377946836114 ) ) ;
#47367=CARTESIAN_POINT ( 'NONE',  ( -11.35316468749999963, 244.2187500034140157, 0.000000000000000000 ) ) ;
#47397=DIRECTION ( 'NONE',  ( 0.000000000000000000, 1.000000000000000000, 0.000000000000000000 ) ) ;
#47420=CARTESIAN_POINT ( 'NONE',  ( -3.042071309553166625, 227.8645833367473301, -11.35316468749999608 ) ) ;
#47424=CARTESIAN_POINT ( 'NONE',  ( 5.676582343750005144, 235.8854166700806729, 9.832129032723416984 ) ) ;
#47438=CARTESIAN_POINT ( 'NONE',  ( 2.326828918379975309E-15, 265.0000000000000000, 19.00000000000003553 ) ) ;
#47456=CARTESIAN_POINT ( 'NONE',  ( 1.836970198721029589E-15, 224.3750000068279746, 10.00000000000000000 ) ) ;
#47480=CARTESIAN_POINT ( 'NONE',  ( 9.999999999999998224, 245.8333333401613174, -2.679491924311229401 ) ) ;
#47487=ORIENTED_EDGE ( 'NONE', *, *, #58332, .F. ) ;
#47520=MECHANICAL_DESIGN_GEOMETRIC_PRESENTATION_REPRESENTATION('',(#28273),#12698);
#47524=CARTESIAN_POINT ( 'NONE',  ( -7.320508075688771932, 249.3750000000000000, -7.320508075688771932 ) ) ;
#47526=CARTESIAN_POINT ( 'NONE',  ( 11.35316468749999608, 231.9270833367473585, -3.042071309553167069 ) ) ;
#47551=FACE_OUTER_BOUND ( 'NONE', #70147, .T. ) ;
#47562=CARTESIAN_POINT ( 'NONE',  ( 10.00000000000000000, 225.6250000068279746, -1.224646799147353256E-15 ) ) ;
#47563=CARTESIAN_POINT ( 'NONE',  ( 11.35316468749999963, 246.1979166700806445, 3.042071309553159519 ) ) ;
#47609=CARTESIAN_POINT ( 'NONE',  ( 1.836970198721029589E-15, 221.2500000000000000, 10.00000000000000000 ) ) ;
#47649=EDGE_CURVE ( 'NONE', #23384, #29935, #48930, .T. ) ;
#47694=CARTESIAN_POINT ( 'NONE',  ( 11.35316468749999963, 231.1979166700806161, 3.042071309553159519 ) ) ;
#47699=CARTESIAN_POINT ( 'NONE',  ( -7.320508075688771932, 259.3750000000000568, -7.320508075688771932 ) ) ;
#47717=( BOUNDED_CURVE ( )  B_SPLINE_CURVE ( 2, ( #8657, #59961, #9032, #55064, #24873, #7549, #49382, #20713, #14295, #47892, #72401, #43729, #70912 ),
 .UNSPECIFIED., .F., .F. ) 
 B_SPLINE_CURVE_WITH_KNOTS ( ( 3, 2, 2, 2, 2, 2, 3 ),
 ( 0.4166666666666664076, 0.4259259259259256525, 0.4351851851851848973, 0.4444444444444441422, 0.4537037037037034981, 0.4629629629629627430, 0.4722222222222219878 ),
 .UNSPECIFIED. ) 
 CURVE ( )  GEOMETRIC_REPRESENTATION_ITEM ( )  RATIONAL_B_SPLINE_CURVE ( ( 1.000000000000001110, 0.9659258262890673130, 1.000000000000000000, 0.9659258262890683122, 1.000000000000000000, 0.9659258262890683122, 1.000000000000000000, 0.9659258262890683122, 1.000000000000000000, 0.9659258262890683122, 1.000000000000000000, 0.9659258262890690894, 0.9999999999999992228 ) ) 
 REPRESENTATION_ITEM ( '' )  );
#47728=CARTESIAN_POINT ( 'NONE',  ( 11.35316468749999963, 226.5104166700806445, 3.042071309553159519 ) ) ;
#47738=( GEOMETRIC_REPRESENTATION_CONTEXT ( 3 ) GLOBAL_UNCERTAINTY_ASSIGNED_CONTEXT ( ( #6595 ) ) GLOBAL_UNIT_ASSIGNED_CONTEXT ( ( #32875, #43800, #44177 ) ) REPRESENTATION_CONTEXT ( 'NONE', 'WORKASPACE' ) );
#47784=CARTESIAN_POINT ( 'NONE',  ( 8.311093377946834337, 237.0312500034139873, -8.311093377946836114 ) ) ;
#47787=EDGE_LOOP ( 'NONE', ( #480, #48911, #16984, #28577 ) ) ;
#47788=CARTESIAN_POINT ( 'NONE',  ( -9.832129032723415207, 224.6354166700806729, 5.676582343750005144 ) ) ;
#47845=CARTESIAN_POINT ( 'NONE',  ( 7.320508075688771044, 263.1249999999999432, -7.320508075688771932 ) ) ;
#47849=CARTESIAN_POINT ( 'NONE',  ( -8.660254037844385522, 238.5416666734946318, 5.000000000000004441 ) ) ;
#47873=CARTESIAN_POINT ( 'NONE',  ( 2.085542519210945334E-15, 260.4687500034140157, 11.35316468749999963 ) ) ;
#47892=CARTESIAN_POINT ( 'NONE',  ( -7.320508075688771932, 242.5000000068279746, -7.320508075688771932 ) ) ;
#47894=CARTESIAN_POINT ( 'NONE',  ( -10.00000000000000000, 250.0000000000000000, 0.000000000000000000 ) ) ;
#47896=CARTESIAN_POINT ( 'NONE',  ( 5.676582343749997150, 222.5520833367473017, -9.832129032723418760 ) ) ;
#47931=CARTESIAN_POINT ( 'NONE',  ( -5.676582343749992710, 234.7395833367473301, 9.832129032723422313 ) ) ;
#47946=( BOUNDED_CURVE ( )  B_SPLINE_CURVE ( 2, ( #53892, #25200, #1118, #47845, #71592, #1489, #70866, #48213, #12773, #36910, #70501, #1843, #13136 ),
 .UNSPECIFIED., .F., .F. ) 
 B_SPLINE_CURVE_WITH_KNOTS ( ( 3, 2, 2, 2, 2, 2, 3 ),
 ( 0.02777777777777718296, 0.03703703703703645211, 0.04629629629629572474, 0.05555555555555498348, 0.06481481481481425611, 0.07407407407407351485, 0.08333333333333278747 ),
 .UNSPECIFIED. ) 
 CURVE ( )  GEOMETRIC_REPRESENTATION_ITEM ( )  RATIONAL_B_SPLINE_CURVE ( ( 1.000000000000002220, 0.9659258262890662028, 1.000000000000000000, 0.9659258262890683122, 1.000000000000000000, 0.9659258262890683122, 1.000000000000000000, 0.9659258262890683122, 1.000000000000000000, 0.9659258262890683122, 1.000000000000000000, 0.9659258262890703106, 0.9999999999999980016 ) ) 
 REPRESENTATION_ITEM ( '' )  );
#47982=CARTESIAN_POINT ( 'NONE',  ( 2.679491924311225848, 228.5416666666666572, -10.00000000000000000 ) ) ;
#47999=CARTESIAN_POINT ( 'NONE',  ( 0.000000000000000000, 0.000000000000000000, 0.000000000000000000 ) ) ;
#48036=CARTESIAN_POINT ( 'NONE',  ( 2.020667218593132706E-15, 219.9523502760175973, 11.00000000000000000 ) ) ;
#48058=DIRECTION ( 'NONE',  ( -0.000000000000000000, -1.000000000000000000, -0.000000000000000000 ) ) ;
#48068=CARTESIAN_POINT ( 'NONE',  ( 9.832129032723420536, 235.9895833367473301, 5.676582343749996262 ) ) ;
#48095=CARTESIAN_POINT ( 'NONE',  ( 1.836970198721029589E-15, 239.3750000068279746, 10.00000000000000000 ) ) ;
#48100=CARTESIAN_POINT ( 'NONE',  ( 5.676582343750005144, 230.8854166700806729, 9.832129032723416984 ) ) ;
#48108=CARTESIAN_POINT ( 'NONE',  ( 6.682541319018295845, 220.0000000000001137, 7.585481667126755312 ) ) ;
#48113=APPLICATION_CONTEXT ( 'automotive_design' ) ;
#48154=CARTESIAN_POINT ( 'NONE',  ( -9.832129032723418760, 238.4895833367473301, -5.676582343749998927 ) ) ;
#48159=CARTESIAN_POINT ( 'NONE',  ( 9.832129032723420536, 221.3020833367473301, 5.676582343749996262 ) ) ;
#48213=CARTESIAN_POINT ( 'NONE',  ( 10.00000000000000178, 262.2916666666666288, 2.679491924311222739 ) ) ;
#48216=CARTESIAN_POINT ( 'NONE',  ( 5.000000000000004441, 234.7916666734946602, 8.660254037844385522 ) ) ;
#48227=CIRCLE ( 'NONE', #42192, 19.00000000000003553 ) ;
#48240=CIRCLE ( 'NONE', #56727, 10.00000000000000000 ) ;
#48244=CARTESIAN_POINT ( 'NONE',  ( -5.676582343750000703, 263.3854166700806445, -9.832129032723418760 ) ) ;
#48267=CARTESIAN_POINT ( 'NONE',  ( 2.085542519210945334E-15, 235.4687500034139873, 11.35316468749999963 ) ) ;
#48276=CARTESIAN_POINT ( 'NONE',  ( -6.123233995736766282E-16, 238.7500000000000284, -10.00000000000000000 ) ) ;
#48280=DIRECTION ( 'NONE',  ( -0.000000000000000000, -1.000000000000000000, -0.000000000000000000 ) ) ;
#48304=CARTESIAN_POINT ( 'NONE',  ( -3.042071309553159075, 239.9479166700806729, 11.35316468749999963 ) ) ;
#48351=CARTESIAN_POINT ( 'NONE',  ( 7.320508075688771044, 223.1250000000000284, -7.320508075688771932 ) ) ;
#48372=CARTESIAN_POINT ( 'NONE',  ( -2.679491924311222295, 231.0416666666666856, 10.00000000000000178 ) ) ;
#48376=EDGE_CURVE ( 'NONE', #56463, #11938, #4564, .T. ) ;
#48380=DIRECTION ( 'NONE',  ( -0.000000000000000000, -1.000000000000000000, -0.000000000000000000 ) ) ;
#48424=ORIENTED_EDGE ( 'NONE', *, *, #29706, .F. ) ;
#48436=CARTESIAN_POINT ( 'NONE',  ( -3.042071309553159075, 229.9479166700806161, 11.35316468749999963 ) ) ;
#48442=CARTESIAN_POINT ( 'NONE',  ( -10.00000000000000000, 264.7916666666666856, -2.679491924311226292 ) ) ;
#48446=CARTESIAN_POINT ( 'NONE',  ( 5.000000000000004441, 239.7916666734946318, 8.660254037844385522 ) ) ;
#48471=CARTESIAN_POINT ( 'NONE',  ( -9.832129032723415207, 229.6354166700806729, 5.676582343750005144 ) ) ;
#48482=CARTESIAN_POINT ( 'NONE',  ( 5.539869284409778771, 219.9999999999998863, 8.691086950455378712 ) ) ;
#48523=CARTESIAN_POINT ( 'NONE',  ( -8.311093377946836114, 223.2812500034140157, -8.311093377946836114 ) ) ;
#48526=CARTESIAN_POINT ( 'NONE',  ( 3.042071309553173286, 225.6770833367473017, 11.35316468749999608 ) ) ;
#48586=CARTESIAN_POINT ( 'NONE',  ( 5.000000000000004441, 239.7916666734946318, 8.660254037844385522 ) ) ;
#48610=CARTESIAN_POINT ( 'NONE',  ( -11.35316468749999785, 258.6979166700807014, -3.042071309553164848 ) ) ;
#48636=CARTESIAN_POINT ( 'NONE',  ( -11.35316468749999963, 219.2187500034139873, 0.000000000000000000 ) ) ;
#48651=CARTESIAN_POINT ( 'NONE',  ( -4.999999999999992895, 260.8333333333333712, 8.660254037844390851 ) ) ;
#48674=CARTESIAN_POINT ( 'NONE',  ( -3.042071309553159075, 229.9479166700806161, 11.35316468749999963 ) ) ;
#48709=CARTESIAN_POINT ( 'NONE',  ( -10.00000000000000000, 220.0000000000000000, 0.000000000000000000 ) ) ;
#48724=CARTESIAN_POINT ( 'NONE',  ( -5.676582343749992710, 250.0520833367473301, 9.832129032723422313 ) ) ;
#48777=ORIENTED_EDGE ( 'NONE', *, *, #23627, .F. ) ;
#48811=CARTESIAN_POINT ( 'NONE',  ( -5.676582343749992710, 229.7395833367473301, 9.832129032723422313 ) ) ;
#48819=CARTESIAN_POINT ( 'NONE',  ( 7.320508075688771044, 241.2500000068279462, -7.320508075688771932 ) ) ;
#48823=CARTESIAN_POINT ( 'NONE',  ( -6.123233995736766282E-16, 261.8750000068280315, -10.00000000000000000 ) ) ;
#48843=CARTESIAN_POINT ( 'NONE',  ( 11.35316468749999963, 236.7187500034139873, -1.390361679473963556E-15 ) ) ;
#48897=CARTESIAN_POINT ( 'NONE',  ( -11.35316468749999963, 229.2187500034139873, 0.000000000000000000 ) ) ;
#48911=ORIENTED_EDGE ( 'NONE', *, *, #34321, .F. ) ;
#48930=LINE ( 'NONE', #42895, #25482 ) ;
#48959=CARTESIAN_POINT ( 'NONE',  ( 7.320508075688776373, 240.0000000068279178, 7.320508075688767491 ) ) ;
#48965=EDGE_LOOP ( 'NONE', ( #50784, #27838, #17705, #73217 ) ) ;
#48975=EDGE_CURVE ( 'NONE', #52445, #24629, #13583, .T. ) ;
#48979=CARTESIAN_POINT ( 'NONE',  ( -8.311093377946836114, 263.2812500034139589, -8.311093377946836114 ) ) ;
#49047=CARTESIAN_POINT ( 'NONE',  ( 3.042071309553163960, 232.4479166700806161, -11.35316468749999785 ) ) ;
#49089=VERTEX_POINT ( 'NONE', #45251 ) ;
#49097=CARTESIAN_POINT ( 'NONE',  ( -3.042071309553166181, 253.1770833367473017, -11.35316468749999608 ) ) ;
#49174=CARTESIAN_POINT ( 'NONE',  ( 0.000000000000000000, 0.000000000000000000, 0.000000000000000000 ) ) ;
#49182=CARTESIAN_POINT ( 'NONE',  ( -11.35316468749999963, 223.9062500034139873, 0.000000000000000000 ) ) ;
#49183=ADVANCED_FACE ( 'NONE', ( #9440 ), #32457, .F. ) ;
#49188=CARTESIAN_POINT ( 'NONE',  ( 10.00000000000000000, 257.5000000000000000, -1.224646799147353256E-15 ) ) ;
#49208=AXIS2_PLACEMENT_3D ( 'NONE', #14388, #10243, #49476 ) ;
#49239=CARTESIAN_POINT ( 'NONE',  ( -6.123233995736766282E-16, 258.7500000000000568, -10.00000000000000000 ) ) ;
#49241=CARTESIAN_POINT ( 'NONE',  ( -6.123233995736766282E-16, 238.7500000000000284, -10.00000000000000000 ) ) ;
#49274=CARTESIAN_POINT ( 'NONE',  ( 5.676582343749997150, 232.5520833367473301, -9.832129032723418760 ) ) ;
#49308=CARTESIAN_POINT ( 'NONE',  ( 4.999999999999997335, 233.3333333333333428, -8.660254037844387298 ) ) ;
#49338=CARTESIAN_POINT ( 'NONE',  ( -7.320508075688771932, 242.5000000068279178, -7.320508075688771932 ) ) ;
#49359=CARTESIAN_POINT ( 'NONE',  ( -3.042071309553166625, 252.8645833367473301, -11.35316468749999608 ) ) ;
#49362=CARTESIAN_POINT ( 'NONE',  ( 11.35316468749999963, 261.5104166700807014, 3.042071309553159519 ) ) ;
#49382=CARTESIAN_POINT ( 'NONE',  ( -10.00000000000000000, 243.1250000068280031, 0.000000000000000000 ) ) ;
#49386=CARTESIAN_POINT ( 'NONE',  ( -9.832129032723415207, 219.6354166700806445, 5.676582343750005144 ) ) ;
#49427=CARTESIAN_POINT ( 'NONE',  ( 5.676582343749997150, 237.2395833367473301, -9.832129032723418760 ) ) ;
#49476=DIRECTION ( 'NONE',  ( 0.000000000000000000, 0.000000000000000000, -1.000000000000000000 ) ) ;
#49478=CARTESIAN_POINT ( 'NONE',  ( -9.832129032723415207, 259.6354166700806445, 5.676582343750005144 ) ) ;
#49569=CARTESIAN_POINT ( 'NONE',  ( 2.679491924311235174, 251.4583333333333428, 9.999999999999998224 ) ) ;
#49603=CARTESIAN_POINT ( 'NONE',  ( -11.35316468749999963, 224.2187500034139873, 0.000000000000000000 ) ) ;
#49613=CYLINDRICAL_SURFACE ( 'NONE', #16836, 10.00000000000000000 ) ;
#49657=CARTESIAN_POINT ( 'NONE',  ( 9.832129032723416984, 256.8229166700806445, -5.676582343750003368 ) ) ;
#49673=EDGE_LOOP ( 'NONE', ( #72780, #42396, #9831, #61582 ) ) ;
#49695=CARTESIAN_POINT ( 'NONE',  ( -8.660254037844387298, 222.7083333401613174, -4.999999999999999112 ) ) ;
#49696=CARTESIAN_POINT ( 'NONE',  ( 9.832129032723420536, 261.3020833367473301, 5.676582343749996262 ) ) ;
#49708=DIRECTION ( 'NONE',  ( 0.000000000000000000, 0.000000000000000000, -1.000000000000000000 ) ) ;
#49721=CARTESIAN_POINT ( 'NONE',  ( 8.660254037844389075, 220.2083333401613174, 4.999999999999997335 ) ) ;
#49742=CARTESIAN_POINT ( 'NONE',  ( -5.000000000000000888, 257.2916666734946034, -8.660254037844387298 ) ) ;
#49747=CARTESIAN_POINT ( 'NONE',  ( 2.085542519210945334E-15, 250.4687500034140157, 11.35316468749999963 ) ) ;
#49795=DIRECTION ( 'NONE',  ( -0.000000000000000000, -1.000000000000000000, -0.000000000000000000 ) ) ;
#49806=CARTESIAN_POINT ( 'NONE',  ( 8.311093377946834337, 227.0312500034140157, -8.311093377946836114 ) ) ;
#49830=CARTESIAN_POINT ( 'NONE',  ( 2.679491924311168560, 236.6666666734946602, -10.00000000000003375 ) ) ;
#49856=CARTESIAN_POINT ( 'NONE',  ( 5.676582343749997150, 252.5520833367473301, -9.832129032723418760 ) ) ;
#49905=ORIENTED_EDGE ( 'NONE', *, *, #20887, .F. ) ;
#49940=CARTESIAN_POINT ( 'NONE',  ( 5.676582343749997150, 222.2395833367473017, -9.832129032723418760 ) ) ;
#49945=CARTESIAN_POINT ( 'NONE',  ( 2.679491924311225848, 248.5416666666666856, -10.00000000000000000 ) ) ;
#49952=CARTESIAN_POINT ( 'NONE',  ( 10.00000000000000000, 260.6250000068279746, -1.224646799147353256E-15 ) ) ;
#49953=DIRECTION ( 'NONE',  ( 0.000000000000000000, 1.000000000000000000, 0.000000000000000000 ) ) ;
#49982=DIRECTION ( 'NONE',  ( 0.000000000000000000, 0.000000000000000000, -1.000000000000000000 ) ) ;
#49995=CARTESIAN_POINT ( 'NONE',  ( 1.836970198721029589E-15, 236.2500000000000284, 10.00000000000000178 ) ) ;
#50001=ORIENTED_EDGE ( 'NONE', *, *, #8254, .T. ) ;
#50023=CARTESIAN_POINT ( 'NONE',  ( -5.676582343749992710, 224.7395833367473301, 9.832129032723422313 ) ) ;
#50027=CARTESIAN_POINT ( 'NONE',  ( -11.35316468749999608, 219.4270833367473301, 3.042071309553173730 ) ) ;
#50034=ORIENTED_EDGE ( 'NONE', *, *, #41835, .F. ) ;
#50062=CARTESIAN_POINT ( 'NONE',  ( -5.000000000000000888, 222.2916666734946602, -8.660254037844387298 ) ) ;
#50063=CARTESIAN_POINT ( 'NONE',  ( 11.35316468749999963, 256.5104166700807014, 3.042071309553159519 ) ) ;
#50090=CARTESIAN_POINT ( 'NONE',  ( -2.679491924311222295, 219.1666666734946602, 10.00000000000000178 ) ) ;
#50113=CARTESIAN_POINT ( 'NONE',  ( 11.35316468749999963, 261.4062500034140157, -1.390361679473963556E-15 ) ) ;
#50117=CARTESIAN_POINT ( 'NONE',  ( 3.042071309553163960, 257.7604166700806445, -11.35316468749999785 ) ) ;
#50176=CARTESIAN_POINT ( 'NONE',  ( 5.000000000000004441, 259.7916666734946034, 8.660254037844385522 ) ) ;
#50191=AXIS2_PLACEMENT_3D ( 'NONE', #29027, #24096, #35446 ) ;
#50217=EDGE_LOOP ( 'NONE', ( #8729, #21420, #25205, #16023 ) ) ;
#50225=CARTESIAN_POINT ( 'NONE',  ( -9.832129032723418760, 253.8020833367473017, -5.676582343749998927 ) ) ;
#50258=CARTESIAN_POINT ( 'NONE',  ( -11.35316468749999785, 263.6979166700807014, -3.042071309553164848 ) ) ;
#50267=CARTESIAN_POINT ( 'NONE',  ( 2.679491924311226292, 231.6666666734946034, -10.00000000000000000 ) ) ;
#50295=CARTESIAN_POINT ( 'NONE',  ( 0.000000000000000000, 0.000000000000000000, -10.00000000000000000 ) ) ;
#50298=CARTESIAN_POINT ( 'NONE',  ( -10.67658234375000070, 264.6093750017070079, 0.000000000000000000 ) ) ;
#50312=CARTESIAN_POINT ( 'NONE',  ( -4.999999999999992895, 245.8333333333333428, 8.660254037844390851 ) ) ;
#50339=CARTESIAN_POINT ( 'NONE',  ( -11.35316468749999608, 219.4270833367473585, 3.042071309553173730 ) ) ;
#50348=CARTESIAN_POINT ( 'NONE',  ( 9.999999999999998224, 247.7083333333333428, -2.679491924311229401 ) ) ;
#50399=CARTESIAN_POINT ( 'NONE',  ( 9.832129032723420536, 255.9895833367473301, 5.676582343749996262 ) ) ;
#50431=CARTESIAN_POINT ( 'NONE',  ( -8.311093377946836114, 263.5937500034140157, -8.311093377946836114 ) ) ;
#50455=CARTESIAN_POINT ( 'NONE',  ( -7.320508075688771932, 222.5000000068280031, -7.320508075688771932 ) ) ;
#50456=CARTESIAN_POINT ( 'NONE',  ( -10.00000000000000000, 252.9166666734946602, -2.679491924311226292 ) ) ;
#50463=ORIENTED_EDGE ( 'NONE', *, *, #42716, .F. ) ;
#50478=CARTESIAN_POINT ( 'NONE',  ( 9.832129032723416984, 246.8229166700806729, -5.676582343750003368 ) ) ;
#50482=CARTESIAN_POINT ( 'NONE',  ( -9.832129032723415207, 254.6354166700806729, 5.676582343750005144 ) ) ;
#50521=CARTESIAN_POINT ( 'NONE',  ( -7.320508075688770155, 245.6250000000000000, 7.320508075688774596 ) ) ;
#50535=ORIENTED_EDGE ( 'NONE', *, *, #40654, .F. ) ;
#50544=CARTESIAN_POINT ( 'NONE',  ( -9.832129032723415207, 224.3229166700806729, 5.676582343750005144 ) ) ;
#50547=VERTEX_POINT ( 'NONE', #15924 ) ;
#50593=CARTESIAN_POINT ( 'NONE',  ( 8.311093377946839666, 236.0937500034139589, 8.311093377946829008 ) ) ;
#50615=EDGE_CURVE ( 'NONE', #53701, #35109, #70203, .T. ) ;
#50629=CARTESIAN_POINT ( 'NONE',  ( 8.311093377946839666, 260.7812500034140157, 8.311093377946829008 ) ) ;
#50662=DIRECTION ( 'NONE',  ( -0.000000000000000000, -1.000000000000000000, -0.000000000000000000 ) ) ;
#50679=CARTESIAN_POINT ( 'NONE',  ( -7.320508075688771932, 249.3750000000000284, -7.320508075688771932 ) ) ;
#50682=CARTESIAN_POINT ( 'NONE',  ( 0.000000000000000000, 45.00000000000000000, -8.749999999999998224 ) ) ;
#50712=CARTESIAN_POINT ( 'NONE',  ( -11.35316468749999963, 219.2187500034139873, 0.000000000000000000 ) ) ;
#50725=AXIS2_PLACEMENT_3D ( 'NONE', #1394, #24006, #71126 ) ;
#50752=EDGE_CURVE ( 'NONE', #53500, #16650, #60841, .T. ) ;
#50766=CARTESIAN_POINT ( 'NONE',  ( -5.676582343750000703, 258.0729166700806445, -9.832129032723418760 ) ) ;
#50780=CIRCLE ( 'NONE', #60406, 10.00000000000000000 ) ;
#50784=ORIENTED_EDGE ( 'NONE', *, *, #13029, .F. ) ;
#50804=CARTESIAN_POINT ( 'NONE',  ( -3.042071309553159075, 255.2604166700806445, 11.35316468749999963 ) ) ;
#50832=CARTESIAN_POINT ( 'NONE',  ( -8.660254037844387298, 222.7083333401613174, -4.999999999999999112 ) ) ;
#50838=VECTOR ( 'NONE', #28385, 1000.000000000000000 ) ;
#50855=CARTESIAN_POINT ( 'NONE',  ( -11.35316468749999963, 248.9062500034139873, 0.000000000000000000 ) ) ;
#50860=CARTESIAN_POINT ( 'NONE',  ( 3.042071309553163960, 252.7604166700806445, -11.35316468749999785 ) ) ;
#50897=CARTESIAN_POINT ( 'NONE',  ( -8.660254037844385522, 245.4166666666666856, 5.000000000000004441 ) ) ;
#50921=CARTESIAN_POINT ( 'NONE',  ( -8.311093377946836114, 223.2812500034140157, -8.311093377946836114 ) ) ;
#50971=CARTESIAN_POINT ( 'NONE',  ( -3.042071309553159075, 245.2604166700806729, 11.35316468749999963 ) ) ;
#50986=CARTESIAN_POINT ( 'NONE',  ( 10.00000000000000000, 227.5000000000000000, -1.224646799147353256E-15 ) ) ;
#51008=CARTESIAN_POINT ( 'NONE',  ( 2.679491924311226292, 226.6666666734946034, -10.00000000000000000 ) ) ;
#51009=CARTESIAN_POINT ( 'NONE',  ( 11.35316468749999608, 256.6145833367473301, -3.042071309553167069 ) ) ;
#51021=AXIS2_PLACEMENT_3D ( 'NONE', #53575, #54694, #3003 ) ;
#51057=CARTESIAN_POINT ( 'NONE',  ( 4.999999999999997335, 243.3333333333333428, -8.660254037844387298 ) ) ;
#51067=ORIENTED_EDGE ( 'NONE', *, *, #44942, .T. ) ;
#51101=CYLINDRICAL_SURFACE ( 'NONE', #2191, 10.00000000000000000 ) ;
#51142=CARTESIAN_POINT ( 'NONE',  ( 3.042071309553163960, 252.4479166700806729, -11.35316468749999785 ) ) ;
#51146=CARTESIAN_POINT ( 'NONE',  ( -8.577559645643342279, 220.0000000000000284, 6.763852041043552532 ) ) ;
#51178=CARTESIAN_POINT ( 'NONE',  ( 5.676582343749997150, 262.5520833367473301, -9.832129032723418760 ) ) ;
#51205=CARTESIAN_POINT ( 'NONE',  ( 10.00000000000000178, 225.4166666734946602, 2.679491924311222739 ) ) ;
#51230=CARTESIAN_POINT ( 'NONE',  ( -3.042071309553159075, 249.9479166700806729, 11.35316468749999963 ) ) ;
#51234=CARTESIAN_POINT ( 'NONE',  ( 11.35316468749999608, 246.9270833367472733, -3.042071309553167069 ) ) ;
#51293=CARTESIAN_POINT ( 'NONE',  ( 2.679491924311225848, 261.6666666734946602, -10.00000000000000000 ) ) ;
#51342=CARTESIAN_POINT ( 'NONE',  ( 9.832129032723420536, 246.3020833367473301, 5.676582343749996262 ) ) ;
#51376=CARTESIAN_POINT ( 'NONE',  ( 8.660254037844385522, 226.0416666734946602, -5.000000000000003553 ) ) ;
#51377=CARTESIAN_POINT ( 'NONE',  ( 5.676582343749997150, 257.2395833367473301, -9.832129032723418760 ) ) ;
#51385=EDGE_LOOP ( 'NONE', ( #52444, #58403 ) ) ;
#51428=CARTESIAN_POINT ( 'NONE',  ( 10.00000000000000178, 237.2916666666666288, 2.679491924311222739 ) ) ;
#51513=CARTESIAN_POINT ( 'NONE',  ( 5.676582343750005144, 245.5729166700806729, 9.832129032723416984 ) ) ;
#51546=CARTESIAN_POINT ( 'NONE',  ( 2.085542519210945334E-15, 245.4687500034140157, 11.35316468749999963 ) ) ;
#51603=CARTESIAN_POINT ( 'NONE',  ( -6.951808397369817780E-16, 242.6562500034140157, -11.35316468749999963 ) ) ;
#51607=CARTESIAN_POINT ( 'NONE',  ( 3.042071309553163960, 237.7604166700806161, -11.35316468749999785 ) ) ;
#51651=DIRECTION ( 'NONE',  ( 0.000000000000000000, 0.000000000000000000, -1.000000000000000000 ) ) ;
#51668=CARTESIAN_POINT ( 'NONE',  ( 5.000000000000004441, 249.7916666734946318, 8.660254037844385522 ) ) ;
#51715=CARTESIAN_POINT ( 'NONE',  ( -5.676582343750000703, 243.3854166700806445, -9.832129032723418760 ) ) ;
#51722=CARTESIAN_POINT ( 'NONE',  ( -4.999999999999992895, 240.8333333333333428, 8.660254037844390851 ) ) ;
#51753=CARTESIAN_POINT ( 'NONE',  ( -3.042071309553166181, 257.8645833367473301, -11.35316468749999608 ) ) ;
#51758=DIRECTION ( 'NONE',  ( 0.000000000000000000, -0.000000000000000000, 1.000000000000000000 ) ) ;
#51799=CARTESIAN_POINT ( 'NONE',  ( 10.00000000000000178, 252.2916666666666856, 2.679491924311222739 ) ) ;
#51804=CARTESIAN_POINT ( 'NONE',  ( -2.679491924311228512, 238.9583333333333144, -9.999999999999998224 ) ) ;
#51895=CARTESIAN_POINT ( 'NONE',  ( 8.311093377946834337, 242.0312500034140157, -8.311093377946836114 ) ) ;
#51898=CARTESIAN_POINT ( 'NONE',  ( -9.418986816871308676, 219.9999999999999716, 5.041166117107052536 ) ) ;
#51900=ADVANCED_FACE ( 'NONE', ( #62429 ), #73754, .F. ) ;
#51931=CARTESIAN_POINT ( 'NONE',  ( 8.311093377946839666, 246.0937500034139873, 8.311093377946830785 ) ) ;
#51986=CARTESIAN_POINT ( 'NONE',  ( 3.042071309553173286, 240.3645833367473301, 11.35316468749999608 ) ) ;
#51990=CARTESIAN_POINT ( 'NONE',  ( -8.311093377946836114, 243.5937500034140157, -8.311093377946836114 ) ) ;
#52039=ORIENTED_EDGE ( 'NONE', *, *, #65332, .F. ) ;
#52047=CARTESIAN_POINT ( 'NONE',  ( -5.000000000000000888, 252.2916666734946602, -8.660254037844387298 ) ) ;
#52049=EDGE_LOOP ( 'NONE', ( #43650, #40651, #55137, #35110 ) ) ;
#52067=ORIENTED_EDGE ( 'NONE', *, *, #44942, .F. ) ;
#52102=CARTESIAN_POINT ( 'NONE',  ( 9.832129032723416984, 237.1354166700806445, -5.676582343750003368 ) ) ;
#52110=CARTESIAN_POINT ( 'NONE',  ( 0.000000000000000000, 220.0000000000000284, -11.00000000000000000 ) ) ;
#52137=CARTESIAN_POINT ( 'NONE',  ( -5.676582343749992710, 249.7395833367473301, 9.832129032723422313 ) ) ;
#52180=EDGE_CURVE ( 'NONE', #49089, #33033, #60068, .T. ) ;
#52187=CARTESIAN_POINT ( 'NONE',  ( -2.679491924311222295, 236.0416666666666856, 10.00000000000000178 ) ) ;
#52197=ORIENTED_EDGE ( 'NONE', *, *, #56237, .F. ) ;
#52255=CARTESIAN_POINT ( 'NONE',  ( 10.00000000000000178, 250.4166666734946602, 2.679491924311222739 ) ) ;
#52270=CARTESIAN_POINT ( 'NONE',  ( -3.042071309553159075, 244.9479166700806445, 11.35316468749999963 ) ) ;
#52304=CARTESIAN_POINT ( 'NONE',  ( -3.042071309553166625, 248.1770833367473017, -11.35316468749999608 ) ) ;
#52326=VERTEX_POINT ( 'NONE', #59380 ) ;
#52356=CARTESIAN_POINT ( 'NONE',  ( -9.832129032723418760, 233.4895833367473301, -5.676582343749998927 ) ) ;
#52361=CARTESIAN_POINT ( 'NONE',  ( -8.311093377946834337, 239.8437500034139873, 8.311093377946837890 ) ) ;
#52389=EDGE_CURVE ( 'NONE', #26323, #46305, #38938, .T. ) ;
#52418=CARTESIAN_POINT ( 'NONE',  ( 1.836970198721029589E-15, 254.3750000068280031, 10.00000000000000000 ) ) ;
#52444=ORIENTED_EDGE ( 'NONE', *, *, #63145, .T. ) ;
#52445=VERTEX_POINT ( 'NONE', #72162 ) ;
#52463=CARTESIAN_POINT ( 'NONE',  ( -9.999999999999998224, 250.2083333333333144, 2.679491924311235174 ) ) ;
#52465=CARTESIAN_POINT ( 'NONE',  ( 3.042071309553163960, 227.7604166700806445, -11.35316468749999785 ) ) ;
#52501=CARTESIAN_POINT ( 'NONE',  ( -3.042071309553166181, 252.8645833367473301, -11.35316468749999608 ) ) ;
#52550=CARTESIAN_POINT ( 'NONE',  ( -2.679491924311228512, 223.9583333333333428, -9.999999999999998224 ) ) ;
#52569=EDGE_CURVE ( 'NONE', #32440, #64909, #22334, .T. ) ;
#52638=CARTESIAN_POINT ( 'NONE',  ( -3.042071309553166181, 247.8645833367472733, -11.35316468749999608 ) ) ;
#52666=CARTESIAN_POINT ( 'NONE',  ( -7.320508075688770155, 225.6250000000000000, 7.320508075688774596 ) ) ;
#52671=CARTESIAN_POINT ( 'NONE',  ( 2.085542519210945334E-15, 240.4687500034139873, 11.35316468749999963 ) ) ;
#52727=CARTESIAN_POINT ( 'NONE',  ( 5.676582343749997150, 237.2395833367473301, -9.832129032723418760 ) ) ;
#52732=CARTESIAN_POINT ( 'NONE',  ( -11.35316468749999608, 239.4270833367473301, 3.042071309553173730 ) ) ;
#52784=CARTESIAN_POINT ( 'NONE',  ( -6.123233995736766282E-16, 246.8750000068280031, -10.00000000000000000 ) ) ;
#52827=VECTOR ( 'NONE', #32901, 1000.000000000000000 ) ;
#52835=CARTESIAN_POINT ( 'NONE',  ( 9.832129032723420536, 226.3020833367473301, 5.676582343749996262 ) ) ;
#52873=CARTESIAN_POINT ( 'NONE',  ( 3.042071309553173286, 250.3645833367473301, 11.35316468749999608 ) ) ;
#52923=CARTESIAN_POINT ( 'NONE',  ( -7.320508075688770155, 225.6249999999999716, 7.320508075688774596 ) ) ;
#52927=EDGE_CURVE ( 'NONE', #67635, #71847, #16047, .T. ) ;
#53009=CARTESIAN_POINT ( 'NONE',  ( 3.042071309553163960, 232.4479166700806161, -11.35316468749999785 ) ) ;
#53014=CARTESIAN_POINT ( 'NONE',  ( 8.660254037844385522, 257.9166666666666856, -5.000000000000003553 ) ) ;
#53038=CARTESIAN_POINT ( 'NONE',  ( -8.660254037844387298, 224.5833333333333712, -4.999999999999999112 ) ) ;
#53043=CARTESIAN_POINT ( 'NONE',  ( 5.676582343750005144, 245.8854166700806445, 9.832129032723416984 ) ) ;
#53061=CYLINDRICAL_SURFACE ( 'NONE', #50725, 10.00000000000000000 ) ;
#53085=VECTOR ( 'NONE', #13264, 1000.000000000000000 ) ;
#53098=CARTESIAN_POINT ( 'NONE',  ( 3.042071309553163516, 232.4479166700806445, -11.35316468749999785 ) ) ;
#53103=CARTESIAN_POINT ( 'NONE',  ( 5.676582343750005144, 245.8854166700806445, 9.832129032723416984 ) ) ;
#53158=CARTESIAN_POINT ( 'NONE',  ( -2.679491924311228512, 247.0833333401613174, -9.999999999999998224 ) ) ;
#53207=CARTESIAN_POINT ( 'NONE',  ( 8.311093377946839666, 226.0937500034140157, 8.311093377946829008 ) ) ;
#53218=CARTESIAN_POINT ( 'NONE',  ( 0.000000000000000000, 0.000000000000000000, 0.000000000000000000 ) ) ;
#53237=ORIENTED_EDGE ( 'NONE', *, *, #67089, .T. ) ;
#53246=CARTESIAN_POINT ( 'NONE',  ( -8.311093377946836114, 248.2812500034139873, -8.311093377946836114 ) ) ;
#53284=CARTESIAN_POINT ( 'NONE',  ( 0.000000000000000000, 220.0000000000000284, 0.000000000000000000 ) ) ;
#53297=CARTESIAN_POINT ( 'NONE',  ( 8.660254037844385522, 227.9166666666666856, -5.000000000000003553 ) ) ;
#53372=CARTESIAN_POINT ( 'NONE',  ( 7.320508075688776373, 255.0000000068279746, 7.320508075688767491 ) ) ;
#53381=CARTESIAN_POINT ( 'NONE',  ( -9.832129032723418760, 228.4895833367473585, -5.676582343749998927 ) ) ;
#53390=CARTESIAN_POINT ( 'NONE',  ( 10.00000000000000178, 240.4166666734946318, 2.679491924311222739 ) ) ;
#53413=CARTESIAN_POINT ( 'NONE',  ( 7.320508075688771044, 221.2500000068279746, -7.320508075688771932 ) ) ;
#53415=CARTESIAN_POINT ( 'NONE',  ( 11.35316468749999963, 226.7187500034139873, -1.390361679473963556E-15 ) ) ;
#53431=AXIS2_PLACEMENT_3D ( 'NONE', #32080, #26392, #67528 ) ;
#53468=CARTESIAN_POINT ( 'NONE',  ( -6.951808397369817780E-16, 227.6562500034139873, -11.35316468749999963 ) ) ;
#53472=CARTESIAN_POINT ( 'NONE',  ( -5.676582343750000703, 223.3854166700806729, -9.832129032723418760 ) ) ;
#53486=DIRECTION ( 'NONE',  ( 0.000000000000000000, 0.000000000000000000, -1.000000000000000000 ) ) ;
#53500=VERTEX_POINT ( 'NONE', #21810 ) ;
#53527=FACE_OUTER_BOUND ( 'NONE', #31741, .T. ) ;
#53529=CARTESIAN_POINT ( 'NONE',  ( 7.320508075688776373, 245.0000000068279462, 7.320508075688767491 ) ) ;
#53553=CARTESIAN_POINT ( 'NONE',  ( 3.042071309553173286, 260.6770833367473301, 11.35316468749999608 ) ) ;
#53566=CARTESIAN_POINT ( 'NONE',  ( 1.836970198721029589E-15, 234.3750000068279746, 10.00000000000000000 ) ) ;
#53574=CARTESIAN_POINT ( 'NONE',  ( -8.660254037844385522, 250.4166666666666856, 5.000000000000004441 ) ) ;
#53575=CARTESIAN_POINT ( 'NONE',  ( 0.000000000000000000, 45.00000000000000000, 0.000000000000000000 ) ) ;
#53576=CARTESIAN_POINT ( 'NONE',  ( -9.832129032723415207, 224.6354166700806729, 5.676582343750005144 ) ) ;
#53612=CARTESIAN_POINT ( 'NONE',  ( 1.836970198721029589E-15, 224.3750000068279746, 10.00000000000000000 ) ) ;
#53614=CARTESIAN_POINT ( 'NONE',  ( -5.676582343750000703, 243.0729166700806445, -9.832129032723418760 ) ) ;
#53648=ORIENTED_EDGE ( 'NONE', *, *, #67089, .F. ) ;
#53653=CARTESIAN_POINT ( 'NONE',  ( -11.35316468749999963, 264.2187500034140157, 0.000000000000000000 ) ) ;
#53662=CARTESIAN_POINT ( 'NONE',  ( -4.999999999999992895, 230.8333333333333428, 8.660254037844390851 ) ) ;
#53669=CARTESIAN_POINT ( 'NONE',  ( 10.00000000000000000, 242.5000000000000284, -1.224646799147353256E-15 ) ) ;
#53701=VERTEX_POINT ( 'NONE', #22946 ) ;
#53725=ORIENTED_EDGE ( 'NONE', *, *, #25585, .T. ) ;
#53747=CARTESIAN_POINT ( 'NONE',  ( 8.311093377946839666, 235.7812500034139589, 8.311093377946829008 ) ) ;
#53782=CARTESIAN_POINT ( 'NONE',  ( -9.832129032723415207, 224.6354166700806729, 5.676582343750005144 ) ) ;
#53818=( BOUNDED_CURVE ( )  B_SPLINE_CURVE ( 2, ( #14221, #71569, #49308, #30850, #14599, #19891, #53871, #3302, #1821, #43277, #42158, #30486, #37639 ),
 .UNSPECIFIED., .F., .F. ) 
 B_SPLINE_CURVE_WITH_KNOTS ( ( 3, 2, 2, 2, 2, 2, 3 ),
 ( 0.6944444444444444198, 0.7037037037037037202, 0.7129629629629629095, 0.7222222222222222099, 0.7314814814814815103, 0.7407407407407406996, 0.7500000000000000000 ),
 .UNSPECIFIED. ) 
 CURVE ( )  GEOMETRIC_REPRESENTATION_ITEM ( )  RATIONAL_B_SPLINE_CURVE ( ( 1.000000000000000000, 0.9659258262890683122, 1.000000000000000000, 0.9659258262890683122, 1.000000000000000000, 0.9659258262890683122, 1.000000000000000000, 0.9659258262890683122, 1.000000000000000000, 0.9659258262890683122, 1.000000000000000000, 0.9659258262890683122, 1.000000000000000000 ) ) 
 REPRESENTATION_ITEM ( '' )  );
#53830=VECTOR ( 'NONE', #54215, 1000.000000000000000 ) ;
#53836=CARTESIAN_POINT ( 'NONE',  ( 5.676582343750005144, 235.5729166700806729, 9.832129032723416984 ) ) ;
#53839=CARTESIAN_POINT ( 'NONE',  ( 5.676582343749997150, 222.5520833367473017, -9.832129032723418760 ) ) ;
#53871=CARTESIAN_POINT ( 'NONE',  ( 10.00000000000000000, 232.5000000000000000, -1.224646799147353256E-15 ) ) ;
#53892=CARTESIAN_POINT ( 'NONE',  ( -6.123233995736766282E-16, 263.7500000000000568, -10.00000000000000000 ) ) ;
#53896=CARTESIAN_POINT ( 'NONE',  ( 2.679491924311225848, 241.6666666734946318, -10.00000000000000000 ) ) ;
#53909=CARTESIAN_POINT ( 'NONE',  ( 0.000000000000000000, 0.000000000000000000, 0.000000000000000000 ) ) ;
#53919=DIRECTION ( 'NONE',  ( 0.000000000000000000, 0.000000000000000000, -1.000000000000000000 ) ) ;
#53943=CARTESIAN_POINT ( 'NONE',  ( -8.311093377946836114, 228.5937500034139873, -8.311093377946836114 ) ) ;
#53980=CARTESIAN_POINT ( 'NONE',  ( -5.676582343750000703, 238.0729166700806445, -9.832129032723418760 ) ) ;
#54032=CARTESIAN_POINT ( 'NONE',  ( 1.836970198721029589E-15, 226.2500000000000000, 10.00000000000000000 ) ) ;
#54118=CARTESIAN_POINT ( 'NONE',  ( 5.676582343750005144, 235.5729166700806729, 9.832129032723416984 ) ) ;
#54122=FACE_OUTER_BOUND ( 'NONE', #70390, .T. ) ;
#54155=CARTESIAN_POINT ( 'NONE',  ( -11.35316468749999608, 224.4270833367473017, 3.042071309553173730 ) ) ;
#54180=ORIENTED_EDGE ( 'NONE', *, *, #21981, .F. ) ;
#54212=CARTESIAN_POINT ( 'NONE',  ( 3.042071309553163960, 232.7604166700806445, -11.35316468749999785 ) ) ;
#54213=AXIS2_PLACEMENT_3D ( 'NONE', #71250, #36937, #53919 ) ;
#54215=DIRECTION ( 'NONE',  ( -0.000000000000000000, -1.000000000000000000, -0.000000000000000000 ) ) ;
#54273=CARTESIAN_POINT ( 'NONE',  ( -6.123233995736766282E-16, 241.8750000068280031, -10.00000000000000000 ) ) ;
#54357=CARTESIAN_POINT ( 'NONE',  ( -8.311093377946836114, 228.2812500034140157, -8.311093377946836114 ) ) ;
#54409=CARTESIAN_POINT ( 'NONE',  ( 5.676582343750005144, 255.8854166700806445, 9.832129032723416984 ) ) ;
#54417=CARTESIAN_POINT ( 'NONE',  ( 7.320508075688776373, 241.8749999999999716, 7.320508075688767491 ) ) ;
#54494=CARTESIAN_POINT ( 'NONE',  ( -5.000000000000000888, 254.1666666666666572, -8.660254037844387298 ) ) ;
#54496=CARTESIAN_POINT ( 'NONE',  ( 9.832129032723420536, 230.9895833367473301, 5.676582343749996262 ) ) ;
#54501=CARTESIAN_POINT ( 'NONE',  ( -7.320508075688770155, 260.6249999999999432, 7.320508075688774596 ) ) ;
#54526=CARTESIAN_POINT ( 'NONE',  ( 11.35316468749999608, 231.9270833367473301, -3.042071309553167513 ) ) ;
#54551=CARTESIAN_POINT ( 'NONE',  ( 2.679491924311306672, 244.5833333401612606, 9.999999999999957367 ) ) ;
#54555=CARTESIAN_POINT ( 'NONE',  ( -10.00000000000000000, 264.0625000034140157, 0.000000000000000000 ) ) ;
#54586=CARTESIAN_POINT ( 'NONE',  ( 8.311093377946834337, 227.3437500034140157, -8.311093377946836114 ) ) ;
#54645=CARTESIAN_POINT ( 'NONE',  ( -10.00000000000000000, 237.9166666734946602, -2.679491924311226292 ) ) ;
#54666=CARTESIAN_POINT ( 'NONE',  ( 8.311093377946834337, 257.0312500034139020, -8.311093377946836114 ) ) ;
#54669=CARTESIAN_POINT ( 'NONE',  ( -8.311093377946836114, 263.5937500034140157, -8.311093377946836114 ) ) ;
#54694=DIRECTION ( 'NONE',  ( -0.000000000000000000, -1.000000000000000000, -0.000000000000000000 ) ) ;
#54734=CARTESIAN_POINT ( 'NONE',  ( -11.35316468749999785, 238.6979166700806729, -3.042071309553164848 ) ) ;
#54780=CARTESIAN_POINT ( 'NONE',  ( -11.35316468749999785, 254.0104166700806729, -3.042071309553164848 ) ) ;
#54825=DIRECTION ( 'NONE',  ( -0.000000000000000000, -1.000000000000000000, -0.000000000000000000 ) ) ;
#54844=EDGE_LOOP ( 'NONE', ( #29881, #67703, #18141, #14418, #11770, #74025 ) ) ;
#54852=LINE ( 'NONE', #50295, #31314 ) ;
#54863=CARTESIAN_POINT ( 'NONE',  ( -9.999999999999998224, 255.2083333333333712, 2.679491924311235174 ) ) ;
#54867=CARTESIAN_POINT ( 'NONE',  ( -11.35316468749999608, 224.1145833367473301, 3.042071309553173730 ) ) ;
#54873=CARTESIAN_POINT ( 'NONE',  ( -4.999999999999992895, 250.8333333333333428, 8.660254037844390851 ) ) ;
#54902=CARTESIAN_POINT ( 'NONE',  ( -8.311093377946836114, 228.5937500034139873, -8.311093377946836114 ) ) ;
#54915=CARTESIAN_POINT ( 'NONE',  ( 8.660254037844385522, 257.9166666666666856, -5.000000000000003553 ) ) ;
#54958=CARTESIAN_POINT ( 'NONE',  ( -3.042071309553166181, 228.1770833367473301, -11.35316468749999608 ) ) ;
#55020=CARTESIAN_POINT ( 'NONE',  ( -7.320508075688770155, 243.7500000068279462, 7.320508075688774596 ) ) ;
#55041=CARTESIAN_POINT ( 'NONE',  ( -8.311093377946836114, 253.2812500034140442, -8.311093377946836114 ) ) ;
#55064=CARTESIAN_POINT ( 'NONE',  ( -7.320508075688770155, 243.7500000068279462, 7.320508075688774596 ) ) ;
#55095=ORIENTED_EDGE ( 'NONE', *, *, #52927, .T. ) ;
#55107=CARTESIAN_POINT ( 'NONE',  ( 3.042071309553163960, 237.4479166700806729, -11.35316468749999785 ) ) ;
#55137=ORIENTED_EDGE ( 'NONE', *, *, #47649, .T. ) ;
#55156=LINE ( 'NONE', #44201, #52827 ) ;
#55159=CARTESIAN_POINT ( 'NONE',  ( 8.311093377946839666, 261.0937500034140157, 8.311093377946829008 ) ) ;
#55248=CARTESIAN_POINT ( 'NONE',  ( -10.00000000000000000, 245.0000000000000284, 0.000000000000000000 ) ) ;
#55299=CARTESIAN_POINT ( 'NONE',  ( 10.00000000000000178, 245.4166666734946318, 2.679491924311222739 ) ) ;
#55320=ADVANCED_FACE ( 'NONE', ( #47551 ), #827, .F. ) ;
#55329=CARTESIAN_POINT ( 'NONE',  ( 2.085542519210945334E-15, 220.1562500034139873, 11.35316468749999963 ) ) ;
#55332=CARTESIAN_POINT ( 'NONE',  ( 11.35316468749999608, 251.6145833367473585, -3.042071309553167069 ) ) ;
#55335=CYLINDRICAL_SURFACE ( 'NONE', #65873, 10.00000000000000000 ) ;
#55337=( BOUNDED_SURFACE ( )  B_SPLINE_SURFACE ( 1, 2, ( 
 ( #67989, #50258, #17042, #10280, #5369, #28736, #39689, #61954, #56684, #100, #27620, #34059, #74389, #73280, #62688, #50629, #10649, #4254, #5002, #68728, #21955, #22698, #9906, #11027, #32938, #15920, #15549, #44610, #67625, #51753, #73648, #16284, #51377, #33681, #45717, #51009, #40066, #63071, #67254, #39324, #11394, #38951, #34429, #55944, #27242, #6846, #46088, #40437, #29119, #29492, #69107, #57808, #24186, #52501, #17415, #469, #58913, #30595, #35167, #24556, #23825, #13227, #64918, #7588, #6113, #52873, #7223, #30226, #52137, #47199, #12857, #18903, #29861, #58182, #36263, #53246, #63437, #70229, #839, #35896, #41183, #1205, #11764, #34802, #1576, #47563, #23450, #64193, #70586, #6487, #46462, #69481, #18538, #17792, #40805, #63815, #12129, #41546, #59279, #41910, #53614, #1927, #46830, #69856, #18168, #12498, #35529, #58541, #64562, #66405, #25287, #20372, #2290, #15088, #66032, #48304, #60751, #14338, #32469, #72446, #19264, #54734, #36632, #2667, #53980, #38123, #71681, #55107, #49427, #37370, #42276, #19632, #71313, #14713, #42646, #65658, #31711, #70948, #13955, #36997, #47931, #55479, #65289, #9074, #32086, #60002, #25658, #43389, #20001, #3041, #43011, #49047, #26024, #72055, #31330, #37751, #66784, #60371, #24915, #20755, #13594, #3414, #59639, #48674, #8319, #61122, #8697, #26399, #43770, #9453, #7956, #54357, #30959, #45266, #73194, #21502, #10564, #49806, #32848, #15833, #26790, #34344, #72822, #39609, #10938, #55855, #56223, #73933, #73560, #33595, #50544, #27911, #4917, #56601, #10194, #50921, #45633, #67904, #38867, #33224, #22237, #21870, #68276, #16198, #39237, #62607, #3791, #67536, #16572, #4172, #33974, #56971, #22612, #62237, #21129, #44149, #61499 ),
 ( #5286, #11310, #28287, #67165, #44521, #62988, #15460, #51293, #27159, #68647, #74306, #44898, #16958, #39981, #38497, #9822, #50176, #61873, #4537, #27532, #17702, #41826, #7134, #12776, #58823, #57343, #18079, #70145, #69765, #41095, #34711, #12413, #64837, #35810, #28653, #18452, #6404, #64103, #46378, #29409, #69025, #70504, #52418, #18823, #47107, #35080, #40348, #30142, #384, #41465, #13139, #6766, #52047, #46742, #5654, #23364, #24097, #64479, #63350, #29770, #40719, #753, #17327, #29028, #51668, #69393, #63725, #11, #57719, #22999, #12047, #11675, #46005, #6024, #58092, #24475, #23737, #53158, #52784, #35447, #1121, #58458, #1492, #47480, #65947, #43684, #14253, #53529, #30877, #20666, #1846, #37289, #65195, #55020, #60282, #2583, #8608, #42925, #7504, #49338, #66696, #30510, #54273, #53896, #71224, #36174, #60664, #66320, #37665, #59194, #71595, #48959, #48586, #19917, #13506, #31623, #24832, #14625, #47849, #71970, #59922, #54645, #25203, #8236, #70869, #72354, #31247, #19181, #25942, #13870, #42183, #8985, #2208, #20284, #36545, #2952, #48216, #25572, #59556, #19544, #43305, #32001, #7872, #3328, #42562, #26316, #65573, #36914, #16486, #44434, #45177, #32379, #39148, #55394, #38410, #38036, #67074, #44064, #28194, #10847, #62520, #22150, #21411, #62152, #67448, #21040, #56509, #61035, #22521, #45541, #4825, #15745, #21779, #67819, #33881, #55767, #44806, #56138, #14998, #9360, #61411, #51205, #4084, #4448, #38784, #10475, #3703, #61787, #27823, #16111, #27439, #10106, #33506, #33143, #50832, #50455, #73470, #73843, #26701, #27077, #68190, #15373, #39523, #56881, #5197, #74216, #49721, #72737, #9737, #73104, #32759, #50090, #46660, #297, #68559, #22905, #6682 ) ),
 .UNSPECIFIED., .F., .F., .T. ) 
 B_SPLINE_SURFACE_WITH_KNOTS ( ( 2, 2 ),
 ( 3, 2, 2, 2, 2, 2, 2, 2, 2, 2, 2, 2, 2, 2, 2, 2, 2, 2, 2, 2, 2, 2, 2, 2, 2, 2, 2, 2, 2, 2, 2, 2, 2, 2, 2, 2, 2, 2, 2, 2, 2, 2, 2, 2, 2, 2, 2, 2, 2, 2, 2, 2, 2, 2, 2, 2, 2, 2, 2, 2, 2, 2, 2, 2, 2, 2, 2, 2, 2, 2, 2, 2, 2, 2, 2, 2, 2, 2, 2, 2, 2, 2, 2, 2, 2, 2, 2, 2, 2, 2, 2, 2, 2, 2, 2, 2, 2, 2, 2, 2, 2, 2, 2, 2, 2, 2, 2, 2, 3 ),
 ( 0.000000000000000000, 1.000000000000000000 ),
 ( 0.000000000000000000, 0.009259259259259258745, 0.01851851851851851749, 0.02777777777777777624, 0.03703703703703703498, 0.04629629629629629373, 0.05555555555555555247, 0.06481481481481481122, 0.07407407407407406996, 0.08333333333333332871, 0.09259259259259258745, 0.1018518518518518462, 0.1111111111111111049, 0.1203703703703703637, 0.1296296296296296224, 0.1388888888888888951, 0.1481481481481481399, 0.1574074074074074125, 0.1666666666666666574, 0.1759259259259259300, 0.1851851851851851749, 0.1944444444444444475, 0.2037037037037036924, 0.2129629629629629650, 0.2222222222222222099, 0.2314814814814814825, 0.2407407407407407274, 0.2500000000000000000, 0.2592592592592592449, 0.2685185185185185452, 0.2777777777777777901, 0.2870370370370370350, 0.2962962962962962798, 0.3055555555555555802, 0.3148148148148148251, 0.3240740740740740700, 0.3333333333333333148, 0.3425925925925926152, 0.3518518518518518601, 0.3611111111111111049, 0.3703703703703703498, 0.3796296296296296502, 0.3888888888888888951, 0.3981481481481481399, 0.4074074074074073848, 0.4166666666666666852, 0.4259259259259259300, 0.4351851851851851749, 0.4444444444444444198, 0.4537037037037037202, 0.4629629629629629650, 0.4722222222222222099, 0.4814814814814814548, 0.4907407407407407551, 0.5000000000000000000, 0.5092592592592593004, 0.5185185185185184897, 0.5277777777777777901, 0.5370370370370370905, 0.5462962962962962798, 0.5555555555555555802, 0.5648148148148147696, 0.5740740740740740700, 0.5833333333333333703, 0.5925925925925925597, 0.6018518518518518601, 0.6111111111111111605, 0.6203703703703703498, 0.6296296296296296502, 0.6388888888888888395, 0.6481481481481481399, 0.6574074074074074403, 0.6666666666666666297, 0.6759259259259259300, 0.6851851851851852304, 0.6944444444444444198, 0.7037037037037037202, 0.7129629629629629095, 0.7222222222222222099, 0.7314814814814815103, 0.7407407407407406996, 0.7500000000000000000, 0.7592592592592593004, 0.7685185185185184897, 0.7777777777777777901, 0.7870370370370370905, 0.7962962962962962798, 0.8055555555555555802, 0.8148148148148147696, 0.8240740740740740700, 0.8333333333333333703, 0.8425925925925925597, 0.8518518518518518601, 0.8611111111111111605, 0.8703703703703703498, 0.8796296296296296502, 0.8888888888888888395, 0.8981481481481481399, 0.9074074074074074403, 0.9166666666666666297, 0.9259259259259259300, 0.9351851851851852304, 0.9444444444444444198, 0.9537037037037037202, 0.9629629629629629095, 0.9722222222222222099, 0.9814814814814815103, 0.9907407407407406996, 1.000000000000000000 ),
 .UNSPECIFIED. ) 
 GEOMETRIC_REPRESENTATION_ITEM ( )  RATIONAL_B_SPLINE_SURFACE ( (
 ( 1.000000000000000000, 0.9659258262890683122, 1.000000000000000000, 0.9659258262890683122, 1.000000000000000000, 0.9659258262890683122, 1.000000000000000000, 0.9659258262890683122, 1.000000000000000000, 0.9659258262890683122, 1.000000000000000000, 0.9659258262890683122, 1.000000000000000000, 0.9659258262890683122, 1.000000000000000000, 0.9659258262890683122, 1.000000000000000000, 0.9659258262890683122, 1.000000000000000000, 0.9659258262890683122, 1.000000000000000000, 0.9659258262890683122, 1.000000000000000000, 0.9659258262890683122, 1.000000000000000000, 0.9659258262890683122, 1.000000000000000000, 0.9659258262890683122, 1.000000000000000000, 0.9659258262890683122, 1.000000000000000000, 0.9659258262890683122, 1.000000000000000000, 0.9659258262890683122, 1.000000000000000000, 0.9659258262890683122, 1.000000000000000000, 0.9659258262890683122, 1.000000000000000000, 0.9659258262890683122, 1.000000000000000000, 0.9659258262890683122, 1.000000000000000000, 0.9659258262890683122, 1.000000000000000000, 0.9659258262890683122, 1.000000000000000000, 0.9659258262890683122, 1.000000000000000000, 0.9659258262890683122, 1.000000000000000000, 0.9659258262890683122, 1.000000000000000000, 0.9659258262890683122, 1.000000000000000000, 0.9659258262890683122, 1.000000000000000000, 0.9659258262890683122, 1.000000000000000000, 0.9659258262890683122, 1.000000000000000000, 0.9659258262890683122, 1.000000000000000000, 0.9659258262890683122, 1.000000000000000000, 0.9659258262890683122, 1.000000000000000000, 0.9659258262890683122, 1.000000000000000000, 0.9659258262890683122, 1.000000000000000000, 0.9659258262890683122, 1.000000000000000000, 0.9659258262890683122, 1.000000000000000000, 0.9659258262890683122, 1.000000000000000000, 0.9659258262890683122, 1.000000000000000000, 0.9659258262890683122, 1.000000000000000000, 0.9659258262890683122, 1.000000000000000000, 0.9659258262890683122, 1.000000000000000000, 0.9659258262890683122, 1.000000000000000000, 0.9659258262890683122, 1.000000000000000000, 0.9659258262890683122, 1.000000000000000000, 0.9659258262890683122, 1.000000000000000000, 0.9659258262890683122, 1.000000000000000000, 0.9659258262890683122, 1.000000000000000000, 0.9659258262890683122, 1.000000000000000000, 0.9659258262890683122, 1.000000000000000000, 0.9659258262890683122, 1.000000000000000000, 0.9659258262890683122, 1.000000000000000000, 0.9659258262890683122, 1.000000000000000000, 0.9659258262890683122, 1.000000000000000000, 0.9659258262890683122, 1.000000000000000000, 0.9659258262890683122, 1.000000000000000000, 0.9659258262890683122, 1.000000000000000000, 0.9659258262890683122, 1.000000000000000000, 0.9659258262890683122, 1.000000000000000000, 0.9659258262890683122, 1.000000000000000000, 0.9659258262890683122, 1.000000000000000000, 0.9659258262890683122, 1.000000000000000000, 0.9659258262890683122, 1.000000000000000000, 0.9659258262890683122, 1.000000000000000000, 0.9659258262890683122, 1.000000000000000000, 0.9659258262890683122, 1.000000000000000000, 0.9659258262890683122, 1.000000000000000000, 0.9659258262890683122, 1.000000000000000000, 0.9659258262890683122, 1.000000000000000000, 0.9659258262890683122, 1.000000000000000000, 0.9659258262890683122, 1.000000000000000000, 0.9659258262890683122, 1.000000000000000000, 0.9659258262890683122, 1.000000000000000000, 0.9659258262890683122, 1.000000000000000000, 0.9659258262890683122, 1.000000000000000000, 0.9659258262890683122, 1.000000000000000000, 0.9659258262890683122, 1.000000000000000000, 0.9659258262890683122, 1.000000000000000000, 0.9659258262890683122, 1.000000000000000000, 0.9659258262890683122, 1.000000000000000000, 0.9659258262890683122, 1.000000000000000000, 0.9659258262890683122, 1.000000000000000000, 0.9659258262890683122, 1.000000000000000000, 0.9659258262890683122, 1.000000000000000000, 0.9659258262890683122, 1.000000000000000000, 0.9659258262890683122, 1.000000000000000000, 0.9659258262890683122, 1.000000000000000000, 0.9659258262890683122, 1.000000000000000000, 0.9659258262890683122, 1.000000000000000000, 0.9659258262890683122, 1.000000000000000000, 0.9659258262890683122, 1.000000000000000000, 0.9659258262890683122, 1.000000000000000000, 0.9659258262890683122, 1.000000000000000000, 0.9659258262890683122, 1.000000000000000000, 0.9659258262890683122, 1.000000000000000000, 0.9659258262890683122, 1.000000000000000000, 0.9659258262890683122, 1.000000000000000000, 0.9659258262890683122, 1.000000000000000000, 0.9659258262890683122, 1.000000000000000000, 0.9659258262890683122, 1.000000000000000000, 0.9659258262890683122, 1.000000000000000000, 0.9659258262890683122, 1.000000000000000000, 0.9659258262890683122, 1.000000000000000000, 0.9659258262890683122, 1.000000000000000000, 0.9659258262890683122, 1.000000000000000000, 0.9659258262890683122, 1.000000000000000000, 0.9659258262890683122, 1.000000000000000000, 0.9659258262890683122, 1.000000000000000000),
 ( 1.000000000000000000, 0.9659258262890683122, 1.000000000000000000, 0.9659258262890683122, 1.000000000000000000, 0.9659258262890683122, 1.000000000000000000, 0.9659258262890683122, 1.000000000000000000, 0.9659258262890683122, 1.000000000000000000, 0.9659258262890683122, 1.000000000000000000, 0.9659258262890683122, 1.000000000000000000, 0.9659258262890683122, 1.000000000000000000, 0.9659258262890683122, 1.000000000000000000, 0.9659258262890683122, 1.000000000000000000, 0.9659258262890683122, 1.000000000000000000, 0.9659258262890683122, 1.000000000000000000, 0.9659258262890683122, 1.000000000000000000, 0.9659258262890683122, 1.000000000000000000, 0.9659258262890683122, 1.000000000000000000, 0.9659258262890683122, 1.000000000000000000, 0.9659258262890683122, 1.000000000000000000, 0.9659258262890683122, 1.000000000000000000, 0.9659258262890683122, 1.000000000000000000, 0.9659258262890683122, 1.000000000000000000, 0.9659258262890683122, 1.000000000000000000, 0.9659258262890683122, 1.000000000000000000, 0.9659258262890683122, 1.000000000000000000, 0.9659258262890683122, 1.000000000000000000, 0.9659258262890683122, 1.000000000000000000, 0.9659258262890683122, 1.000000000000000000, 0.9659258262890683122, 1.000000000000000000, 0.9659258262890683122, 1.000000000000000000, 0.9659258262890683122, 1.000000000000000000, 0.9659258262890683122, 1.000000000000000000, 0.9659258262890683122, 1.000000000000000000, 0.9659258262890683122, 1.000000000000000000, 0.9659258262890683122, 1.000000000000000000, 0.9659258262890683122, 1.000000000000000000, 0.9659258262890683122, 1.000000000000000000, 0.9659258262890683122, 1.000000000000000000, 0.9659258262890683122, 1.000000000000000000, 0.9659258262890683122, 1.000000000000000000, 0.9659258262890683122, 1.000000000000000000, 0.9659258262890683122, 1.000000000000000000, 0.9659258262890683122, 1.000000000000000000, 0.9659258262890683122, 1.000000000000000000, 0.9659258262890683122, 1.000000000000000000, 0.9659258262890683122, 1.000000000000000000, 0.9659258262890683122, 1.000000000000000000, 0.9659258262890683122, 1.000000000000000000, 0.9659258262890683122, 1.000000000000000000, 0.9659258262890683122, 1.000000000000000000, 0.9659258262890683122, 1.000000000000000000, 0.9659258262890683122, 1.000000000000000000, 0.9659258262890683122, 1.000000000000000000, 0.9659258262890683122, 1.000000000000000000, 0.9659258262890683122, 1.000000000000000000, 0.9659258262890683122, 1.000000000000000000, 0.9659258262890683122, 1.000000000000000000, 0.9659258262890683122, 1.000000000000000000, 0.9659258262890683122, 1.000000000000000000, 0.9659258262890683122, 1.000000000000000000, 0.9659258262890683122, 1.000000000000000000, 0.9659258262890683122, 1.000000000000000000, 0.9659258262890683122, 1.000000000000000000, 0.9659258262890683122, 1.000000000000000000, 0.9659258262890683122, 1.000000000000000000, 0.9659258262890683122, 1.000000000000000000, 0.9659258262890683122, 1.000000000000000000, 0.9659258262890683122, 1.000000000000000000, 0.9659258262890683122, 1.000000000000000000, 0.9659258262890683122, 1.000000000000000000, 0.9659258262890683122, 1.000000000000000000, 0.9659258262890683122, 1.000000000000000000, 0.9659258262890683122, 1.000000000000000000, 0.9659258262890683122, 1.000000000000000000, 0.9659258262890683122, 1.000000000000000000, 0.9659258262890683122, 1.000000000000000000, 0.9659258262890683122, 1.000000000000000000, 0.9659258262890683122, 1.000000000000000000, 0.9659258262890683122, 1.000000000000000000, 0.9659258262890683122, 1.000000000000000000, 0.9659258262890683122, 1.000000000000000000, 0.9659258262890683122, 1.000000000000000000, 0.9659258262890683122, 1.000000000000000000, 0.9659258262890683122, 1.000000000000000000, 0.9659258262890683122, 1.000000000000000000, 0.9659258262890683122, 1.000000000000000000, 0.9659258262890683122, 1.000000000000000000, 0.9659258262890683122, 1.000000000000000000, 0.9659258262890683122, 1.000000000000000000, 0.9659258262890683122, 1.000000000000000000, 0.9659258262890683122, 1.000000000000000000, 0.9659258262890683122, 1.000000000000000000, 0.9659258262890683122, 1.000000000000000000, 0.9659258262890683122, 1.000000000000000000, 0.9659258262890683122, 1.000000000000000000, 0.9659258262890683122, 1.000000000000000000, 0.9659258262890683122, 1.000000000000000000, 0.9659258262890683122, 1.000000000000000000, 0.9659258262890683122, 1.000000000000000000, 0.9659258262890683122, 1.000000000000000000, 0.9659258262890683122, 1.000000000000000000, 0.9659258262890683122, 1.000000000000000000, 0.9659258262890683122, 1.000000000000000000, 0.9659258262890683122, 1.000000000000000000, 0.9659258262890683122, 1.000000000000000000, 0.9659258262890683122, 1.000000000000000000, 0.9659258262890683122, 1.000000000000000000, 0.9659258262890683122, 1.000000000000000000, 0.9659258262890683122, 1.000000000000000000, 0.9659258262890683122, 1.000000000000000000) ) ) 
 REPRESENTATION_ITEM ( '' )  SURFACE ( )  );
#55367=CARTESIAN_POINT ( 'NONE',  ( 8.311093377946839666, 251.0937500034139873, 8.311093377946830785 ) ) ;
#55394=CARTESIAN_POINT ( 'NONE',  ( 7.320508075688771044, 231.2500000068279462, -7.320508075688771932 ) ) ;
#55415=CARTESIAN_POINT ( 'NONE',  ( -4.999999999999992895, 258.9583333401613459, 8.660254037844390851 ) ) ;
#55419=CARTESIAN_POINT ( 'NONE',  ( -11.35316468749999608, 259.4270833367472164, 3.042071309553173730 ) ) ;
#55442=CARTESIAN_POINT ( 'NONE',  ( 11.35316468749999963, 221.7187500034139873, -1.390361679473963556E-15 ) ) ;
#55455=CARTESIAN_POINT ( 'NONE',  ( -2.679491924311081963, 261.0416666666666856, 10.00000000000008171 ) ) ;
#55463=CIRCLE ( 'NONE', #54213, 10.00000000000000000 ) ;
#55479=CARTESIAN_POINT ( 'NONE',  ( -8.311093377946834337, 234.5312500034139589, 8.311093377946837890 ) ) ;
#55535=CARTESIAN_POINT ( 'NONE',  ( 3.042071309553173286, 255.6770833367473301, 11.35316468749999608 ) ) ;
#55545=VERTEX_POINT ( 'NONE', #34080 ) ;
#55576=( BOUNDED_CURVE ( )  B_SPLINE_CURVE ( 2, ( #61902, #44931, #67938, #16232, #32885 ),
 .UNSPECIFIED., .F., .F. ) 
 B_SPLINE_CURVE_WITH_KNOTS ( ( 3, 2, 3 ),
 ( 0.9871528671839122637, 0.9907407407407406996, 1.000000000000000000 ),
 .UNSPECIFIED. ) 
 CURVE ( )  GEOMETRIC_REPRESENTATION_ITEM ( )  RATIONAL_B_SPLINE_CURVE ( ( 0.9838255637299375689, 0.9867965867025509930, 1.000000000000000000, 0.9659258262890683122, 1.000000000000000000 ) ) 
 REPRESENTATION_ITEM ( '' )  );
#55584=CARTESIAN_POINT ( 'NONE',  ( -5.000000000000000888, 247.2916666734946318, -8.660254037844387298 ) ) ;
#55589=DIRECTION ( 'NONE',  ( -0.000000000000000000, -1.000000000000000000, -0.000000000000000000 ) ) ;
#55620=CARTESIAN_POINT ( 'NONE',  ( -8.660254037844387298, 249.5833333333333428, -4.999999999999999112 ) ) ;
#55707=CARTESIAN_POINT ( 'NONE',  ( 8.311093377946834337, 262.0312500034139589, -8.311093377946836114 ) ) ;
#55715=CARTESIAN_POINT ( 'NONE',  ( -5.499999999999992006, 219.5356836093509685, 9.526279441628830114 ) ) ;
#55741=CARTESIAN_POINT ( 'NONE',  ( 11.35316468749999608, 261.9270833367472733, -3.042071309553167513 ) ) ;
#55767=CARTESIAN_POINT ( 'NONE',  ( 2.679491924311225848, 226.6666666734946034, -10.00000000000000000 ) ) ;
#55768=CARTESIAN_POINT ( 'NONE',  ( -5.000000000000000888, 252.2916666734946602, -8.660254037844387298 ) ) ;
#55789=CARTESIAN_POINT ( 'NONE',  ( -6.951808397369817780E-16, 262.6562500034140157, -11.35316468749999963 ) ) ;
#55793=CARTESIAN_POINT ( 'NONE',  ( -9.832129032723415207, 259.6354166700806445, 5.676582343750005144 ) ) ;
#55835=CARTESIAN_POINT ( 'NONE',  ( -10.00000000000000000, 245.0000000000000284, 0.000000000000000000 ) ) ;
#55855=CARTESIAN_POINT ( 'NONE',  ( 3.042071309553173286, 225.3645833367473301, 11.35316468749999608 ) ) ;
#55880=CARTESIAN_POINT ( 'NONE',  ( 10.00000000000000000, 235.6250000068279746, -1.224646799147353256E-15 ) ) ;
#55908=CARTESIAN_POINT ( 'NONE',  ( -3.042071309553159075, 260.2604166700805877, 11.35316468749999963 ) ) ;
#55944=CARTESIAN_POINT ( 'NONE',  ( -3.042071309553159075, 254.9479166700806729, 11.35316468749999963 ) ) ;
#55952=CARTESIAN_POINT ( 'NONE',  ( 7.320508075688771044, 231.2500000068279746, -7.320508075688771932 ) ) ;
#55988=CARTESIAN_POINT ( 'NONE',  ( -11.35316468749999608, 219.1145833367473017, 3.042071309553173730 ) ) ;
#55992=CARTESIAN_POINT ( 'NONE',  ( 10.00000000000000000, 247.5000000000000000, -1.224646799147353256E-15 ) ) ;
#56038=CARTESIAN_POINT ( 'NONE',  ( 4.999999999999997335, 258.3333333333333712, -8.660254037844387298 ) ) ;
#56047=CARTESIAN_POINT ( 'NONE',  ( 10.00000000000000178, 237.2916666666666288, 2.679491924311222739 ) ) ;
#56056=EDGE_CURVE ( 'NONE', #44513, #14535, #54852, .T. ) ;
#56077=CARTESIAN_POINT ( 'NONE',  ( 8.311093377946834337, 257.0312500034139020, -8.311093377946836114 ) ) ;
#56098=EDGE_CURVE ( 'NONE', #26323, #55545, #30166, .T. ) ;
#56111=CARTESIAN_POINT ( 'NONE',  ( -3.042071309553166625, 263.1770833367473301, -11.35316468749999608 ) ) ;
#56136=CARTESIAN_POINT ( 'NONE',  ( 0.000000000000000000, 0.000000000000000000, -10.00000000000000000 ) ) ;
#56138=CARTESIAN_POINT ( 'NONE',  ( 7.320508075688771044, 226.2500000068279746, -7.320508075688771932 ) ) ;
#56159=CARTESIAN_POINT ( 'NONE',  ( -2.679491924311358186, 257.0833333401612890, -9.999999999999923617 ) ) ;
#56160=CARTESIAN_POINT ( 'NONE',  ( 9.832129032723420536, 250.9895833367473017, 5.676582343749996262 ) ) ;
#56163=ORIENTED_EDGE ( 'NONE', *, *, #1329, .F. ) ;
#56164=CARTESIAN_POINT ( 'NONE',  ( 11.35316468749999608, 256.9270833367473301, -3.042071309553167069 ) ) ;
#56223=CARTESIAN_POINT ( 'NONE',  ( 2.085542519210945334E-15, 225.1562500034139873, 11.35316468749999963 ) ) ;
#56237=EDGE_CURVE ( 'NONE', #8879, #50547, #70168, .T. ) ;
#56269=CYLINDRICAL_SURFACE ( 'NONE', #49208, 10.00000000000000000 ) ;
#56271=CARTESIAN_POINT ( 'NONE',  ( -5.676582343749992710, 245.0520833367473301, 9.832129032723422313 ) ) ;
#56307=EDGE_LOOP ( 'NONE', ( #19572, #10781, #11336, #52067, #46670, #50463 ) ) ;
#56358=CARTESIAN_POINT ( 'NONE',  ( -2.679491924311222295, 256.0416666666666856, 10.00000000000000178 ) ) ;
#56368=ORIENTED_EDGE ( 'NONE', *, *, #25585, .F. ) ;
#56387=CARTESIAN_POINT ( 'NONE',  ( 3.042071309553173286, 220.6770833367472733, 11.35316468749999608 ) ) ;
#56444=CARTESIAN_POINT ( 'NONE',  ( -8.311093377946834337, 254.5312500034139873, 8.311093377946837890 ) ) ;
#56463=VERTEX_POINT ( 'NONE', #7894 ) ;
#56464=EDGE_CURVE ( 'NONE', #34088, #5951, #55463, .T. ) ;
#56481=CARTESIAN_POINT ( 'NONE',  ( 11.35316468749999608, 256.9270833367473301, -3.042071309553167513 ) ) ;
#56493=DIRECTION ( 'NONE',  ( -0.000000000000000000, -1.000000000000000000, -0.000000000000000000 ) ) ;
#56509=CARTESIAN_POINT ( 'NONE',  ( -8.660254037844385522, 228.5416666734946602, 5.000000000000004441 ) ) ;
#56522=ADVANCED_FACE ( 'NONE', ( #60308 ), #66449, .T. ) ;
#56532=CARTESIAN_POINT ( 'NONE',  ( -5.676582343750000703, 243.0729166700806445, -9.832129032723418760 ) ) ;
#56537=CARTESIAN_POINT ( 'NONE',  ( 11.35316468749999963, 251.7187500034139873, -1.390361679473963556E-15 ) ) ;
#56577=CARTESIAN_POINT ( 'NONE',  ( -8.660254037844387298, 244.5833333333333428, -4.999999999999999112 ) ) ;
#56583=( BOUNDED_CURVE ( )  B_SPLINE_CURVE ( 2, ( #48095, #42066, #70023, #41344, #1001, #65453, #64354, #18703, #7751, #12657, #35688, #58703, #7014 ),
 .UNSPECIFIED., .F., .F. ) 
 B_SPLINE_CURVE_WITH_KNOTS ( ( 3, 2, 2, 2, 2, 2, 3 ),
 ( 0.5277777777777775681, 0.5370370370370368684, 0.5462962962962960578, 0.5555555555555553582, 0.5648148148148145475, 0.5740740740740738479, 0.5833333333333331483 ),
 .UNSPECIFIED. ) 
 CURVE ( )  GEOMETRIC_REPRESENTATION_ITEM ( )  RATIONAL_B_SPLINE_CURVE ( ( 1.000000000000000888, 0.9659258262890675351, 1.000000000000000000, 0.9659258262890683122, 1.000000000000000000, 0.9659258262890683122, 1.000000000000000000, 0.9659258262890683122, 1.000000000000000000, 0.9659258262890683122, 1.000000000000000000, 0.9659258262890690894, 0.9999999999999992228 ) ) 
 REPRESENTATION_ITEM ( '' )  );
#56601=CARTESIAN_POINT ( 'NONE',  ( -11.35316468749999785, 223.6979166700806445, -3.042071309553164848 ) ) ;
#56623=CARTESIAN_POINT ( 'NONE',  ( 0.000000000000000000, 45.00000000000000000, 0.000000000000000000 ) ) ;
#56626=CARTESIAN_POINT ( 'NONE',  ( 1.836970198721029589E-15, 239.3750000068279746, 10.00000000000000000 ) ) ;
#56643=VECTOR ( 'NONE', #39354, 1000.000000000000000 ) ;
#56650=CARTESIAN_POINT ( 'NONE',  ( -3.042071309553159075, 240.2604166700806729, 11.35316468749999963 ) ) ;
#56668=CARTESIAN_POINT ( 'NONE',  ( -7.320508075688771932, 229.3749999999999716, -7.320508075688771932 ) ) ;
#56684=CARTESIAN_POINT ( 'NONE',  ( 5.676582343749997150, 262.2395833367473301, -9.832129032723418760 ) ) ;
#56695=EDGE_CURVE ( 'NONE', #18027, #50547, #72172, .T. ) ;
#56727=AXIS2_PLACEMENT_3D ( 'NONE', #35763, #29727, #337 ) ;
#56734=CARTESIAN_POINT ( 'NONE',  ( 9.999999999999998224, 242.7083333333333428, -2.679491924311229401 ) ) ;
#56762=CARTESIAN_POINT ( 'NONE',  ( -9.832129032723418760, 223.8020833367473301, -5.676582343749998927 ) ) ;
#56816=CARTESIAN_POINT ( 'NONE',  ( -6.951808397369817780E-16, 252.6562500034140157, -11.35316468749999963 ) ) ;
#56833=ORIENTED_EDGE ( 'NONE', *, *, #15384, .F. ) ;
#56851=CARTESIAN_POINT ( 'NONE',  ( 11.35316468749999963, 251.5104166700806729, 3.042071309553159519 ) ) ;
#56866=ORIENTED_EDGE ( 'NONE', *, *, #61830, .F. ) ;
#56881=CARTESIAN_POINT ( 'NONE',  ( 9.999999999999998224, 220.8333333401613174, -2.679491924311229401 ) ) ;
#56894=CARTESIAN_POINT ( 'NONE',  ( 1.224646799147353256E-15, 265.0000000000000000, 10.00000000000000000 ) ) ;
#56907=CARTESIAN_POINT ( 'NONE',  ( -9.832129032723415207, 249.3229166700806729, 5.676582343750005144 ) ) ;
#56909=SHAPE_DEFINITION_REPRESENTATION ( #68631, #4585 ) ;
#56912=CARTESIAN_POINT ( 'NONE',  ( -11.35316468749999963, 249.2187500034139873, 0.000000000000000000 ) ) ;
#56934=CARTESIAN_POINT ( 'NONE',  ( -10.00000000000000000, 234.7916666666666856, -2.679491924311226292 ) ) ;
#56971=CARTESIAN_POINT ( 'NONE',  ( -3.042071309553159075, 219.9479166700806445, 11.35316468749999963 ) ) ;
#57005=CARTESIAN_POINT ( 'NONE',  ( -7.320508075688771932, 254.3750000000000284, -7.320508075688771932 ) ) ;
#57020=CARTESIAN_POINT ( 'NONE',  ( 3.042071309553173286, 245.6770833367473017, 11.35316468749999608 ) ) ;
#57072=CARTESIAN_POINT ( 'NONE',  ( 0.000000000000000000, 0.000000000000000000, -10.00000000000000000 ) ) ;
#57101=CARTESIAN_POINT ( 'NONE',  ( 7.320508075688771044, 238.1249999999999716, -7.320508075688771932 ) ) ;
#57140=CARTESIAN_POINT ( 'NONE',  ( 2.679491924311139250, 248.5416666666666856, -10.00000000000004796 ) ) ;
#57187=CARTESIAN_POINT ( 'NONE',  ( -11.35316468749999785, 238.6979166700806729, -3.042071309553164848 ) ) ;
#57217=CARTESIAN_POINT ( 'NONE',  ( -9.999999999999998224, 225.2083333333333144, 2.679491924311235174 ) ) ;
#57224=CARTESIAN_POINT ( 'NONE',  ( -8.311093377946834337, 239.8437500034139873, 8.311093377946837890 ) ) ;
#57280=CARTESIAN_POINT ( 'NONE',  ( 5.676582343749997150, 247.2395833367473301, -9.832129032723418760 ) ) ;
#57285=CARTESIAN_POINT ( 'NONE',  ( 5.676582343749997150, 237.5520833367473301, -9.832129032723418760 ) ) ;
#57343=CARTESIAN_POINT ( 'NONE',  ( -10.00000000000000000, 257.9166666734946602, -2.679491924311226292 ) ) ;
#57354=AXIS2_PLACEMENT_3D ( 'NONE', #63097, #11422, #34459 ) ;
#57394=CARTESIAN_POINT ( 'NONE',  ( -9.832129032723418760, 243.8020833367473301, -5.676582343749998927 ) ) ;
#57431=PLANE ( 'NONE',  #63922 ) ;
#57481=CARTESIAN_POINT ( 'NONE',  ( 7.320508075688771044, 253.1250000000000000, -7.320508075688771932 ) ) ;
#57487=CARTESIAN_POINT ( 'NONE',  ( -8.660254037844387298, 239.5833333333333428, -4.999999999999999112 ) ) ;
#57518=AXIS2_PLACEMENT_3D ( 'NONE', #63507, #23143, #21371 ) ;
#57555=CARTESIAN_POINT ( 'NONE',  ( 5.000000000000004441, 249.7916666734946318, 8.660254037844385522 ) ) ;
#57557=ORIENTED_EDGE ( 'NONE', *, *, #13029, .T. ) ;
#57569=CARTESIAN_POINT ( 'NONE',  ( -11.35316468749999963, 243.9062500034140157, 0.000000000000000000 ) ) ;
#57588=VECTOR ( 'NONE', #40776, 1000.000000000000000 ) ;
#57598=ORIENTED_EDGE ( 'NONE', *, *, #67048, .F. ) ;
#57602=CARTESIAN_POINT ( 'NONE',  ( 2.085542519210945334E-15, 250.4687500034140157, 11.35316468749999963 ) ) ;
#57635=EDGE_CURVE ( 'NONE', #41296, #52445, #25019, .T. ) ;
#57657=CARTESIAN_POINT ( 'NONE',  ( 3.042071309553173286, 250.3645833367473301, 11.35316468749999608 ) ) ;
#57661=CARTESIAN_POINT ( 'NONE',  ( -9.832129032723415207, 234.6354166700806445, 5.676582343750005144 ) ) ;
#57719=CARTESIAN_POINT ( 'NONE',  ( -4.999999999999992895, 248.9583333401613174, 8.660254037844390851 ) ) ;
#57769=CARTESIAN_POINT ( 'NONE',  ( 11.35316468749999963, 241.5104166700806729, 3.042071309553159519 ) ) ;
#57808=CARTESIAN_POINT ( 'NONE',  ( -8.311093377946836114, 253.2812500034139873, -8.311093377946836114 ) ) ;
#57824=EDGE_CURVE ( 'NONE', #5951, #34088, #35011, .T. ) ;
#57857=CARTESIAN_POINT ( 'NONE',  ( -6.123233995736766282E-16, 238.7500000000000284, -10.00000000000000000 ) ) ;
#57865=CARTESIAN_POINT ( 'NONE',  ( -4.999999999999992895, 228.9583333401612890, 8.660254037844390851 ) ) ;
#57918=( BOUNDED_CURVE ( )  B_SPLINE_CURVE ( 2, ( #42946, #15395, #25960, #48979, #38807, #14647, #55789, #37307, #60304, #71993, #65966, #38432, #50113, #44087, #14271, #26338, #33163, #3724, #8633, #31646, #60687, #9382, #72760, #25595, #4105, #48610, #71616, #37687, #61435, #32400, #20687, #44458, #67098, #54666, #2975, #61808, #43324, #20305, #26723, #72376, #73129, #66339, #21435, #67472, #9762, #15769, #32021, #32782, #43706, #27098, #9007, #55041, #3347, #49359, #66720, #15024, #38059, #11615, #5219, #16131, #10498, #4474, #56160, #34277, #28220, #57657, #39914, #51230, #62921, #33532, #56907, #45945, #50855, #40660, #63664, #45200, #74241, #5963, #11247, #22547, #57280, #27464, #50478, #33908, #73493, #21800, #28966, #44831, #68958, #4850, #67840, #16891, #39170, #73870, #45569, #16507, #10872, #68583, #63288, #5595, #56532, #28592, #51603, #62173, #11988, #74618, #27847, #22934, #17268, #22176, #40287, #68211, #34652, #51986, #62543, #39548, #324, #23302, #46316, #69330, #17641, #6345, #48154, #24040, #6706, #7074, #42498, #1432, #52727, #47784, #71163, #59136, #58764, #23678, #1061, #69707, #53836, #29714, #47050, #30080, #7444, #70085, #13446, #18020, #41038, #58401, #52356, #70804, #7810, #1786, #694, #53098, #65513, #36114, #46683, #64045, #18392, #35023, #19483, #41404, #2145, #58036, #29349, #64418, #19118, #41768, #24415, #25138, #30452, #12355, #35389, #12715, #35747, #47420, #53468, #70445, #30812, #18761, #24771, #64776, #13079, #42123, #65135, #36483, #59497, #60972, #9292, #20598, #50023, #66254, #2887, #3634, #65879, #43997, #37596, #48523, #42860, #26252, #36853, #13808, #66626, #8920, #31932, #14932, #25510, #31184, #61349, #59860, #73039, #32315, #55329, #71529, #15305, #37973, #19856, #9675, #32696 ),
 .UNSPECIFIED., .F., .F. ) 
 B_SPLINE_CURVE_WITH_KNOTS ( ( 3, 2, 2, 2, 2, 2, 2, 2, 2, 2, 2, 2, 2, 2, 2, 2, 2, 2, 2, 2, 2, 2, 2, 2, 2, 2, 2, 2, 2, 2, 2, 2, 2, 2, 2, 2, 2, 2, 2, 2, 2, 2, 2, 2, 2, 2, 2, 2, 2, 2, 2, 2, 2, 2, 2, 2, 2, 2, 2, 2, 2, 2, 2, 2, 2, 2, 2, 2, 2, 2, 2, 2, 2, 2, 2, 2, 2, 2, 2, 2, 2, 2, 2, 2, 2, 2, 2, 2, 2, 2, 2, 2, 2, 2, 2, 2, 2, 2, 2, 2, 2, 2, 2, 2, 2, 2, 2, 2, 3 ),
 ( 0.000000000000000000, 0.009259259259259258745, 0.01851851851851851749, 0.02777777777777777624, 0.03703703703703703498, 0.04629629629629629373, 0.05555555555555555247, 0.06481481481481481122, 0.07407407407407406996, 0.08333333333333332871, 0.09259259259259258745, 0.1018518518518518462, 0.1111111111111111049, 0.1203703703703703637, 0.1296296296296296224, 0.1388888888888888951, 0.1481481481481481399, 0.1574074074074074125, 0.1666666666666666574, 0.1759259259259259300, 0.1851851851851851749, 0.1944444444444444475, 0.2037037037037036924, 0.2129629629629629650, 0.2222222222222222099, 0.2314814814814814825, 0.2407407407407407274, 0.2500000000000000000, 0.2592592592592592449, 0.2685185185185185452, 0.2777777777777777901, 0.2870370370370370350, 0.2962962962962962798, 0.3055555555555555802, 0.3148148148148148251, 0.3240740740740740700, 0.3333333333333333148, 0.3425925925925926152, 0.3518518518518518601, 0.3611111111111111049, 0.3703703703703703498, 0.3796296296296296502, 0.3888888888888888951, 0.3981481481481481399, 0.4074074074074073848, 0.4166666666666666852, 0.4259259259259259300, 0.4351851851851851749, 0.4444444444444444198, 0.4537037037037037202, 0.4629629629629629650, 0.4722222222222222099, 0.4814814814814814548, 0.4907407407407407551, 0.5000000000000000000, 0.5092592592592593004, 0.5185185185185184897, 0.5277777777777777901, 0.5370370370370370905, 0.5462962962962962798, 0.5555555555555555802, 0.5648148148148147696, 0.5740740740740740700, 0.5833333333333333703, 0.5925925925925925597, 0.6018518518518518601, 0.6111111111111111605, 0.6203703703703703498, 0.6296296296296296502, 0.6388888888888888395, 0.6481481481481481399, 0.6574074074074074403, 0.6666666666666666297, 0.6759259259259259300, 0.6851851851851852304, 0.6944444444444444198, 0.7037037037037037202, 0.7129629629629629095, 0.7222222222222222099, 0.7314814814814815103, 0.7407407407407406996, 0.7500000000000000000, 0.7592592592592593004, 0.7685185185185184897, 0.7777777777777777901, 0.7870370370370370905, 0.7962962962962962798, 0.8055555555555555802, 0.8148148148148147696, 0.8240740740740740700, 0.8333333333333333703, 0.8425925925925925597, 0.8518518518518518601, 0.8611111111111111605, 0.8703703703703703498, 0.8796296296296296502, 0.8888888888888888395, 0.8981481481481481399, 0.9074074074074074403, 0.9166666666666666297, 0.9259259259259259300, 0.9351851851851852304, 0.9444444444444444198, 0.9537037037037037202, 0.9629629629629629095, 0.9722222222222222099, 0.9814814814814815103, 0.9907407407407406996, 1.000000000000000000 ),
 .UNSPECIFIED. ) 
 CURVE ( )  GEOMETRIC_REPRESENTATION_ITEM ( )  RATIONAL_B_SPLINE_CURVE ( ( 1.000000000000000000, 0.9659258262890683122, 1.000000000000000000, 0.9659258262890683122, 1.000000000000000000, 0.9659258262890683122, 1.000000000000000000, 0.9659258262890683122, 1.000000000000000000, 0.9659258262890683122, 1.000000000000000000, 0.9659258262890683122, 1.000000000000000000, 0.9659258262890683122, 1.000000000000000000, 0.9659258262890683122, 1.000000000000000000, 0.9659258262890683122, 1.000000000000000000, 0.9659258262890683122, 1.000000000000000000, 0.9659258262890683122, 1.000000000000000000, 0.9659258262890683122, 1.000000000000000000, 0.9659258262890683122, 1.000000000000000000, 0.9659258262890683122, 1.000000000000000000, 0.9659258262890683122, 1.000000000000000000, 0.9659258262890683122, 1.000000000000000000, 0.9659258262890683122, 1.000000000000000000, 0.9659258262890683122, 1.000000000000000000, 0.9659258262890683122, 1.000000000000000000, 0.9659258262890683122, 1.000000000000000000, 0.9659258262890683122, 1.000000000000000000, 0.9659258262890683122, 1.000000000000000000, 0.9659258262890683122, 1.000000000000000000, 0.9659258262890683122, 1.000000000000000000, 0.9659258262890683122, 1.000000000000000000, 0.9659258262890683122, 1.000000000000000000, 0.9659258262890683122, 1.000000000000000000, 0.9659258262890683122, 1.000000000000000000, 0.9659258262890683122, 1.000000000000000000, 0.9659258262890683122, 1.000000000000000000, 0.9659258262890683122, 1.000000000000000000, 0.9659258262890683122, 1.000000000000000000, 0.9659258262890683122, 1.000000000000000000, 0.9659258262890683122, 1.000000000000000000, 0.9659258262890683122, 1.000000000000000000, 0.9659258262890683122, 1.000000000000000000, 0.9659258262890683122, 1.000000000000000000, 0.9659258262890683122, 1.000000000000000000, 0.9659258262890683122, 1.000000000000000000, 0.9659258262890683122, 1.000000000000000000, 0.9659258262890683122, 1.000000000000000000, 0.9659258262890683122, 1.000000000000000000, 0.9659258262890683122, 1.000000000000000000, 0.9659258262890683122, 1.000000000000000000, 0.9659258262890683122, 1.000000000000000000, 0.9659258262890683122, 1.000000000000000000, 0.9659258262890683122, 1.000000000000000000, 0.9659258262890683122, 1.000000000000000000, 0.9659258262890683122, 1.000000000000000000, 0.9659258262890683122, 1.000000000000000000, 0.9659258262890683122, 1.000000000000000000, 0.9659258262890683122, 1.000000000000000000, 0.9659258262890683122, 1.000000000000000000, 0.9659258262890683122, 1.000000000000000000, 0.9659258262890683122, 1.000000000000000000, 0.9659258262890683122, 1.000000000000000000, 0.9659258262890683122, 1.000000000000000000, 0.9659258262890683122, 1.000000000000000000, 0.9659258262890683122, 1.000000000000000000, 0.9659258262890683122, 1.000000000000000000, 0.9659258262890683122, 1.000000000000000000, 0.9659258262890683122, 1.000000000000000000, 0.9659258262890683122, 1.000000000000000000, 0.9659258262890683122, 1.000000000000000000, 0.9659258262890683122, 1.000000000000000000, 0.9659258262890683122, 1.000000000000000000, 0.9659258262890683122, 1.000000000000000000, 0.9659258262890683122, 1.000000000000000000, 0.9659258262890683122, 1.000000000000000000, 0.9659258262890683122, 1.000000000000000000, 0.9659258262890683122, 1.000000000000000000, 0.9659258262890683122, 1.000000000000000000, 0.9659258262890683122, 1.000000000000000000, 0.9659258262890683122, 1.000000000000000000, 0.9659258262890683122, 1.000000000000000000, 0.9659258262890683122, 1.000000000000000000, 0.9659258262890683122, 1.000000000000000000, 0.9659258262890683122, 1.000000000000000000, 0.9659258262890683122, 1.000000000000000000, 0.9659258262890683122, 1.000000000000000000, 0.9659258262890683122, 1.000000000000000000, 0.9659258262890683122, 1.000000000000000000, 0.9659258262890683122, 1.000000000000000000, 0.9659258262890683122, 1.000000000000000000, 0.9659258262890683122, 1.000000000000000000, 0.9659258262890683122, 1.000000000000000000, 0.9659258262890683122, 1.000000000000000000, 0.9659258262890683122, 1.000000000000000000, 0.9659258262890683122, 1.000000000000000000, 0.9659258262890683122, 1.000000000000000000, 0.9659258262890683122, 1.000000000000000000, 0.9659258262890683122, 1.000000000000000000, 0.9659258262890683122, 1.000000000000000000, 0.9659258262890683122, 1.000000000000000000, 0.9659258262890683122, 1.000000000000000000, 0.9659258262890683122, 1.000000000000000000, 0.9659258262890683122, 1.000000000000000000, 0.9659258262890683122, 1.000000000000000000, 0.9659258262890683122, 1.000000000000000000, 0.9659258262890683122, 1.000000000000000000, 0.9659258262890683122, 1.000000000000000000, 0.9659258262890683122, 1.000000000000000000, 0.9659258262890683122, 1.000000000000000000, 0.9659258262890683122, 1.000000000000000000, 0.9659258262890683122, 1.000000000000000000, 0.9659258262890683122, 1.000000000000000000, 0.9659258262890683122, 1.000000000000000000, 0.9659258262890683122, 1.000000000000000000 ) ) 
 REPRESENTATION_ITEM ( '' )  );
#57926=ORIENTED_EDGE ( 'NONE', *, *, #7880, .T. ) ;
#57948=CARTESIAN_POINT ( 'NONE',  ( 11.35316468749999963, 246.1979166700806445, 3.042071309553159519 ) ) ;
#57984=CARTESIAN_POINT ( 'NONE',  ( 11.35316468749999963, 246.5104166700806445, 3.042071309553159519 ) ) ;
#58036=CARTESIAN_POINT ( 'NONE',  ( 3.042071309553173286, 230.3645833367473017, 11.35316468749999608 ) ) ;
#58038=CARTESIAN_POINT ( 'NONE',  ( -5.676582343749992710, 240.0520833367473301, 9.832129032723422313 ) ) ;
#58092=CARTESIAN_POINT ( 'NONE',  ( -8.660254037844387298, 247.7083333401613174, -4.999999999999999112 ) ) ;
#58144=CARTESIAN_POINT ( 'NONE',  ( -7.320508075688770155, 250.6249999999999432, 7.320508075688774596 ) ) ;
#58146=CARTESIAN_POINT ( 'NONE',  ( 5.676582343750005144, 225.8854166700806729, 9.832129032723416984 ) ) ;
#58161=EDGE_CURVE ( 'NONE', #41296, #21159, #35465, .T. ) ;
#58172=DIRECTION ( 'NONE',  ( -0.000000000000000000, -1.000000000000000000, -0.000000000000000000 ) ) ;
#58182=CARTESIAN_POINT ( 'NONE',  ( -11.35316468749999785, 248.6979166700806445, -3.042071309553164848 ) ) ;
#58229=CARTESIAN_POINT ( 'NONE',  ( -6.123233995736766282E-16, 253.7500000000000284, -10.00000000000000000 ) ) ;
#58234=CARTESIAN_POINT ( 'NONE',  ( -2.679491924311222295, 241.0416666666666288, 10.00000000000000178 ) ) ;
#58250=DIRECTION ( 'NONE',  ( -0.000000000000000000, -1.000000000000000000, -0.000000000000000000 ) ) ;
#58260=CARTESIAN_POINT ( 'NONE',  ( 0.000000000000000000, 0.000000000000000000, -10.00000000000000000 ) ) ;
#58314=CARTESIAN_POINT ( 'NONE',  ( 9.832129032723416984, 241.8229166700806445, -5.676582343750003368 ) ) ;
#58332=EDGE_CURVE ( 'NONE', #5036, #9311, #5222, .T. ) ;
#58349=CARTESIAN_POINT ( 'NONE',  ( -8.311093377946834337, 249.8437500034139589, 8.311093377946837890 ) ) ;
#58376=AXIS2_PLACEMENT_3D ( 'NONE', #53909, #14640, #8628 ) ;
#58401=CARTESIAN_POINT ( 'NONE',  ( -11.35316468749999785, 233.6979166700806445, -3.042071309553164848 ) ) ;
#58403=ORIENTED_EDGE ( 'NONE', *, *, #12160, .T. ) ;
#58405=CARTESIAN_POINT ( 'NONE',  ( -11.35316468749999963, 239.2187500034139873, 0.000000000000000000 ) ) ;
#58454=PLANE ( 'NONE',  #44366 ) ;
#58458=CARTESIAN_POINT ( 'NONE',  ( 7.320508075688771044, 246.2500000068279746, -7.320508075688771932 ) ) ;
#58477=CIRCLE ( 'NONE', #12625, 8.749999999999998224 ) ;
#58504=CARTESIAN_POINT ( 'NONE',  ( 5.676582343749997150, 232.5520833367473301, -9.832129032723418760 ) ) ;
#58535=CARTESIAN_POINT ( 'NONE',  ( 2.679491924311306672, 246.4583333333333144, 9.999999999999957367 ) ) ;
#58541=CARTESIAN_POINT ( 'NONE',  ( 11.35316468749999608, 241.6145833367473585, -3.042071309553167069 ) ) ;
#58546=EDGE_CURVE ( 'NONE', #41315, #33033, #33818, .T. ) ;
#58591=CARTESIAN_POINT ( 'NONE',  ( -7.320508075688770155, 230.6250000000000284, 7.320508075688774596 ) ) ;
#58601=VERTEX_POINT ( 'NONE', #53653 ) ;
#58612=EDGE_CURVE ( 'NONE', #39173, #14438, #18940, .T. ) ;
#58675=CARTESIAN_POINT ( 'NONE',  ( 11.35316468749999608, 246.6145833367472733, -3.042071309553167069 ) ) ;
#58680=CARTESIAN_POINT ( 'NONE',  ( 2.679491924311225848, 258.5416666666666856, -10.00000000000000000 ) ) ;
#58703=CARTESIAN_POINT ( 'NONE',  ( -2.679491924311287132, 237.0833333401613743, -9.999999999999968026 ) ) ;
#58706=CARTESIAN_POINT ( 'NONE',  ( 10.00000000000000000, 220.6250000068279746, -1.224646799147353256E-15 ) ) ;
#58709=CARTESIAN_POINT ( 'NONE',  ( -9.832129032723415207, 249.6354166700806445, 5.676582343750005144 ) ) ;
#58764=CARTESIAN_POINT ( 'NONE',  ( 11.35316468749999963, 236.4062500034140157, -1.390361679473963556E-15 ) ) ;
#58769=CARTESIAN_POINT ( 'NONE',  ( -8.311093377946834337, 244.8437500034140157, 8.311093377946837890 ) ) ;
#58823=CARTESIAN_POINT ( 'NONE',  ( -10.00000000000000000, 258.1250000068279746, 0.000000000000000000 ) ) ;
#58827=APPLICATION_CONTEXT ( 'automotive_design' ) ;
#58844=DIRECTION ( 'NONE',  ( -0.000000000000000000, -1.000000000000000000, -0.000000000000000000 ) ) ;
#58871=CARTESIAN_POINT ( 'NONE',  ( -2.679491924311121043, 251.0416666666666572, 10.00000000000005862 ) ) ;
#58873=CARTESIAN_POINT ( 'NONE',  ( -5.676582343750000703, 228.3854166700806729, -9.832129032723418760 ) ) ;
#58913=CARTESIAN_POINT ( 'NONE',  ( 5.676582343749997150, 252.2395833367473301, -9.832129032723418760 ) ) ;
#58962=CARTESIAN_POINT ( 'NONE',  ( -11.35316468749999785, 264.0104166700807014, -3.042071309553164848 ) ) ;
#58969=CARTESIAN_POINT ( 'NONE',  ( 2.679491924311168560, 243.5416666666666856, -10.00000000000003375 ) ) ;
#58973=AXIS2_PLACEMENT_3D ( 'NONE', #45615, #28637, #51651 ) ;
#59037=CARTESIAN_POINT ( 'NONE',  ( 10.00000000000000178, 255.4166666734946602, 2.679491924311222739 ) ) ;
#59048=CARTESIAN_POINT ( 'NONE',  ( -11.35316468749999963, 233.9062500034139873, 0.000000000000000000 ) ) ;
#59051=CARTESIAN_POINT ( 'NONE',  ( 1.836970198721029589E-15, 261.2500000000000568, 10.00000000000000000 ) ) ;
#59080=CARTESIAN_POINT ( 'NONE',  ( 9.832129032723416984, 232.1354166700806445, -5.676582343750003368 ) ) ;
#59136=CARTESIAN_POINT ( 'NONE',  ( 11.35316468749999608, 236.6145833367473301, -3.042071309553167513 ) ) ;
#59140=CARTESIAN_POINT ( 'NONE',  ( 9.832129032723420536, 231.3020833367473301, 5.676582343749996262 ) ) ;
#59194=CARTESIAN_POINT ( 'NONE',  ( 10.00000000000000178, 240.4166666734946318, 2.679491924311222739 ) ) ;
#59240=CARTESIAN_POINT ( 'NONE',  ( 0.000000000000000000, 0.000000000000000000, 0.000000000000000000 ) ) ;
#59243=CARTESIAN_POINT ( 'NONE',  ( 11.35316468749999963, 231.7187500034139873, -1.390361679473963556E-15 ) ) ;
#59279=CARTESIAN_POINT ( 'NONE',  ( -9.832129032723418760, 243.4895833367473301, -5.676582343749998927 ) ) ;
#59320=AXIS2_PLACEMENT_3D ( 'NONE', #16183, #49795, #4161 ) ;
#59328=CARTESIAN_POINT ( 'NONE',  ( 8.660254037844385522, 222.9166666666666856, -5.000000000000003553 ) ) ;
#59336=CARTESIAN_POINT ( 'NONE',  ( 9.999999999999998224, 242.7083333333333428, -2.679491924311229401 ) ) ;
#59344=FACE_OUTER_BOUND ( 'NONE', #35461, .T. ) ;
#59380=CARTESIAN_POINT ( 'NONE',  ( 1.836970198721029589E-15, 226.2500000000000000, 10.00000000000000000 ) ) ;
#59386=EDGE_LOOP ( 'NONE', ( #3892, #31654, #6608, #39437 ) ) ;
#59395=ORIENTED_EDGE ( 'NONE', *, *, #33260, .F. ) ;
#59409=CARTESIAN_POINT ( 'NONE',  ( 8.311093377946839666, 225.7812500034140157, 8.311093377946829008 ) ) ;
#59444=CARTESIAN_POINT ( 'NONE',  ( -3.042071309553159075, 225.2604166700806161, 11.35316468749999963 ) ) ;
#59468=CARTESIAN_POINT ( 'NONE',  ( 8.660254037844385522, 246.0416666734946318, -5.000000000000003553 ) ) ;
#59497=CARTESIAN_POINT ( 'NONE',  ( 5.676582343750005144, 225.5729166700806729, 9.832129032723416984 ) ) ;
#59500=CARTESIAN_POINT ( 'NONE',  ( 5.676582343750005144, 230.8854166700806729, 9.832129032723416984 ) ) ;
#59556=CARTESIAN_POINT ( 'NONE',  ( 1.836970198721029589E-15, 234.3750000068279746, 10.00000000000000000 ) ) ;
#59603=CARTESIAN_POINT ( 'NONE',  ( 9.832129032723416984, 227.1354166700806729, -5.676582343750003368 ) ) ;
#59639=CARTESIAN_POINT ( 'NONE',  ( 2.085542519210945334E-15, 230.1562500034139873, 11.35316468749999963 ) ) ;
#59692=CARTESIAN_POINT ( 'NONE',  ( -5.000000000000000888, 229.1666666666666856, -8.660254037844387298 ) ) ;
#59700=CARTESIAN_POINT ( 'NONE',  ( 7.320508075688771044, 243.1249999999999716, -7.320508075688771932 ) ) ;
#59718=CYLINDRICAL_SURFACE ( 'NONE', #1246, 11.00000000000000000 ) ;
#59719=DIRECTION ( 'NONE',  ( 0.000000000000000000, 0.000000000000000000, -1.000000000000000000 ) ) ;
#59777=CARTESIAN_POINT ( 'NONE',  ( -5.676582343750000703, 228.0729166700806729, -9.832129032723418760 ) ) ;
#59780=CARTESIAN_POINT ( 'NONE',  ( -4.999999999999992895, 260.8333333333333712, 8.660254037844390851 ) ) ;
#59808=CARTESIAN_POINT ( 'NONE',  ( 3.042071309553163516, 232.7604166700806161, -11.35316468749999785 ) ) ;
#59815=LINE ( 'NONE', #14513, #24485 ) ;
#59860=CARTESIAN_POINT ( 'NONE',  ( 8.311093377946839666, 220.7812500034139873, 8.311093377946830785 ) ) ;
#59864=CARTESIAN_POINT ( 'NONE',  ( 11.35316468749999608, 231.9270833367473585, -3.042071309553167069 ) ) ;
#59866=CARTESIAN_POINT ( 'NONE',  ( 0.000000000000000000, 0.000000000000000000, -10.00000000000000000 ) ) ;
#59922=CARTESIAN_POINT ( 'NONE',  ( -10.00000000000000000, 238.1250000068279746, 0.000000000000000000 ) ) ;
#59961=CARTESIAN_POINT ( 'NONE',  ( -2.679491924311150353, 244.1666666734946887, 10.00000000000004441 ) ) ;
#59965=CARTESIAN_POINT ( 'NONE',  ( 3.042071309553173286, 220.6770833367472733, 11.35316468749999608 ) ) ;
#59981=LINE ( 'NONE', #25636, #60071 ) ;
#60002=CARTESIAN_POINT ( 'NONE',  ( -11.35316468749999785, 233.6979166700806161, -3.042071309553164848 ) ) ;
#60003=ADVANCED_FACE ( 'NONE', ( #20331 ), #37710, .F. ) ;
#60046=CARTESIAN_POINT ( 'NONE',  ( -2.679491924311222295, 221.0416666666667140, 10.00000000000000178 ) ) ;
#60066=CARTESIAN_POINT ( 'NONE',  ( -9.999999999999998224, 230.2083333333333428, 2.679491924311235174 ) ) ;
#60068=( BOUNDED_CURVE ( )  B_SPLINE_CURVE ( 2, ( #48036, #25394, #42378 ),
 .UNSPECIFIED., .F., .T. ) 
 B_SPLINE_CURVE_WITH_KNOTS ( ( 3, 3 ),
 ( 0.02777777777777780052, 0.02886181444060835141 ),
 .UNSPECIFIED. ) 
 CURVE ( )  GEOMETRIC_REPRESENTATION_ITEM ( )  RATIONAL_B_SPLINE_CURVE ( ( 1.000000000000000000, 0.9960107334157028980, 0.9929555612582052770 ) ) 
 REPRESENTATION_ITEM ( '' )  );
#60070=EDGE_CURVE ( 'NONE', #32440, #5866, #47717, .T. ) ;
#60071=VECTOR ( 'NONE', #66381, 1000.000000000000000 ) ;
#60134=CARTESIAN_POINT ( 'NONE',  ( -3.042071309553159075, 224.9479166700806445, 11.35316468749999963 ) ) ;
#60169=CARTESIAN_POINT ( 'NONE',  ( -3.042071309553166625, 233.1770833367472733, -11.35316468749999608 ) ) ;
#60223=CARTESIAN_POINT ( 'NONE',  ( 5.676582343750005144, 225.8854166700806729, 9.832129032723416984 ) ) ;
#60282=CARTESIAN_POINT ( 'NONE',  ( -8.660254037844385522, 243.5416666734946318, 5.000000000000004441 ) ) ;
#60303=CARTESIAN_POINT ( 'NONE',  ( -10.00000000000000000, 258.1250000068279746, 0.000000000000000000 ) ) ;
#60304=CARTESIAN_POINT ( 'NONE',  ( 5.676582343749997150, 262.2395833367473301, -9.832129032723418760 ) ) ;
#60308=FACE_OUTER_BOUND ( 'NONE', #59386, .T. ) ;
#60324=CARTESIAN_POINT ( 'NONE',  ( -5.000000000000000888, 232.2916666734946602, -8.660254037844387298 ) ) ;
#60342=LINE ( 'NONE', #25995, #369 ) ;
#60361=ORIENTED_EDGE ( 'NONE', *, *, #71237, .F. ) ;
#60364=FACE_OUTER_BOUND ( 'NONE', #33185, .T. ) ;
#60371=CARTESIAN_POINT ( 'NONE',  ( 11.35316468749999963, 231.1979166700806161, 3.042071309553159519 ) ) ;
#60398=CARTESIAN_POINT ( 'NONE',  ( 2.679491924311263151, 234.5833333401612890, 9.999999999999980460 ) ) ;
#60406=AXIS2_PLACEMENT_3D ( 'NONE', #64534, #8203, #2549 ) ;
#60423=CARTESIAN_POINT ( 'NONE',  ( -11.35316468749999608, 249.4270833367472733, 3.042071309553173730 ) ) ;
#60506=CARTESIAN_POINT ( 'NONE',  ( 1.836970198721029589E-15, 256.2500000000000568, 10.00000000000000000 ) ) ;
#60509=CARTESIAN_POINT ( 'NONE',  ( -6.951808397369817780E-16, 237.6562500034140157, -11.35316468749999963 ) ) ;
#60514=CARTESIAN_POINT ( 'NONE',  ( -8.660254037844387298, 244.5833333333333428, -4.999999999999999112 ) ) ;
#60538=DIRECTION ( 'NONE',  ( -0.000000000000000000, -1.000000000000000000, -0.000000000000000000 ) ) ;
#60543=CARTESIAN_POINT ( 'NONE',  ( -11.35316468749999608, 234.4270833367473017, 3.042071309553173730 ) ) ;
#60557=CARTESIAN_POINT ( 'NONE',  ( 8.660254037844389075, 257.0833333333333144, 4.999999999999997335 ) ) ;
#60566=CARTESIAN_POINT ( 'NONE',  ( 9.999999999999998224, 245.8333333401612890, -2.679491924311229401 ) ) ;
#60598=ORIENTED_EDGE ( 'NONE', *, *, #29785, .T. ) ;
#60600=CARTESIAN_POINT ( 'NONE',  ( -9.832129032723415207, 229.6354166700806729, 5.676582343750005144 ) ) ;
#60645=CARTESIAN_POINT ( 'NONE',  ( -6.123233995736766282E-16, 251.8750000068280031, -10.00000000000000000 ) ) ;
#60648=CARTESIAN_POINT ( 'NONE',  ( 0.000000000000000000, 0.000000000000000000, 0.000000000000000000 ) ) ;
#60664=CARTESIAN_POINT ( 'NONE',  ( 8.660254037844385522, 241.0416666734946318, -5.000000000000003553 ) ) ;
#60665=CARTESIAN_POINT ( 'NONE',  ( 1.836970198721029589E-15, 254.3750000068280031, 10.00000000000000000 ) ) ;
#60687=CARTESIAN_POINT ( 'NONE',  ( -5.676582343749992710, 259.7395833367473301, 9.832129032723422313 ) ) ;
#60727=CARTESIAN_POINT ( 'NONE',  ( -10.00000000000000000, 259.7916666666666288, -2.679491924311226292 ) ) ;
#60751=CARTESIAN_POINT ( 'NONE',  ( -5.676582343749992710, 239.7395833367473301, 9.832129032723422313 ) ) ;
#60774=CARTESIAN_POINT ( 'NONE',  ( 10.00000000000000178, 235.4166666734946318, 2.679491924311222739 ) ) ;
#60797=CARTESIAN_POINT ( 'NONE',  ( 11.35316468749999608, 256.9270833367473301, -3.042071309553167069 ) ) ;
#60841=LINE ( 'NONE', #3505, #34082 ) ;
#60880=ORIENTED_EDGE ( 'NONE', *, *, #70513, .F. ) ;
#60881=CARTESIAN_POINT ( 'NONE',  ( 8.311093377946839666, 220.7812500034139873, 8.311093377946829008 ) ) ;
#60888=CARTESIAN_POINT ( 'NONE',  ( 10.00000000000000178, 247.2916666666666856, 2.679491924311222739 ) ) ;
#60972=CARTESIAN_POINT ( 'NONE',  ( 3.042071309553173286, 225.3645833367473301, 11.35316468749999608 ) ) ;
#60975=CARTESIAN_POINT ( 'NONE',  ( 5.676582343749997150, 252.2395833367473301, -9.832129032723418760 ) ) ;
#61007=CARTESIAN_POINT ( 'NONE',  ( -11.35316468749999963, 254.2187500034139873, 0.000000000000000000 ) ) ;
#61035=CARTESIAN_POINT ( 'NONE',  ( -9.999999999999998224, 228.3333333401612606, 2.679491924311235618 ) ) ;
#61089=EDGE_CURVE ( 'NONE', #58601, #29199, #59981, .T. ) ;
#61106=EDGE_CURVE ( 'NONE', #6411, #73780, #11602, .T. ) ;
#61114=DIRECTION ( 'NONE',  ( 0.000000000000000000, 0.000000000000000000, -1.000000000000000000 ) ) ;
#61122=CARTESIAN_POINT ( 'NONE',  ( -8.311093377946834337, 229.5312500034139873, 8.311093377946837890 ) ) ;
#61149=CARTESIAN_POINT ( 'NONE',  ( 4.999999999999997335, 236.4583333401613174, -8.660254037844387298 ) ) ;
#61177=CARTESIAN_POINT ( 'NONE',  ( 9.832129032723420536, 251.3020833367473017, 5.676582343749996262 ) ) ;
#61232=CARTESIAN_POINT ( 'NONE',  ( -10.00000000000000000, 248.1250000068279746, 0.000000000000000000 ) ) ;
#61264=CARTESIAN_POINT ( 'NONE',  ( -9.999999999999998224, 250.2083333333333428, 2.679491924311235618 ) ) ;
#61307=CARTESIAN_POINT ( 'NONE',  ( 3.687316037205747854, 219.9999999999999432, 9.950260519150386784 ) ) ;
#61309=DIRECTION ( 'NONE',  ( -0.000000000000000000, -1.000000000000000000, -0.000000000000000000 ) ) ;
#61311=CARTESIAN_POINT ( 'NONE',  ( 7.320508075688771044, 258.1250000000000000, -7.320508075688771932 ) ) ;
#61349=CARTESIAN_POINT ( 'NONE',  ( 9.832129032723420536, 220.9895833367473301, 5.676582343749996262 ) ) ;
#61352=CARTESIAN_POINT ( 'NONE',  ( -9.832129032723418760, 263.4895833367473301, -5.676582343749998927 ) ) ;
#61385=CARTESIAN_POINT ( 'NONE',  ( -8.311093377946836114, 258.5937500034140157, -8.311093377946836114 ) ) ;
#61411=CARTESIAN_POINT ( 'NONE',  ( 10.00000000000000000, 225.6250000068279746, -1.224646799147353256E-15 ) ) ;
#61435=CARTESIAN_POINT ( 'NONE',  ( -5.676582343750000703, 258.0729166700806445, -9.832129032723418760 ) ) ;
#61440=CARTESIAN_POINT ( 'NONE',  ( 8.311093377946834337, 252.3437500034139873, -8.311093377946836114 ) ) ;
#61499=CARTESIAN_POINT ( 'NONE',  ( -11.35316468749999963, 218.9062500034139873, 0.000000000000000000 ) ) ;
#61554=CARTESIAN_POINT ( 'NONE',  ( 3.042071309553173286, 250.6770833367473017, 11.35316468749999608 ) ) ;
#61569=CARTESIAN_POINT ( 'NONE',  ( 0.6686838642329748783, 220.0000000000000284, 10.97965672913483814 ) ) ;
#61573=CARTESIAN_POINT ( 'NONE',  ( -2.679491924311228512, 228.9583333333333144, -9.999999999999998224 ) ) ;
#61582=ORIENTED_EDGE ( 'NONE', *, *, #62144, .F. ) ;
#61587=FACE_BOUND ( 'NONE', #23356, .T. ) ;
#61642=CARTESIAN_POINT ( 'NONE',  ( 7.320508075688771044, 253.1249999999999716, -7.320508075688771932 ) ) ;
#61649=CARTESIAN_POINT ( 'NONE',  ( 7.320508075688776373, 260.0000000068279746, 7.320508075688767491 ) ) ;
#61650=DIRECTION ( 'NONE',  ( 0.000000000000000000, -0.000000000000000000, 1.000000000000000000 ) ) ;
#61672=CARTESIAN_POINT ( 'NONE',  ( 8.311093377946834337, 222.3437500034139589, -8.311093377946836114 ) ) ;
#61681=CARTESIAN_POINT ( 'NONE',  ( 0.000000000000000000, 0.000000000000000000, 0.000000000000000000 ) ) ;
#61698=DIRECTION ( 'NONE',  ( 0.000000000000000000, 0.000000000000000000, -1.000000000000000000 ) ) ;
#61724=CARTESIAN_POINT ( 'NONE',  ( -5.676582343749992710, 259.7395833367473301, 9.832129032723422313 ) ) ;
#61761=CARTESIAN_POINT ( 'NONE',  ( -11.35316468749999785, 254.0104166700806729, -3.042071309553164848 ) ) ;
#61787=CARTESIAN_POINT ( 'NONE',  ( -2.679491924311222295, 224.1666666734946602, 10.00000000000000178 ) ) ;
#61808=CARTESIAN_POINT ( 'NONE',  ( 11.35316468749999608, 256.6145833367473870, -3.042071309553167513 ) ) ;
#61812=CARTESIAN_POINT ( 'NONE',  ( -3.042071309553166181, 258.1770833367473301, -11.35316468749999608 ) ) ;
#61830=EDGE_CURVE ( 'NONE', #67635, #6411, #23994, .T. ) ;
#61873=CARTESIAN_POINT ( 'NONE',  ( 2.679491924311235174, 259.5833333401612322, 9.999999999999998224 ) ) ;
#61902=CARTESIAN_POINT ( 'NONE',  ( -8.224976990608492855, 220.0000000000001421, 7.304091559116764110 ) ) ;
#61920=CARTESIAN_POINT ( 'NONE',  ( -9.832129032723415207, 254.6354166700806729, 5.676582343750005144 ) ) ;
#61947=( BOUNDED_CURVE ( )  B_SPLINE_CURVE ( 2, ( #32825, #4516, #21480, #50521, #50897, #10542, #55835, #16550, #56577, #27511, #44501, #44876, #16934 ),
 .UNSPECIFIED., .F., .F. ) 
 B_SPLINE_CURVE_WITH_KNOTS ( ( 3, 2, 2, 2, 2, 2, 3 ),
 ( 0.4166666666666664076, 0.4259259259259256525, 0.4351851851851848973, 0.4444444444444441422, 0.4537037037037034981, 0.4629629629629627430, 0.4722222222222219878 ),
 .UNSPECIFIED. ) 
 CURVE ( )  GEOMETRIC_REPRESENTATION_ITEM ( )  RATIONAL_B_SPLINE_CURVE ( ( 1.000000000000001110, 0.9659258262890673130, 1.000000000000000000, 0.9659258262890683122, 1.000000000000000000, 0.9659258262890683122, 1.000000000000000000, 0.9659258262890683122, 1.000000000000000000, 0.9659258262890683122, 1.000000000000000000, 0.9659258262890690894, 0.9999999999999992228 ) ) 
 REPRESENTATION_ITEM ( '' )  );
#61954=CARTESIAN_POINT ( 'NONE',  ( 3.042071309553163960, 262.4479166700806445, -11.35316468749999785 ) ) ;
#62007=CARTESIAN_POINT ( 'NONE',  ( -8.660254037844385522, 245.4166666666666856, 5.000000000000004441 ) ) ;
#62048=EDGE_CURVE ( 'NONE', #66955, #53500, #59815, .T. ) ;
#62092=CARTESIAN_POINT ( 'NONE',  ( -11.35316468749999785, 263.6979166700807014, -3.042071309553164848 ) ) ;
#62125=CARTESIAN_POINT ( 'NONE',  ( -8.311093377946834337, 259.8437500034139589, 8.311093377946837890 ) ) ;
#62144=EDGE_CURVE ( 'NONE', #67329, #34088, #65832, .T. ) ;
#62152=CARTESIAN_POINT ( 'NONE',  ( -2.679491924311222295, 229.1666666734946034, 10.00000000000000178 ) ) ;
#62173=CARTESIAN_POINT ( 'NONE',  ( 3.042071309553163516, 242.4479166700806161, -11.35316468749999785 ) ) ;
#62178=CARTESIAN_POINT ( 'NONE',  ( -9.832129032723418760, 248.8020833367473301, -5.676582343749998927 ) ) ;
#62181=ORIENTED_EDGE ( 'NONE', *, *, #25072, .F. ) ;
#62237=CARTESIAN_POINT ( 'NONE',  ( -8.311093377946834337, 219.5312500034139589, 8.311093377946837890 ) ) ;
#62258=CARTESIAN_POINT ( 'NONE',  ( 8.660254037844389075, 222.0833333333333428, 4.999999999999997335 ) ) ;
#62288=CARTESIAN_POINT ( 'NONE',  ( -6.951808397369817780E-16, 237.9687500034139873, -11.35316468749999963 ) ) ;
#62322=CARTESIAN_POINT ( 'NONE',  ( -6.123233995736766282E-16, 226.8750000068279746, -10.00000000000000000 ) ) ;
#62369=CARTESIAN_POINT ( 'NONE',  ( -9.999999999999998224, 235.2083333333333712, 2.679491924311235618 ) ) ;
#62379=CARTESIAN_POINT ( 'NONE',  ( -8.224976990608492855, 220.0000000000001421, 7.304091559116764110 ) ) ;
#62409=CARTESIAN_POINT ( 'NONE',  ( 10.00000000000000178, 247.2916666666666856, 2.679491924311222739 ) ) ;
#62429=FACE_OUTER_BOUND ( 'NONE', #48965, .T. ) ;
#62455=CARTESIAN_POINT ( 'NONE',  ( -9.832129032723418760, 253.4895833367473017, -5.676582343749998927 ) ) ;
#62474=CARTESIAN_POINT ( 'NONE',  ( -5.676582343749992710, 220.0520833367473301, 9.832129032723422313 ) ) ;
#62490=CARTESIAN_POINT ( 'NONE',  ( -5.676582343749992710, 255.0520833367473301, 9.832129032723422313 ) ) ;
#62520=CARTESIAN_POINT ( 'NONE',  ( 5.000000000000004441, 229.7916666734946602, 8.660254037844385522 ) ) ;
#62543=CARTESIAN_POINT ( 'NONE',  ( 2.085542519210945334E-15, 240.1562500034140157, 11.35316468749999963 ) ) ;
#62547=CARTESIAN_POINT ( 'NONE',  ( 5.676582343749997150, 257.5520833367473301, -9.832129032723418760 ) ) ;
#62607=CARTESIAN_POINT ( 'NONE',  ( 11.35316468749999963, 221.1979166700806161, 3.042071309553159519 ) ) ;
#62611=AXIS2_PLACEMENT_3D ( 'NONE', #70575, #41898, #13213 ) ;
#62630=CARTESIAN_POINT ( 'NONE',  ( 5.000000000000004441, 221.6666666666666856, 8.660254037844385522 ) ) ;
#62656=CARTESIAN_POINT ( 'NONE',  ( -11.35316468749999785, 244.0104166700806729, -3.042071309553164848 ) ) ;
#62688=CARTESIAN_POINT ( 'NONE',  ( 9.832129032723420536, 260.9895833367473301, 5.676582343749996262 ) ) ;
#62726=DIRECTION ( 'NONE',  ( -0.000000000000000000, -1.000000000000000000, -0.000000000000000000 ) ) ;
#62738=CARTESIAN_POINT ( 'NONE',  ( 5.000000000000004441, 231.6666666666666856, 8.660254037844385522 ) ) ;
#62826=CARTESIAN_POINT ( 'NONE',  ( -9.832129032723415207, 239.3229166700806445, 5.676582343750005144 ) ) ;
#62830=CARTESIAN_POINT ( 'NONE',  ( -8.406549073443436271, 220.0000000000000284, 7.038866479487354333 ) ) ;
#62860=CARTESIAN_POINT ( 'NONE',  ( 11.35316468749999963, 241.5104166700806729, 3.042071309553159519 ) ) ;
#62901=PRODUCT_DEFINITION_CONTEXT ( 'detailed design', #58827, 'design' ) ;
#62913=ADVANCED_FACE ( 'NONE', ( #60364 ), #8690, .T. ) ;
#62921=CARTESIAN_POINT ( 'NONE',  ( -5.676582343749992710, 249.7395833367473301, 9.832129032723422313 ) ) ;
#62926=CARTESIAN_POINT ( 'NONE',  ( -5.676582343750000703, 233.3854166700806729, -9.832129032723418760 ) ) ;
#62929=ORIENTED_EDGE ( 'NONE', *, *, #62048, .T. ) ;
#62988=CARTESIAN_POINT ( 'NONE',  ( -2.679491924311228512, 262.0833333401612322, -9.999999999999998224 ) ) ;
#63033=CARTESIAN_POINT ( 'NONE',  ( -8.311093377946836114, 238.5937500034139589, -8.311093377946836114 ) ) ;
#63048=CARTESIAN_POINT ( 'NONE',  ( 8.660254037844389075, 227.0833333333333712, 4.999999999999997335 ) ) ;
#63071=CARTESIAN_POINT ( 'NONE',  ( 11.35316468749999963, 256.1979166700806445, 3.042071309553159519 ) ) ;
#63078=ORIENTED_EDGE ( 'NONE', *, *, #42912, .F. ) ;
#63097=CARTESIAN_POINT ( 'NONE',  ( 0.000000000000000000, 0.000000000000000000, 0.000000000000000000 ) ) ;
#63118=CARTESIAN_POINT ( 'NONE',  ( 2.679491924311235174, 236.4583333333333712, 9.999999999999998224 ) ) ;
#63145=EDGE_CURVE ( 'NONE', #23527, #2698, #65475, .T. ) ;
#63200=CARTESIAN_POINT ( 'NONE',  ( 11.35316468749999608, 241.6145833367473585, -3.042071309553167069 ) ) ;
#63235=CARTESIAN_POINT ( 'NONE',  ( -5.676582343749992710, 250.0520833367473301, 9.832129032723422313 ) ) ;
#63288=CARTESIAN_POINT ( 'NONE',  ( -9.832129032723418760, 243.4895833367473301, -5.676582343749998927 ) ) ;
#63292=CARTESIAN_POINT ( 'NONE',  ( 11.35316468749999608, 241.9270833367473301, -3.042071309553167069 ) ) ;
#63294=ORIENTED_EDGE ( 'NONE', *, *, #52569, .T. ) ;
#63350=CARTESIAN_POINT ( 'NONE',  ( 8.660254037844385522, 251.0416666734946318, -5.000000000000003553 ) ) ;
#63401=CARTESIAN_POINT ( 'NONE',  ( -8.311093377946836114, 248.5937500034139589, -8.311093377946836114 ) ) ;
#63402=DIRECTION ( 'NONE',  ( -0.000000000000000000, -1.000000000000000000, -0.000000000000000000 ) ) ;
#63437=CARTESIAN_POINT ( 'NONE',  ( -5.676582343750000703, 248.0729166700806729, -9.832129032723418760 ) ) ;
#63491=CARTESIAN_POINT ( 'NONE',  ( -8.660254037844387298, 234.5833333333333428, -4.999999999999999112 ) ) ;
#63500=CARTESIAN_POINT ( 'NONE',  ( -8.660254037844387298, 227.7083333401613174, -4.999999999999999112 ) ) ;
#63507=CARTESIAN_POINT ( 'NONE',  ( 0.000000000000000000, 220.0000000000000284, 0.000000000000000000 ) ) ;
#63552=CARTESIAN_POINT ( 'NONE',  ( 0.000000000000000000, 265.0000000000000000, 0.000000000000000000 ) ) ;
#63575=CARTESIAN_POINT ( 'NONE',  ( -6.951808397369817780E-16, 247.6562500034140157, -11.35316468749999963 ) ) ;
#63609=CARTESIAN_POINT ( 'NONE',  ( 5.676582343750005144, 240.8854166700806445, 9.832129032723416984 ) ) ;
#63664=CARTESIAN_POINT ( 'NONE',  ( -9.832129032723418760, 248.4895833367473301, -5.676582343749998927 ) ) ;
#63667=CARTESIAN_POINT ( 'NONE',  ( 2.085542519210945334E-15, 240.4687500034139873, 11.35316468749999963 ) ) ;
#63725=CARTESIAN_POINT ( 'NONE',  ( 1.836970198721029589E-15, 249.3750000068279746, 10.00000000000000000 ) ) ;
#63768=B_SPLINE_CURVE_WITH_KNOTS ( 'NONE', 3,
 ( #65090, #48108, #71118, #48482, #15266, #66584, #25832, #61307, #71860, #20174, #2842, #38299 ),
 .UNSPECIFIED., .F., .F.,
 ( 4, 2, 2, 2, 2, 4 ),
 ( 6.134400178827896381E-17, 0.001907903290037582782, 0.002861854935056343165, 0.003815806580075103982, 0.005723709870112623013, 0.007631613160150140310 ),
 .UNSPECIFIED. ) ;
#63776=CARTESIAN_POINT ( 'NONE',  ( 9.832129032723416984, 232.1354166700806445, -5.676582343750003368 ) ) ;
#63783=CARTESIAN_POINT ( 'NONE',  ( -10.00000000000000000, 240.0000000000000284, 0.000000000000000000 ) ) ;
#63815=CARTESIAN_POINT ( 'NONE',  ( -11.35316468749999608, 244.1145833367472733, 3.042071309553173730 ) ) ;
#63840=EDGE_CURVE ( 'NONE', #71972, #67635, #67952, .T. ) ;
#63866=CARTESIAN_POINT ( 'NONE',  ( -2.679491924311228512, 243.9583333333333144, -9.999999999999998224 ) ) ;
#63892=ORIENTED_EDGE ( 'NONE', *, *, #21763, .F. ) ;
#63907=VECTOR ( 'NONE', #58844, 1000.000000000000000 ) ;
#63922=AXIS2_PLACEMENT_3D ( 'NONE', #4621, #33307, #38587 ) ;
#63957=CARTESIAN_POINT ( 'NONE',  ( 9.832129032723416984, 246.8229166700806729, -5.676582343750003368 ) ) ;
#63983=CARTESIAN_POINT ( 'NONE',  ( -10.00000000000000000, 224.7916666666666288, -2.679491924311226292 ) ) ;
#63990=CARTESIAN_POINT ( 'NONE',  ( 3.042071309553173286, 245.6770833367473017, 11.35316468749999608 ) ) ;
#64035=DIRECTION ( 'NONE',  ( 0.000000000000000000, 0.000000000000000000, -1.000000000000000000 ) ) ;
#64045=CARTESIAN_POINT ( 'NONE',  ( 11.35316468749999608, 231.6145833367473017, -3.042071309553167513 ) ) ;
#64046=CARTESIAN_POINT ( 'NONE',  ( 0.000000000000000000, 0.000000000000000000, 0.000000000000000000 ) ) ;
#64049=CARTESIAN_POINT ( 'NONE',  ( -9.832129032723415207, 244.6354166700806445, 5.676582343750005144 ) ) ;
#64080=FACE_OUTER_BOUND ( 'NONE', #21532, .T. ) ;
#64103=CARTESIAN_POINT ( 'NONE',  ( 10.00000000000000178, 255.4166666734946602, 2.679491924311222739 ) ) ;
#64143=CARTESIAN_POINT ( 'NONE',  ( -4.999999999999992895, 233.9583333401613174, 8.660254037844390851 ) ) ;
#64150=CARTESIAN_POINT ( 'NONE',  ( -5.000000000000000888, 249.1666666666666856, -8.660254037844387298 ) ) ;
#64152=CARTESIAN_POINT ( 'NONE',  ( -9.832129032723418760, 228.8020833367473301, -5.676582343749998927 ) ) ;
#64157=( BOUNDED_CURVE ( )  B_SPLINE_CURVE ( 2, ( #47456, #18799, #32732, #14971, #3672, #15718, #27049, #44780, #49695, #26670, #50062, #72708, #33115 ),
 .UNSPECIFIED., .F., .F. ) 
 B_SPLINE_CURVE_WITH_KNOTS ( ( 3, 2, 2, 2, 2, 2, 3 ),
 ( 0.8611111111111111605, 0.8703703703703703498, 0.8796296296296297612, 0.8888888888888889506, 0.8981481481481482509, 0.9074074074074076623, 0.9166666666666668517 ),
 .UNSPECIFIED. ) 
 CURVE ( )  GEOMETRIC_REPRESENTATION_ITEM ( )  RATIONAL_B_SPLINE_CURVE ( ( 1.000000000000000000, 0.9659258262890683122, 1.000000000000000000, 0.9659258262890683122, 1.000000000000000000, 0.9659258262890683122, 1.000000000000000000, 0.9659258262890683122, 1.000000000000000000, 0.9659258262890683122, 1.000000000000000000, 0.9659258262890675351, 1.000000000000000888 ) ) 
 REPRESENTATION_ITEM ( '' )  );
#64159=( BOUNDED_CURVE ( )  B_SPLINE_CURVE ( 2, ( #7277, #58969, #36689, #59700, #31015, #59336, #53669, #7647, #19319, #54417, #64620, #31391, #18960 ),
 .UNSPECIFIED., .F., .F. ) 
 B_SPLINE_CURVE_WITH_KNOTS ( ( 3, 2, 2, 2, 2, 2, 3 ),
 ( 0.4722222222222219878, 0.4814814814814812327, 0.4907407407407405331, 0.4999999999999997780, 0.5092592592592590783, 0.5185185185185182677, 0.5277777777777775681 ),
 .UNSPECIFIED. ) 
 CURVE ( )  GEOMETRIC_REPRESENTATION_ITEM ( )  RATIONAL_B_SPLINE_CURVE ( ( 1.000000000000000888, 0.9659258262890675351, 1.000000000000000000, 0.9659258262890683122, 1.000000000000000000, 0.9659258262890683122, 1.000000000000000000, 0.9659258262890683122, 1.000000000000000000, 0.9659258262890683122, 1.000000000000000000, 0.9659258262890690894, 0.9999999999999992228 ) ) 
 REPRESENTATION_ITEM ( '' )  );
#64193=CARTESIAN_POINT ( 'NONE',  ( 8.311093377946839666, 245.7812500034139873, 8.311093377946829008 ) ) ;
#64239=CARTESIAN_POINT ( 'NONE',  ( 8.660254037844389075, 227.0833333333333712, 4.999999999999997335 ) ) ;
#64325=CARTESIAN_POINT ( 'NONE',  ( 2.085542519210945334E-15, 250.1562500034140157, 11.35316468749999963 ) ) ;
#64329=CARTESIAN_POINT ( 'NONE',  ( -8.660254037844387298, 264.5833333333333144, -4.999999999999999112 ) ) ;
#64354=CARTESIAN_POINT ( 'NONE',  ( -10.00000000000000000, 238.1250000068279746, 0.000000000000000000 ) ) ;
#64357=CARTESIAN_POINT ( 'NONE',  ( 9.999999999999998224, 220.8333333401613174, -2.679491924311229401 ) ) ;
#64361=CARTESIAN_POINT ( 'NONE',  ( -11.35316468749999608, 239.4270833367473017, 3.042071309553173730 ) ) ;
#64384=EDGE_CURVE ( 'NONE', #35109, #2698, #72558, .T. ) ;
#64418=CARTESIAN_POINT ( 'NONE',  ( -3.042071309553159075, 229.9479166700806161, 11.35316468749999963 ) ) ;
#64421=CARTESIAN_POINT ( 'NONE',  ( 5.676582343750005144, 240.8854166700806445, 9.832129032723416984 ) ) ;
#64452=ORIENTED_EDGE ( 'NONE', *, *, #66617, .F. ) ;
#64479=CARTESIAN_POINT ( 'NONE',  ( 7.320508075688771044, 251.2500000068279746, -7.320508075688771932 ) ) ;
#64525=CARTESIAN_POINT ( 'NONE',  ( 8.311093377946839666, 231.0937500034139873, 8.311093377946829008 ) ) ;
#64534=CARTESIAN_POINT ( 'NONE',  ( 0.000000000000000000, 220.0000000000000284, 0.000000000000000000 ) ) ;
#64562=CARTESIAN_POINT ( 'NONE',  ( 11.35316468749999963, 241.4062500034140157, -1.390361679473963556E-15 ) ) ;
#64613=CARTESIAN_POINT ( 'NONE',  ( -11.35316468749999963, 264.2187500034140157, 0.000000000000000000 ) ) ;
#64620=CARTESIAN_POINT ( 'NONE',  ( 5.000000000000004441, 241.6666666666666572, 8.660254037844385522 ) ) ;
#64692=( BOUNDED_CURVE ( )  B_SPLINE_CURVE ( 2, ( #71084, #25430, #14479, #48819, #7363, #71826, #8461, #53390, #1715, #65432, #48446, #70724, #20143 ),
 .UNSPECIFIED., .F., .F. ) 
 B_SPLINE_CURVE_WITH_KNOTS ( ( 3, 2, 2, 2, 2, 2, 3 ),
 ( 0.4722222222222219878, 0.4814814814814812327, 0.4907407407407405331, 0.4999999999999997780, 0.5092592592592590783, 0.5185185185185182677, 0.5277777777777775681 ),
 .UNSPECIFIED. ) 
 CURVE ( )  GEOMETRIC_REPRESENTATION_ITEM ( )  RATIONAL_B_SPLINE_CURVE ( ( 1.000000000000000888, 0.9659258262890675351, 1.000000000000000000, 0.9659258262890683122, 1.000000000000000000, 0.9659258262890683122, 1.000000000000000000, 0.9659258262890683122, 1.000000000000000000, 0.9659258262890683122, 1.000000000000000000, 0.9659258262890690894, 0.9999999999999992228 ) ) 
 REPRESENTATION_ITEM ( '' )  );
#64694=CARTESIAN_POINT ( 'NONE',  ( -3.042071309553166181, 237.8645833367473301, -11.35316468749999608 ) ) ;
#64728=CARTESIAN_POINT ( 'NONE',  ( -5.676582343750000703, 233.3854166700806729, -9.832129032723418760 ) ) ;
#64735=DIRECTION ( 'NONE',  ( -0.8660254037844389297, 0.4999999999999994449, -0.000000000000000000 ) ) ;
#64776=CARTESIAN_POINT ( 'NONE',  ( 11.35316468749999608, 226.6145833367473301, -3.042071309553167513 ) ) ;
#64782=CARTESIAN_POINT ( 'NONE',  ( -3.042071309553159075, 225.2604166700806161, 11.35316468749999963 ) ) ;
#64837=CARTESIAN_POINT ( 'NONE',  ( 4.999999999999997335, 256.4583333401613459, -8.660254037844387298 ) ) ;
#64853=ORIENTED_EDGE ( 'NONE', *, *, #8254, .F. ) ;
#64877=AXIS2_PLACEMENT_3D ( 'NONE', #20422, #43438, #67214 ) ;
#64886=CARTESIAN_POINT ( 'NONE',  ( -11.35316468749999785, 234.0104166700806161, -3.042071309553164848 ) ) ;
#64887=LINE ( 'NONE', #46794, #40986 ) ;
#64909=VERTEX_POINT ( 'NONE', #670 ) ;
#64917=CARTESIAN_POINT ( 'NONE',  ( 2.679491924311234730, 224.5833333401613174, 9.999999999999998224 ) ) ;
#64918=CARTESIAN_POINT ( 'NONE',  ( 9.832129032723420536, 250.9895833367473017, 5.676582343749996262 ) ) ;
#64954=CARTESIAN_POINT ( 'NONE',  ( 1.224646799147353256E-15, 0.000000000000000000, 10.00000000000000000 ) ) ;
#64963=CARTESIAN_POINT ( 'NONE',  ( -5.000000000000000888, 224.1666666666666856, -8.660254037844387298 ) ) ;
#65009=( BOUNDED_CURVE ( )  B_SPLINE_CURVE ( 2, ( #24012, #25109, #31903, #3233, #59468, #60566, #42468, #55299, #31529, #65485, #26220, #54551, #72641 ),
 .UNSPECIFIED., .F., .F. ) 
 B_SPLINE_CURVE_WITH_KNOTS ( ( 3, 2, 2, 2, 2, 2, 3 ),
 ( 0.3611111111111107719, 0.3703703703703700167, 0.3796296296296293171, 0.3888888888888886175, 0.3981481481481478624, 0.4074074074074071072, 0.4166666666666664076 ),
 .UNSPECIFIED. ) 
 CURVE ( )  GEOMETRIC_REPRESENTATION_ITEM ( )  RATIONAL_B_SPLINE_CURVE ( ( 1.000000000000001332, 0.9659258262890670910, 1.000000000000000000, 0.9659258262890683122, 1.000000000000000000, 0.9659258262890683122, 1.000000000000000000, 0.9659258262890683122, 1.000000000000000000, 0.9659258262890683122, 1.000000000000000000, 0.9659258262890693114, 0.9999999999999990008 ) ) 
 REPRESENTATION_ITEM ( '' )  );
#65037=CARTESIAN_POINT ( 'NONE',  ( 8.660254037844389075, 255.2083333401612890, 4.999999999999997335 ) ) ;
#65046=CARTESIAN_POINT ( 'NONE',  ( 9.832129032723416984, 236.8229166700806445, -5.676582343750003368 ) ) ;
#65051=CARTESIAN_POINT ( 'NONE',  ( 10.00000000000000000, 262.5000000000000000, -1.224646799147353256E-15 ) ) ;
#65080=CARTESIAN_POINT ( 'NONE',  ( 11.35316468749999963, 231.7187500034139873, -1.390361679473963556E-15 ) ) ;
#65090=CARTESIAN_POINT ( 'NONE',  ( 7.071067751884405617, 220.0000000000000284, 7.071067871846544506 ) ) ;
#65104=EDGE_LOOP ( 'NONE', ( #56833, #10730, #41006, #25629 ) ) ;
#65135=CARTESIAN_POINT ( 'NONE',  ( 9.832129032723420536, 225.9895833367473585, 5.676582343749996262 ) ) ;
#65140=CARTESIAN_POINT ( 'NONE',  ( 9.832129032723416984, 232.1354166700806445, -5.676582343750003368 ) ) ;
#65174=EDGE_CURVE ( 'NONE', #71847, #66887, #67559, .T. ) ;
#65195=CARTESIAN_POINT ( 'NONE',  ( -4.999999999999992895, 243.9583333401613174, 8.660254037844390851 ) ) ;
#65224=CARTESIAN_POINT ( 'NONE',  ( -5.676582343749992710, 260.0520833367473301, 9.832129032723422313 ) ) ;
#65239=CARTESIAN_POINT ( 'NONE',  ( -7.320508075688770155, 233.7500000068280031, 7.320508075688774596 ) ) ;
#65249=CARTESIAN_POINT ( 'NONE',  ( -11.35316468749999608, 229.4270833367473585, 3.042071309553173730 ) ) ;
#65289=CARTESIAN_POINT ( 'NONE',  ( -9.832129032723415207, 234.3229166700806445, 5.676582343750005144 ) ) ;
#65308=EDGE_CURVE ( 'NONE', #41315, #25962, #72845, .T. ) ;
#65314=CARTESIAN_POINT ( 'NONE',  ( 0.000000000000000000, 0.000000000000000000, -11.00000000000000000 ) ) ;
#65332=EDGE_CURVE ( 'NONE', #17439, #72211, #36718, .T. ) ;
#65340=CARTESIAN_POINT ( 'NONE',  ( 8.311093377946834337, 262.3437500034140157, -8.311093377946836114 ) ) ;
#65344=EDGE_CURVE ( 'NONE', #67329, #3433, #6574, .T. ) ;
#65378=ORIENTED_EDGE ( 'NONE', *, *, #60070, .F. ) ;
#65423=ORIENTED_EDGE ( 'NONE', *, *, #29785, .F. ) ;
#65424=CARTESIAN_POINT ( 'NONE',  ( 8.311093377946839666, 230.7812500034139589, 8.311093377946829008 ) ) ;
#65432=CARTESIAN_POINT ( 'NONE',  ( 7.320508075688776373, 240.0000000068279462, 7.320508075688767491 ) ) ;
#65453=CARTESIAN_POINT ( 'NONE',  ( -9.999999999999998224, 238.3333333401612890, 2.679491924311235174 ) ) ;
#65460=CARTESIAN_POINT ( 'NONE',  ( 11.35316468749999608, 226.9270833367473301, -3.042071309553167513 ) ) ;
#65475=CIRCLE ( 'NONE', #19678, 19.00000000000000000 ) ;
#65485=CARTESIAN_POINT ( 'NONE',  ( 7.320508075688776373, 245.0000000068279462, 7.320508075688767491 ) ) ;
#65513=CARTESIAN_POINT ( 'NONE',  ( 5.676582343749997150, 232.2395833367473301, -9.832129032723418760 ) ) ;
#65517=CARTESIAN_POINT ( 'NONE',  ( 3.042071309553163960, 222.7604166700806161, -11.35316468749999785 ) ) ;
#65573=CARTESIAN_POINT ( 'NONE',  ( -8.660254037844387298, 232.7083333401613174, -4.999999999999999112 ) ) ;
#65622=CARTESIAN_POINT ( 'NONE',  ( -8.660254037844387298, 249.5833333333333428, -4.999999999999999112 ) ) ;
#65658=CARTESIAN_POINT ( 'NONE',  ( 8.311093377946839666, 235.7812500034139589, 8.311093377946829008 ) ) ;
#65705=CARTESIAN_POINT ( 'NONE',  ( -6.123233995736766282E-16, 223.7500000000000000, -10.00000000000000000 ) ) ;
#65794=CARTESIAN_POINT ( 'NONE',  ( 5.676582343750005144, 225.5729166700806729, 9.832129032723416984 ) ) ;
#65798=CARTESIAN_POINT ( 'NONE',  ( -9.999999999999998224, 260.2083333333333144, 2.679491924311235618 ) ) ;
#65825=CARTESIAN_POINT ( 'NONE',  ( -9.832129032723418760, 228.8020833367473301, -5.676582343749998927 ) ) ;
#65832=LINE ( 'NONE', #7765, #30521 ) ;
#65873=AXIS2_PLACEMENT_3D ( 'NONE', #27019, #73046, #9299 ) ;
#65879=CARTESIAN_POINT ( 'NONE',  ( -11.35316468749999963, 223.9062500034139873, 0.000000000000000000 ) ) ;
#65882=CARTESIAN_POINT ( 'NONE',  ( 11.35316468749999608, 226.9270833367473301, -3.042071309553167069 ) ) ;
#65947=CARTESIAN_POINT ( 'NONE',  ( 10.00000000000000000, 245.6250000068279746, -1.224646799147353256E-15 ) ) ;
#65966=CARTESIAN_POINT ( 'NONE',  ( 9.832129032723416984, 261.8229166700807014, -5.676582343750003368 ) ) ;
#65990=DIRECTION ( 'NONE',  ( -0.000000000000000000, -1.000000000000000000, -0.000000000000000000 ) ) ;
#66032=CARTESIAN_POINT ( 'NONE',  ( 2.085542519210945334E-15, 240.1562500034140157, 11.35316468749999963 ) ) ;
#66078=FACE_OUTER_BOUND ( 'NONE', #54844, .T. ) ;
#66079=CARTESIAN_POINT ( 'NONE',  ( -8.311093377946836114, 253.5937500034140157, -8.311093377946836114 ) ) ;
#66167=CARTESIAN_POINT ( 'NONE',  ( 2.085542519210945334E-15, 235.1562500034140157, 11.35316468749999963 ) ) ;
#66172=CARTESIAN_POINT ( 'NONE',  ( 1.836970198721029589E-15, 246.2500000000000284, 10.00000000000000000 ) ) ;
#66201=CARTESIAN_POINT ( 'NONE',  ( -9.832129032723418760, 233.8020833367473301, -5.676582343749998927 ) ) ;
#66212=EDGE_LOOP ( 'NONE', ( #47487, #25033, #47324, #56163 ) ) ;
#66254=CARTESIAN_POINT ( 'NONE',  ( -8.311093377946834337, 224.5312500034140157, 8.311093377946837890 ) ) ;
#66258=CARTESIAN_POINT ( 'NONE',  ( -11.35316468749999608, 224.4270833367473017, 3.042071309553173730 ) ) ;
#66320=CARTESIAN_POINT ( 'NONE',  ( 9.999999999999998224, 240.8333333401612890, -2.679491924311229401 ) ) ;
#66339=CARTESIAN_POINT ( 'NONE',  ( 3.042071309553173286, 255.3645833367473301, 11.35316468749999608 ) ) ;
#66381=DIRECTION ( 'NONE',  ( 0.000000000000000000, -1.000000000000000000, 0.000000000000000000 ) ) ;
#66397=CARTESIAN_POINT ( 'NONE',  ( 0.000000000000000000, 45.00000000000000000, 0.000000000000000000 ) ) ;
#66405=CARTESIAN_POINT ( 'NONE',  ( 11.35316468749999963, 241.1979166700806729, 3.042071309553159519 ) ) ;
#66449=( BOUNDED_SURFACE ( )  B_SPLINE_SURFACE ( 1, 2, ( 
 ( #66724, #9010, #8636, #54669, #48244, #2978, #20310, #30537, #19570, #25963, #30900, #43327, #37690, #49362, #32025, #26342, #72380, #53553, #47873, #42212, #65224, #68587, #55793, #55419, #44462, #10504, #16895, #38812, #33911, #61812, #22180, #50117, #62547, #27102, #9386, #56164, #10130, #4110, #67476, #4479, #68215, #45204, #27469, #16513, #32405, #33536, #50482, #33168, #73133, #21068, #39919, #44092, #32786, #3728, #21439, #50860, #45574, #61440, #73497, #21804, #56537, #15775, #22552, #26727, #44837, #72763, #49747, #67844, #15398, #16135, #39174, #73875, #56912, #10877, #62178, #67101, #9766, #38436, #4854, #27851, #39552, #5224, #28225, #51234, #74245, #46320, #68964, #11992, #53103, #45948, #46687, #35026, #29354, #58769, #64049, #28970, #34281, #1066, #328, #51990, #69335, #7077, #23307, #70089, #11251, #17272, #40291, #63292, #12359, #23681, #18023, #17644, #64421, #6351, #63667, #18765, #58038, #52361, #1437, #52732, #58405, #29717, #697, #69711, #11620, #41041, #35393, #51607, #57285, #34657, #6710, #41409, #12719, #24418, #24043, #22938, #47424, #47053, #74623, #5599, #18395, #30083, #57661, #35752, #70449, #5967, #28597, #40664, #62926, #71911, #37226, #54212, #49274, #26255, #65140, #59864, #14564, #25513, #59140, #7448, #59500, #20224, #37601, #43242, #25878, #13449, #60600, #25142, #48897, #8923, #31935, #19858, #2522, #54958, #24774, #3267, #7813, #54586, #72289, #65882, #70811, #36118, #13812, #36856, #60223, #48526, #41772, #64782, #31187, #8177, #47788, #66258, #42864, #30456, #13083, #71166, #53472, #71532, #1789, #65517, #53839, #2149, #19122, #42127, #36487, #30816, #48159, #19486, #42501, #14189, #8549, #31563, #2890, #16055, #73781, #50027, #21350 ),
 ( #38728, #62092, #61352, #67383, #44374, #4022, #5136, #67009, #66630, #55707, #21718, #28130, #73043, #45114, #15686, #33444, #9679, #22090, #38345, #20601, #61724, #10044, #15308, #27015, #20977, #3637, #39087, #4387, #50766, #10414, #14937, #33080, #26635, #56077, #49657, #27379, #10782, #72675, #50399, #73413, #44746, #16422, #67761, #32699, #37976, #56444, #4762, #27755, #68127, #39455, #62455, #33819, #43618, #44002, #56816, #51142, #60975, #9295, #32320, #55332, #974, #17554, #235, #29994, #46227, #40571, #64325, #40947, #11902, #39823, #35300, #46964, #11530, #23957, #69244, #29625, #35661, #52638, #63575, #34935, #68867, #5879, #63957, #58675, #22837, #57948, #28504, #6253, #51513, #18301, #29257, #52270, #12267, #40198, #604, #23216, #57569, #6983, #45851, #45476, #34563, #23585, #74152, #28874, #69994, #51895, #58314, #63200, #41317, #17177, #22456, #46595, #69618, #17932, #6619, #12630, #68494, #16794, #62826, #11162, #34185, #57187, #5504, #74528, #42040, #64694, #60509, #12992, #1706, #47334, #65046, #19769, #14471, #30361, #48068, #53747, #54118, #24683, #66167, #70361, #19392, #41683, #18673, #13720, #59048, #42406, #71076, #42777, #25791, #31473, #36394, #53009, #1341, #36029, #20135, #19035, #13357, #47694, #54496, #65424, #2801, #24323, #36765, #48436, #48811, #7723, #2058, #25047, #7354, #37510, #53381, #8453, #59777, #71816, #8086, #31088, #70715, #2429, #43150, #25422, #30727, #8834, #71441, #59409, #65794, #14096, #37131, #60134, #26539, #68038, #32225, #54867, #49182, #14845, #43521, #26923, #4671, #21632, #27291, #73327, #49940, #72953, #37885, #21260, #67297, #20506, #3177, #60881, #44284, #10326, #33352, #22004, #15596, #66535, #45030, #55988, #9205 ) ),
 .UNSPECIFIED., .F., .F., .F. ) 
 B_SPLINE_SURFACE_WITH_KNOTS ( ( 2, 2 ),
 ( 3, 2, 2, 2, 2, 2, 2, 2, 2, 2, 2, 2, 2, 2, 2, 2, 2, 2, 2, 2, 2, 2, 2, 2, 2, 2, 2, 2, 2, 2, 2, 2, 2, 2, 2, 2, 2, 2, 2, 2, 2, 2, 2, 2, 2, 2, 2, 2, 2, 2, 2, 2, 2, 2, 2, 2, 2, 2, 2, 2, 2, 2, 2, 2, 2, 2, 2, 2, 2, 2, 2, 2, 2, 2, 2, 2, 2, 2, 2, 2, 2, 2, 2, 2, 2, 2, 2, 2, 2, 2, 2, 2, 2, 2, 2, 2, 2, 2, 2, 2, 2, 2, 2, 2, 2, 2, 2, 2, 3 ),
 ( 0.000000000000000000, 1.000000000000000000 ),
 ( 0.000000000000000000, 0.009259259259259258745, 0.01851851851851851749, 0.02777777777777777624, 0.03703703703703703498, 0.04629629629629629373, 0.05555555555555555247, 0.06481481481481481122, 0.07407407407407406996, 0.08333333333333332871, 0.09259259259259258745, 0.1018518518518518462, 0.1111111111111111049, 0.1203703703703703637, 0.1296296296296296224, 0.1388888888888888951, 0.1481481481481481399, 0.1574074074074074125, 0.1666666666666666574, 0.1759259259259259300, 0.1851851851851851749, 0.1944444444444444475, 0.2037037037037036924, 0.2129629629629629650, 0.2222222222222222099, 0.2314814814814814825, 0.2407407407407407274, 0.2500000000000000000, 0.2592592592592592449, 0.2685185185185185452, 0.2777777777777777901, 0.2870370370370370350, 0.2962962962962962798, 0.3055555555555555802, 0.3148148148148148251, 0.3240740740740740700, 0.3333333333333333148, 0.3425925925925926152, 0.3518518518518518601, 0.3611111111111111049, 0.3703703703703703498, 0.3796296296296296502, 0.3888888888888888951, 0.3981481481481481399, 0.4074074074074073848, 0.4166666666666666852, 0.4259259259259259300, 0.4351851851851851749, 0.4444444444444444198, 0.4537037037037037202, 0.4629629629629629650, 0.4722222222222222099, 0.4814814814814814548, 0.4907407407407407551, 0.5000000000000000000, 0.5092592592592593004, 0.5185185185185184897, 0.5277777777777777901, 0.5370370370370370905, 0.5462962962962962798, 0.5555555555555555802, 0.5648148148148147696, 0.5740740740740740700, 0.5833333333333333703, 0.5925925925925925597, 0.6018518518518518601, 0.6111111111111111605, 0.6203703703703703498, 0.6296296296296296502, 0.6388888888888888395, 0.6481481481481481399, 0.6574074074074074403, 0.6666666666666666297, 0.6759259259259259300, 0.6851851851851852304, 0.6944444444444444198, 0.7037037037037037202, 0.7129629629629629095, 0.7222222222222222099, 0.7314814814814815103, 0.7407407407407406996, 0.7500000000000000000, 0.7592592592592593004, 0.7685185185185184897, 0.7777777777777777901, 0.7870370370370370905, 0.7962962962962962798, 0.8055555555555555802, 0.8148148148148147696, 0.8240740740740740700, 0.8333333333333333703, 0.8425925925925925597, 0.8518518518518518601, 0.8611111111111111605, 0.8703703703703703498, 0.8796296296296296502, 0.8888888888888888395, 0.8981481481481481399, 0.9074074074074074403, 0.9166666666666666297, 0.9259259259259259300, 0.9351851851851852304, 0.9444444444444444198, 0.9537037037037037202, 0.9629629629629629095, 0.9722222222222222099, 0.9814814814814815103, 0.9907407407407406996, 1.000000000000000000 ),
 .UNSPECIFIED. ) 
 GEOMETRIC_REPRESENTATION_ITEM ( )  RATIONAL_B_SPLINE_SURFACE ( (
 ( 1.000000000000000000, 0.9659258262890683122, 1.000000000000000000, 0.9659258262890683122, 1.000000000000000000, 0.9659258262890683122, 1.000000000000000000, 0.9659258262890683122, 1.000000000000000000, 0.9659258262890683122, 1.000000000000000000, 0.9659258262890683122, 1.000000000000000000, 0.9659258262890683122, 1.000000000000000000, 0.9659258262890683122, 1.000000000000000000, 0.9659258262890683122, 1.000000000000000000, 0.9659258262890683122, 1.000000000000000000, 0.9659258262890683122, 1.000000000000000000, 0.9659258262890683122, 1.000000000000000000, 0.9659258262890683122, 1.000000000000000000, 0.9659258262890683122, 1.000000000000000000, 0.9659258262890683122, 1.000000000000000000, 0.9659258262890683122, 1.000000000000000000, 0.9659258262890683122, 1.000000000000000000, 0.9659258262890683122, 1.000000000000000000, 0.9659258262890683122, 1.000000000000000000, 0.9659258262890683122, 1.000000000000000000, 0.9659258262890683122, 1.000000000000000000, 0.9659258262890683122, 1.000000000000000000, 0.9659258262890683122, 1.000000000000000000, 0.9659258262890683122, 1.000000000000000000, 0.9659258262890683122, 1.000000000000000000, 0.9659258262890683122, 1.000000000000000000, 0.9659258262890683122, 1.000000000000000000, 0.9659258262890683122, 1.000000000000000000, 0.9659258262890683122, 1.000000000000000000, 0.9659258262890683122, 1.000000000000000000, 0.9659258262890683122, 1.000000000000000000, 0.9659258262890683122, 1.000000000000000000, 0.9659258262890683122, 1.000000000000000000, 0.9659258262890683122, 1.000000000000000000, 0.9659258262890683122, 1.000000000000000000, 0.9659258262890683122, 1.000000000000000000, 0.9659258262890683122, 1.000000000000000000, 0.9659258262890683122, 1.000000000000000000, 0.9659258262890683122, 1.000000000000000000, 0.9659258262890683122, 1.000000000000000000, 0.9659258262890683122, 1.000000000000000000, 0.9659258262890683122, 1.000000000000000000, 0.9659258262890683122, 1.000000000000000000, 0.9659258262890683122, 1.000000000000000000, 0.9659258262890683122, 1.000000000000000000, 0.9659258262890683122, 1.000000000000000000, 0.9659258262890683122, 1.000000000000000000, 0.9659258262890683122, 1.000000000000000000, 0.9659258262890683122, 1.000000000000000000, 0.9659258262890683122, 1.000000000000000000, 0.9659258262890683122, 1.000000000000000000, 0.9659258262890683122, 1.000000000000000000, 0.9659258262890683122, 1.000000000000000000, 0.9659258262890683122, 1.000000000000000000, 0.9659258262890683122, 1.000000000000000000, 0.9659258262890683122, 1.000000000000000000, 0.9659258262890683122, 1.000000000000000000, 0.9659258262890683122, 1.000000000000000000, 0.9659258262890683122, 1.000000000000000000, 0.9659258262890683122, 1.000000000000000000, 0.9659258262890683122, 1.000000000000000000, 0.9659258262890683122, 1.000000000000000000, 0.9659258262890683122, 1.000000000000000000, 0.9659258262890683122, 1.000000000000000000, 0.9659258262890683122, 1.000000000000000000, 0.9659258262890683122, 1.000000000000000000, 0.9659258262890683122, 1.000000000000000000, 0.9659258262890683122, 1.000000000000000000, 0.9659258262890683122, 1.000000000000000000, 0.9659258262890683122, 1.000000000000000000, 0.9659258262890683122, 1.000000000000000000, 0.9659258262890683122, 1.000000000000000000, 0.9659258262890683122, 1.000000000000000000, 0.9659258262890683122, 1.000000000000000000, 0.9659258262890683122, 1.000000000000000000, 0.9659258262890683122, 1.000000000000000000, 0.9659258262890683122, 1.000000000000000000, 0.9659258262890683122, 1.000000000000000000, 0.9659258262890683122, 1.000000000000000000, 0.9659258262890683122, 1.000000000000000000, 0.9659258262890683122, 1.000000000000000000, 0.9659258262890683122, 1.000000000000000000, 0.9659258262890683122, 1.000000000000000000, 0.9659258262890683122, 1.000000000000000000, 0.9659258262890683122, 1.000000000000000000, 0.9659258262890683122, 1.000000000000000000, 0.9659258262890683122, 1.000000000000000000, 0.9659258262890683122, 1.000000000000000000, 0.9659258262890683122, 1.000000000000000000, 0.9659258262890683122, 1.000000000000000000, 0.9659258262890683122, 1.000000000000000000, 0.9659258262890683122, 1.000000000000000000, 0.9659258262890683122, 1.000000000000000000, 0.9659258262890683122, 1.000000000000000000, 0.9659258262890683122, 1.000000000000000000, 0.9659258262890683122, 1.000000000000000000, 0.9659258262890683122, 1.000000000000000000, 0.9659258262890683122, 1.000000000000000000, 0.9659258262890683122, 1.000000000000000000, 0.9659258262890683122, 1.000000000000000000, 0.9659258262890683122, 1.000000000000000000, 0.9659258262890683122, 1.000000000000000000, 0.9659258262890683122, 1.000000000000000000, 0.9659258262890683122, 1.000000000000000000, 0.9659258262890683122, 1.000000000000000000, 0.9659258262890683122, 1.000000000000000000, 0.9659258262890683122, 1.000000000000000000, 0.9659258262890683122, 1.000000000000000000),
 ( 1.000000000000000000, 0.9659258262890683122, 1.000000000000000000, 0.9659258262890683122, 1.000000000000000000, 0.9659258262890683122, 1.000000000000000000, 0.9659258262890683122, 1.000000000000000000, 0.9659258262890683122, 1.000000000000000000, 0.9659258262890683122, 1.000000000000000000, 0.9659258262890683122, 1.000000000000000000, 0.9659258262890683122, 1.000000000000000000, 0.9659258262890683122, 1.000000000000000000, 0.9659258262890683122, 1.000000000000000000, 0.9659258262890683122, 1.000000000000000000, 0.9659258262890683122, 1.000000000000000000, 0.9659258262890683122, 1.000000000000000000, 0.9659258262890683122, 1.000000000000000000, 0.9659258262890683122, 1.000000000000000000, 0.9659258262890683122, 1.000000000000000000, 0.9659258262890683122, 1.000000000000000000, 0.9659258262890683122, 1.000000000000000000, 0.9659258262890683122, 1.000000000000000000, 0.9659258262890683122, 1.000000000000000000, 0.9659258262890683122, 1.000000000000000000, 0.9659258262890683122, 1.000000000000000000, 0.9659258262890683122, 1.000000000000000000, 0.9659258262890683122, 1.000000000000000000, 0.9659258262890683122, 1.000000000000000000, 0.9659258262890683122, 1.000000000000000000, 0.9659258262890683122, 1.000000000000000000, 0.9659258262890683122, 1.000000000000000000, 0.9659258262890683122, 1.000000000000000000, 0.9659258262890683122, 1.000000000000000000, 0.9659258262890683122, 1.000000000000000000, 0.9659258262890683122, 1.000000000000000000, 0.9659258262890683122, 1.000000000000000000, 0.9659258262890683122, 1.000000000000000000, 0.9659258262890683122, 1.000000000000000000, 0.9659258262890683122, 1.000000000000000000, 0.9659258262890683122, 1.000000000000000000, 0.9659258262890683122, 1.000000000000000000, 0.9659258262890683122, 1.000000000000000000, 0.9659258262890683122, 1.000000000000000000, 0.9659258262890683122, 1.000000000000000000, 0.9659258262890683122, 1.000000000000000000, 0.9659258262890683122, 1.000000000000000000, 0.9659258262890683122, 1.000000000000000000, 0.9659258262890683122, 1.000000000000000000, 0.9659258262890683122, 1.000000000000000000, 0.9659258262890683122, 1.000000000000000000, 0.9659258262890683122, 1.000000000000000000, 0.9659258262890683122, 1.000000000000000000, 0.9659258262890683122, 1.000000000000000000, 0.9659258262890683122, 1.000000000000000000, 0.9659258262890683122, 1.000000000000000000, 0.9659258262890683122, 1.000000000000000000, 0.9659258262890683122, 1.000000000000000000, 0.9659258262890683122, 1.000000000000000000, 0.9659258262890683122, 1.000000000000000000, 0.9659258262890683122, 1.000000000000000000, 0.9659258262890683122, 1.000000000000000000, 0.9659258262890683122, 1.000000000000000000, 0.9659258262890683122, 1.000000000000000000, 0.9659258262890683122, 1.000000000000000000, 0.9659258262890683122, 1.000000000000000000, 0.9659258262890683122, 1.000000000000000000, 0.9659258262890683122, 1.000000000000000000, 0.9659258262890683122, 1.000000000000000000, 0.9659258262890683122, 1.000000000000000000, 0.9659258262890683122, 1.000000000000000000, 0.9659258262890683122, 1.000000000000000000, 0.9659258262890683122, 1.000000000000000000, 0.9659258262890683122, 1.000000000000000000, 0.9659258262890683122, 1.000000000000000000, 0.9659258262890683122, 1.000000000000000000, 0.9659258262890683122, 1.000000000000000000, 0.9659258262890683122, 1.000000000000000000, 0.9659258262890683122, 1.000000000000000000, 0.9659258262890683122, 1.000000000000000000, 0.9659258262890683122, 1.000000000000000000, 0.9659258262890683122, 1.000000000000000000, 0.9659258262890683122, 1.000000000000000000, 0.9659258262890683122, 1.000000000000000000, 0.9659258262890683122, 1.000000000000000000, 0.9659258262890683122, 1.000000000000000000, 0.9659258262890683122, 1.000000000000000000, 0.9659258262890683122, 1.000000000000000000, 0.9659258262890683122, 1.000000000000000000, 0.9659258262890683122, 1.000000000000000000, 0.9659258262890683122, 1.000000000000000000, 0.9659258262890683122, 1.000000000000000000, 0.9659258262890683122, 1.000000000000000000, 0.9659258262890683122, 1.000000000000000000, 0.9659258262890683122, 1.000000000000000000, 0.9659258262890683122, 1.000000000000000000, 0.9659258262890683122, 1.000000000000000000, 0.9659258262890683122, 1.000000000000000000, 0.9659258262890683122, 1.000000000000000000, 0.9659258262890683122, 1.000000000000000000, 0.9659258262890683122, 1.000000000000000000, 0.9659258262890683122, 1.000000000000000000, 0.9659258262890683122, 1.000000000000000000, 0.9659258262890683122, 1.000000000000000000, 0.9659258262890683122, 1.000000000000000000, 0.9659258262890683122, 1.000000000000000000, 0.9659258262890683122, 1.000000000000000000, 0.9659258262890683122, 1.000000000000000000, 0.9659258262890683122, 1.000000000000000000, 0.9659258262890683122, 1.000000000000000000, 0.9659258262890683122, 1.000000000000000000, 0.9659258262890683122, 1.000000000000000000) ) ) 
 REPRESENTATION_ITEM ( '' )  SURFACE ( )  );
#66454=CARTESIAN_POINT ( 'NONE',  ( 11.35316468749999963, 251.7187500034139873, -1.390361679473963556E-15 ) ) ;
#66535=CARTESIAN_POINT ( 'NONE',  ( -8.311093377946834337, 219.5312500034139589, 8.311093377946837890 ) ) ;
#66539=DIRECTION ( 'NONE',  ( 1.000000000000000000, 0.000000000000000000, -0.000000000000000000 ) ) ;
#66541=CARTESIAN_POINT ( 'NONE',  ( -10.00000000000000000, 255.0000000000000000, 0.000000000000000000 ) ) ;
#66548=CARTESIAN_POINT ( 'NONE',  ( 2.679491924311375506, 259.5833333401613459, 9.999999999999916511 ) ) ;
#66568=ORIENTED_EDGE ( 'NONE', *, *, #21100, .T. ) ;
#66574=CARTESIAN_POINT ( 'NONE',  ( 5.676582343750005144, 220.8854166700806445, 9.832129032723416984 ) ) ;
#66575=AXIS2_PLACEMENT_3D ( 'NONE', #9548, #54825, #31804 ) ;
#66584=CARTESIAN_POINT ( 'NONE',  ( 4.776596266111742928, 220.0000000000000000, 9.272667727651805691 ) ) ;
#66617=EDGE_CURVE ( 'NONE', #66955, #49089, #25671, .T. ) ;
#66626=CARTESIAN_POINT ( 'NONE',  ( 5.676582343749997150, 222.2395833367473017, -9.832129032723418760 ) ) ;
#66630=CARTESIAN_POINT ( 'NONE',  ( 5.676582343749997150, 262.2395833367473301, -9.832129032723418760 ) ) ;
#66633=FACE_OUTER_BOUND ( 'NONE', #66212, .T. ) ;
#66695=CIRCLE ( 'NONE', #51021, 11.00000000000000000 ) ;
#66696=CARTESIAN_POINT ( 'NONE',  ( -5.000000000000000888, 242.2916666734946318, -8.660254037844387298 ) ) ;
#66698=ORIENTED_EDGE ( 'NONE', *, *, #5486, .F. ) ;
#66720=CARTESIAN_POINT ( 'NONE',  ( -6.951808397369817780E-16, 252.6562500034140157, -11.35316468749999963 ) ) ;
#66724=CARTESIAN_POINT ( 'NONE',  ( -11.35316468749999963, 264.2187500034140157, 0.000000000000000000 ) ) ;
#66747=CARTESIAN_POINT ( 'NONE',  ( -3.042071309553159075, 220.2604166700806161, 11.35316468749999963 ) ) ;
#66784=CARTESIAN_POINT ( 'NONE',  ( 11.35316468749999963, 231.4062500034139873, -1.390361679473963556E-15 ) ) ;
#66799=MANIFOLD_SOLID_BREP ( 'Thread1', #27380 ) ;
#66839=CARTESIAN_POINT ( 'NONE',  ( 11.35316468749999608, 251.9270833367473301, -3.042071309553167069 ) ) ;
#66845=LINE ( 'NONE', #10251, #9425 ) ;
#66882=CARTESIAN_POINT ( 'NONE',  ( 1.836970198721029589E-15, 229.3750000068279746, 10.00000000000000000 ) ) ;
#66887=VERTEX_POINT ( 'NONE', #11538 ) ;
#66924=CARTESIAN_POINT ( 'NONE',  ( 9.999999999999998224, 257.7083333333333712, -2.679491924311229401 ) ) ;
#66953=CARTESIAN_POINT ( 'NONE',  ( 9.832129032723420536, 221.3020833367473301, 5.676582343749996262 ) ) ;
#66955=VERTEX_POINT ( 'NONE', #614 ) ;
#67009=CARTESIAN_POINT ( 'NONE',  ( 3.042071309553163960, 262.4479166700806445, -11.35316468749999785 ) ) ;
#67017=( LENGTH_UNIT ( ) NAMED_UNIT ( * ) SI_UNIT ( .MILLI., .METRE. ) );
#67045=CARTESIAN_POINT ( 'NONE',  ( -8.311093377946834337, 254.8437500034139589, 8.311093377946837890 ) ) ;
#67048=EDGE_CURVE ( 'NONE', #49089, #7137, #2810, .T. ) ;
#67074=CARTESIAN_POINT ( 'NONE',  ( 10.00000000000000000, 230.6250000068279746, -1.224646799147353256E-15 ) ) ;
#67089=EDGE_CURVE ( 'NONE', #5866, #39173, #64692, .T. ) ;
#67093=CYLINDRICAL_SURFACE ( 'NONE', #58376, 10.00000000000000000 ) ;
#67098=CARTESIAN_POINT ( 'NONE',  ( 5.676582343749997150, 257.2395833367473301, -9.832129032723418760 ) ) ;
#67101=CARTESIAN_POINT ( 'NONE',  ( -8.311093377946836114, 248.5937500034139589, -8.311093377946836114 ) ) ;
#67165=CARTESIAN_POINT ( 'NONE',  ( -7.320508075688771932, 262.5000000068279746, -7.320508075688771932 ) ) ;
#67188=CARTESIAN_POINT ( 'NONE',  ( 10.00000000000000000, 222.5000000000000000, -1.224646799147353256E-15 ) ) ;
#67190=CARTESIAN_POINT ( 'NONE',  ( 8.660254037844389075, 235.2083333401613174, 4.999999999999997335 ) ) ;
#67214=DIRECTION ( 'NONE',  ( 0.000000000000000000, 0.000000000000000000, -1.000000000000000000 ) ) ;
#67216=CARTESIAN_POINT ( 'NONE',  ( 8.311093377946839666, 256.0937500034140157, 8.311093377946829008 ) ) ;
#67254=CARTESIAN_POINT ( 'NONE',  ( 9.832129032723420536, 255.9895833367473301, 5.676582343749996262 ) ) ;
#67297=CARTESIAN_POINT ( 'NONE',  ( 11.35316468749999963, 221.4062500034139873, -1.390361679473963556E-15 ) ) ;
#67302=CARTESIAN_POINT ( 'NONE',  ( -8.660254037844387298, 254.5833333333333144, -4.999999999999999112 ) ) ;
#67329=VERTEX_POINT ( 'NONE', #50682 ) ;
#67340=CARTESIAN_POINT ( 'NONE',  ( -6.123233995736766282E-16, 248.7500000000000284, -10.00000000000000000 ) ) ;
#67383=CARTESIAN_POINT ( 'NONE',  ( -8.311093377946836114, 263.2812500034139020, -8.311093377946836114 ) ) ;
#67399=CARTESIAN_POINT ( 'NONE',  ( 1.224646799147353256E-15, 0.000000000000000000, 10.00000000000000000 ) ) ;
#67420=CARTESIAN_POINT ( 'NONE',  ( 3.042071309553163516, 257.7604166700806445, -11.35316468749999785 ) ) ;
#67448=CARTESIAN_POINT ( 'NONE',  ( -4.999999999999992895, 228.9583333401612890, 8.660254037844390851 ) ) ;
#67472=CARTESIAN_POINT ( 'NONE',  ( -3.042071309553159075, 254.9479166700806445, 11.35316468749999963 ) ) ;
#67476=CARTESIAN_POINT ( 'NONE',  ( 9.832129032723420536, 256.3020833367473301, 5.676582343749996262 ) ) ;
#67528=DIRECTION ( 'NONE',  ( 0.000000000000000000, 0.000000000000000000, -1.000000000000000000 ) ) ;
#67536=CARTESIAN_POINT ( 'NONE',  ( 8.311093377946839666, 220.7812500034139873, 8.311093377946829008 ) ) ;
#67559=( BOUNDED_CURVE ( )  B_SPLINE_CURVE ( 2, ( #18367, #7050, #36092, #13054, #41381, #35724, #30059 ),
 .UNSPECIFIED., .F., .F. ) 
 B_SPLINE_CURVE_WITH_KNOTS ( ( 3, 2, 2, 3 ),
 ( 0.000000000000000000, 0.009259259259259060987, 0.01851851851851812197, 0.02777777777777718296 ),
 .UNSPECIFIED. ) 
 CURVE ( )  GEOMETRIC_REPRESENTATION_ITEM ( )  RATIONAL_B_SPLINE_CURVE ( ( 1.000000000000000000, 0.9659258262890683122, 1.000000000000000000, 0.9659258262890683122, 1.000000000000000000, 0.9659258262890705327, 0.9999999999999977796 ) ) 
 REPRESENTATION_ITEM ( '' )  );
#67561=CARTESIAN_POINT ( 'NONE',  ( -6.123233995736766282E-16, 236.8750000068279746, -10.00000000000000000 ) ) ;
#67590=CARTESIAN_POINT ( 'NONE',  ( 11.35316468749999963, 261.5104166700807014, 3.042071309553159519 ) ) ;
#67625=CARTESIAN_POINT ( 'NONE',  ( -5.676582343750000703, 258.0729166700806445, -9.832129032723418760 ) ) ;
#67627=ORIENTED_EDGE ( 'NONE', *, *, #56098, .F. ) ;
#67635=VERTEX_POINT ( 'NONE', #56894 ) ;
#67675=CARTESIAN_POINT ( 'NONE',  ( 1.836970198721029589E-15, 251.2500000000000284, 10.00000000000000000 ) ) ;
#67703=ORIENTED_EDGE ( 'NONE', *, *, #61830, .T. ) ;
#67714=CARTESIAN_POINT ( 'NONE',  ( 8.660254037844389075, 247.0833333333333428, 4.999999999999997335 ) ) ;
#67758=DIRECTION ( 'NONE',  ( -0.000000000000000000, -1.000000000000000000, -0.000000000000000000 ) ) ;
#67761=CARTESIAN_POINT ( 'NONE',  ( 2.085542519210945334E-15, 255.1562500034140157, 11.35316468749999963 ) ) ;
#67795=CARTESIAN_POINT ( 'NONE',  ( 8.311093377946839666, 261.0937500034140157, 8.311093377946830785 ) ) ;
#67819=CARTESIAN_POINT ( 'NONE',  ( -2.679491924311228512, 227.0833333401612606, -9.999999999999998224 ) ) ;
#67840=CARTESIAN_POINT ( 'NONE',  ( 2.085542519210945334E-15, 245.1562500034140157, 11.35316468749999963 ) ) ;
#67844=CARTESIAN_POINT ( 'NONE',  ( -3.042071309553159075, 250.2604166700806445, 11.35316468749999963 ) ) ;
#67904=CARTESIAN_POINT ( 'NONE',  ( -3.042071309553166181, 222.8645833367473301, -11.35316468749999608 ) ) ;
#67938=CARTESIAN_POINT ( 'NONE',  ( -9.526279441628821232, 219.8393163974770630, 5.500000000000004441 ) ) ;
#67952=CIRCLE ( 'NONE', #46247, 10.00000000000000000 ) ;
#67956=CARTESIAN_POINT ( 'NONE',  ( -9.832129032723418760, 248.8020833367473301, -5.676582343749998927 ) ) ;
#67989=CARTESIAN_POINT ( 'NONE',  ( -11.35316468749999963, 263.9062500034140157, 0.000000000000000000 ) ) ;
#68003=CARTESIAN_POINT ( 'NONE',  ( -2.679491924311315110, 247.0833333401613174, -9.999999999999950262 ) ) ;
#68024=EDGE_CURVE ( 'NONE', #44513, #26323, #5436, .T. ) ;
#68036=ORIENTED_EDGE ( 'NONE', *, *, #39451, .F. ) ;
#68038=CARTESIAN_POINT ( 'NONE',  ( -8.311093377946834337, 224.5312500034140157, 8.311093377946837890 ) ) ;
#68044=CARTESIAN_POINT ( 'NONE',  ( 10.00000000000000000, 232.5000000000000000, -1.224646799147353256E-15 ) ) ;
#68076=CARTESIAN_POINT ( 'NONE',  ( 8.311093377946839666, 221.0937500034139589, 8.311093377946830785 ) ) ;
#68096=ORIENTED_EDGE ( 'NONE', *, *, #65174, .T. ) ;
#68127=CARTESIAN_POINT ( 'NONE',  ( -11.35316468749999963, 253.9062500034139873, 0.000000000000000000 ) ) ;
#68139=LINE ( 'NONE', #16434, #47000 ) ;
#68146=CARTESIAN_POINT ( 'NONE',  ( 8.311093377946839666, 221.0937500034139589, 8.311093377946829008 ) ) ;
#68159=CARTESIAN_POINT ( 'NONE',  ( -9.832129032723418760, 263.8020833367473301, -5.676582343749998927 ) ) ;
#68190=CARTESIAN_POINT ( 'NONE',  ( 4.999999999999997335, 221.4583333401612890, -8.660254037844387298 ) ) ;
#68211=CARTESIAN_POINT ( 'NONE',  ( 8.311093377946839666, 240.7812500034139873, 8.311093377946830785 ) ) ;
#68215=CARTESIAN_POINT ( 'NONE',  ( 5.676582343750005144, 255.8854166700806445, 9.832129032723416984 ) ) ;
#68235=EDGE_LOOP ( 'NONE', ( #57598, #31364, #8870, #39454, #38531 ) ) ;
#68242=CARTESIAN_POINT ( 'NONE',  ( -5.000000000000000888, 234.1666666666666856, -8.660254037844387298 ) ) ;
#68276=CARTESIAN_POINT ( 'NONE',  ( 9.832129032723416984, 221.8229166700806729, -5.676582343750003368 ) ) ;
#68295=CARTESIAN_POINT ( 'NONE',  ( 4.999999999999997335, 223.3333333333333144, -8.660254037844387298 ) ) ;
#68325=CARTESIAN_POINT ( 'NONE',  ( 8.311093377946834337, 247.3437500034139589, -8.311093377946836114 ) ) ;
#68342=CARTESIAN_POINT ( 'NONE',  ( 2.679491924311226292, 228.5416666666666288, -10.00000000000000000 ) ) ;
#68395=CYLINDRICAL_SURFACE ( 'NONE', #70169, 10.00000000000000000 ) ;
#68408=CARTESIAN_POINT ( 'NONE',  ( 8.660254037844389075, 237.0833333333333428, 4.999999999999997335 ) ) ;
#68494=CARTESIAN_POINT ( 'NONE',  ( -5.676582343749992710, 239.7395833367473301, 9.832129032723422313 ) ) ;
#68497=CARTESIAN_POINT ( 'NONE',  ( -10.09650806435399772, 220.0000000000001137, 1.283633865712600297 ) ) ;
#68529=CARTESIAN_POINT ( 'NONE',  ( -9.832129032723415207, 254.6354166700806729, 5.676582343750005144 ) ) ;
#68559=CARTESIAN_POINT ( 'NONE',  ( -8.660254037844385522, 218.5416666734946318, 5.000000000000004441 ) ) ;
#68572=DIRECTION ( 'NONE',  ( -0.000000000000000000, -1.000000000000000000, -0.000000000000000000 ) ) ;
#68583=CARTESIAN_POINT ( 'NONE',  ( -11.35316468749999785, 243.6979166700806445, -3.042071309553164848 ) ) ;
#68587=CARTESIAN_POINT ( 'NONE',  ( -8.311093377946834337, 259.8437500034140157, 8.311093377946837890 ) ) ;
#68604=EDGE_LOOP ( 'NONE', ( #54180, #66698, #68096 ) ) ;
#68611=CARTESIAN_POINT ( 'NONE',  ( -7.320508075688771932, 234.3750000000000000, -7.320508075688771932 ) ) ;
#68624=CARTESIAN_POINT ( 'NONE',  ( -7.320508075688771932, 259.3750000000000000, -7.320508075688771932 ) ) ;
#68631=PRODUCT_DEFINITION_SHAPE ( 'NONE', 'NONE',  #44081 ) ;
#68647=CARTESIAN_POINT ( 'NONE',  ( 7.320508075688771044, 261.2500000068278609, -7.320508075688771932 ) ) ;
#68695=CARTESIAN_POINT ( 'NONE',  ( 3.042071309553163960, 242.7604166700806729, -11.35316468749999785 ) ) ;
#68719=CARTESIAN_POINT ( 'NONE',  ( 0.000000000000000000, 265.0000000000000000, 0.000000000000000000 ) ) ;
#68728=CARTESIAN_POINT ( 'NONE',  ( -3.042071309553159075, 259.9479166700807014, 11.35316468749999963 ) ) ;
#68780=CARTESIAN_POINT ( 'NONE',  ( 7.320508075688776373, 236.8749999999999716, 7.320508075688767491 ) ) ;
#68867=CARTESIAN_POINT ( 'NONE',  ( 5.676582343749997150, 247.2395833367473301, -9.832129032723418760 ) ) ;
#68871=CARTESIAN_POINT ( 'NONE',  ( -10.00000000000000000, 220.0000000000000000, 0.000000000000000000 ) ) ;
#68902=CARTESIAN_POINT ( 'NONE',  ( 3.042071309553163516, 237.7604166700806445, -11.35316468749999785 ) ) ;
#68958=CARTESIAN_POINT ( 'NONE',  ( 5.676582343750005144, 245.5729166700806729, 9.832129032723416984 ) ) ;
#68964=CARTESIAN_POINT ( 'NONE',  ( 9.832129032723420536, 246.3020833367473301, 5.676582343749996262 ) ) ;
#68995=DIRECTION ( 'NONE',  ( 0.000000000000000000, 0.000000000000000000, -1.000000000000000000 ) ) ;
#69025=CARTESIAN_POINT ( 'NONE',  ( 5.000000000000004441, 254.7916666734946318, 8.660254037844385522 ) ) ;
#69072=CARTESIAN_POINT ( 'NONE',  ( -6.123233995736766282E-16, 256.8750000068279746, -10.00000000000000000 ) ) ;
#69073=CARTESIAN_POINT ( 'NONE',  ( -3.042071309553166181, 243.1770833367473017, -11.35316468749999608 ) ) ;
#69083=ORIENTED_EDGE ( 'NONE', *, *, #56464, .F. ) ;
#69087=CARTESIAN_POINT ( 'NONE',  ( 1.836970198721029589E-15, 226.2500000000000000, 10.00000000000000000 ) ) ;
#69107=CARTESIAN_POINT ( 'NONE',  ( -9.832129032723418760, 253.4895833367473017, -5.676582343749998927 ) ) ;
#69133=CARTESIAN_POINT ( 'NONE',  ( -10.00000000000000000, 262.9166666734946034, -2.679491924311226292 ) ) ;
#69157=CARTESIAN_POINT ( 'NONE',  ( 5.000000000000004441, 241.6666666666666572, 8.660254037844385522 ) ) ;
#69191=ADVANCED_FACE ( 'NONE', ( #9291 ), #73037, .F. ) ;
#69197=ORIENTED_EDGE ( 'NONE', *, *, #21416, .F. ) ;
#69244=CARTESIAN_POINT ( 'NONE',  ( -9.832129032723418760, 248.4895833367473301, -5.676582343749998927 ) ) ;
#69247=CARTESIAN_POINT ( 'NONE',  ( -9.720591898830647892, 220.0000000000000000, 4.125769721654016564 ) ) ;
#69272=CARTESIAN_POINT ( 'NONE',  ( 1.836970198721029589E-15, 226.2500000000000000, 10.00000000000000000 ) ) ;
#69278=CARTESIAN_POINT ( 'NONE',  ( 8.311093377946834337, 247.3437500034139589, -8.311093377946836114 ) ) ;
#69330=CARTESIAN_POINT ( 'NONE',  ( -11.35316468749999608, 239.1145833367473301, 3.042071309553173730 ) ) ;
#69335=CARTESIAN_POINT ( 'NONE',  ( -5.676582343750000703, 243.3854166700806445, -9.832129032723418760 ) ) ;
#69393=CARTESIAN_POINT ( 'NONE',  ( 2.679491924311235174, 249.5833333401613174, 9.999999999999998224 ) ) ;
#69394=CARTESIAN_POINT ( 'NONE',  ( 1.836970198721029589E-15, 249.3750000068279746, 10.00000000000000000 ) ) ;
#69443=CARTESIAN_POINT ( 'NONE',  ( 11.35316468749999963, 246.7187500034139873, -1.390361679473963556E-15 ) ) ;
#69453=CARTESIAN_POINT ( 'NONE',  ( -2.679491924311165008, 241.0416666666666572, 10.00000000000003553 ) ) ;
#69481=CARTESIAN_POINT ( 'NONE',  ( -3.042071309553159075, 244.9479166700806445, 11.35316468749999963 ) ) ;
#69487=CARTESIAN_POINT ( 'NONE',  ( 0.000000000000000000, 0.000000000000000000, 19.00000000000000000 ) ) ;
#69531=CARTESIAN_POINT ( 'NONE',  ( 2.679491924311225848, 233.5416666666666572, -10.00000000000000000 ) ) ;
#69573=LINE ( 'NONE', #41272, #6977 ) ;
#69618=CARTESIAN_POINT ( 'NONE',  ( 5.676582343750005144, 240.5729166700806445, 9.832129032723416984 ) ) ;
#69651=CARTESIAN_POINT ( 'NONE',  ( 9.832129032723416984, 242.1354166700806445, -5.676582343750003368 ) ) ;
#69696=CIRCLE ( 'NONE', #38414, 10.00000000000000000 ) ;
#69707=CARTESIAN_POINT ( 'NONE',  ( 8.311093377946839666, 235.7812500034139589, 8.311093377946830785 ) ) ;
#69711=CARTESIAN_POINT ( 'NONE',  ( -8.311093377946836114, 238.5937500034139589, -8.311093377946836114 ) ) ;
#69765=CARTESIAN_POINT ( 'NONE',  ( -5.000000000000000888, 257.2916666734946034, -8.660254037844387298 ) ) ;
#69815=CARTESIAN_POINT ( 'NONE',  ( -9.832129032723418760, 233.8020833367473301, -5.676582343749998927 ) ) ;
#69856=CARTESIAN_POINT ( 'NONE',  ( 3.042071309553163960, 242.4479166700806729, -11.35316468749999785 ) ) ;
#69860=FACE_BOUND ( 'NONE', #38589, .T. ) ;
#69872=( BOUNDED_CURVE ( )  B_SPLINE_CURVE ( 2, ( #67561, #49830, #61149, #44176, #43413, #15116, #55880, #60774, #67190, #37779, #73221, #60398, #72472 ),
 .UNSPECIFIED., .F., .F. ) 
 B_SPLINE_CURVE_WITH_KNOTS ( ( 3, 2, 2, 2, 2, 2, 3 ),
 ( 0.5833333333333331483, 0.5925925925925923377, 0.6018518518518516380, 0.6111111111111109384, 0.6203703703703702388, 0.6296296296296295392, 0.6388888888888887285 ),
 .UNSPECIFIED. ) 
 CURVE ( )  GEOMETRIC_REPRESENTATION_ITEM ( )  RATIONAL_B_SPLINE_CURVE ( ( 1.000000000000000888, 0.9659258262890675351, 1.000000000000000000, 0.9659258262890683122, 1.000000000000000000, 0.9659258262890683122, 1.000000000000000000, 0.9659258262890683122, 1.000000000000000000, 0.9659258262890683122, 1.000000000000000000, 0.9659258262890687563, 0.9999999999999995559 ) ) 
 REPRESENTATION_ITEM ( '' )  );
#69907=CARTESIAN_POINT ( 'NONE',  ( -9.999999999999998224, 220.2083333333333428, 2.679491924311235618 ) ) ;
#69984=ORIENTED_EDGE ( 'NONE', *, *, #56237, .T. ) ;
#69994=CARTESIAN_POINT ( 'NONE',  ( 5.676582343749997150, 242.2395833367473301, -9.832129032723418760 ) ) ;
#70010=ORIENTED_EDGE ( 'NONE', *, *, #66617, .T. ) ;
#70023=CARTESIAN_POINT ( 'NONE',  ( -4.999999999999992895, 238.9583333401613174, 8.660254037844390851 ) ) ;
#70028=CARTESIAN_POINT ( 'NONE',  ( 3.042071309553173286, 250.6770833367473301, 11.35316468749999608 ) ) ;
#70085=CARTESIAN_POINT ( 'NONE',  ( -8.311093377946834337, 234.5312500034139589, 8.311093377946837890 ) ) ;
#70089=CARTESIAN_POINT ( 'NONE',  ( 3.042071309553163960, 242.7604166700806729, -11.35316468749999785 ) ) ;
#70140=CARTESIAN_POINT ( 'NONE',  ( 0.000000000000000000, 45.00000000000000000, 8.749999999999998224 ) ) ;
#70145=CARTESIAN_POINT ( 'NONE',  ( -7.320508075688771932, 257.5000000068279746, -7.320508075688771932 ) ) ;
#70147=EDGE_LOOP ( 'NONE', ( #26482, #1578, #7667, #37282 ) ) ;
#70168=LINE ( 'NONE', #16318, #56643 ) ;
#70169=AXIS2_PLACEMENT_3D ( 'NONE', #34092, #62726, #22734 ) ;
#70191=CARTESIAN_POINT ( 'NONE',  ( -9.832129032723418760, 223.8020833367473301, -5.676582343749998927 ) ) ;
#70199=CARTESIAN_POINT ( 'NONE',  ( -7.320508075688771932, 239.3749999999999716, -7.320508075688771932 ) ) ;
#70203=CIRCLE ( 'NONE', #66575, 19.00000000000003553 ) ;
#70229=CARTESIAN_POINT ( 'NONE',  ( -3.042071309553166181, 247.8645833367472733, -11.35316468749999608 ) ) ;
#70244=ADVANCED_FACE ( 'NONE', ( #16343 ), #26934, .F. ) ;
#70275=CARTESIAN_POINT ( 'NONE',  ( -8.660254037844385522, 220.4166666666666856, 5.000000000000004441 ) ) ;
#70314=CARTESIAN_POINT ( 'NONE',  ( 0.000000000000000000, 45.00000000000000000, -11.00000000000000000 ) ) ;
#70334=VECTOR ( 'NONE', #55589, 1000.000000000000000 ) ;
#70361=CARTESIAN_POINT ( 'NONE',  ( -3.042071309553159075, 234.9479166700806445, 11.35316468749999963 ) ) ;
#70365=CARTESIAN_POINT ( 'NONE',  ( -7.320508075688771932, 264.3750000000000568, -7.320508075688771932 ) ) ;
#70383=VECTOR ( 'NONE', #13617, 1000.000000000000000 ) ;
#70390=EDGE_LOOP ( 'NONE', ( #24765, #69197, #52039, #64853, #59395, #73135, #42482, #22816, #32185, #60361, #60880, #62181, #30744, #63078, #71780, #12954, #56368, #45348, #20134, #23657, #66568, #7522, #37950, #63892 ) ) ;
#70393=CARTESIAN_POINT ( 'NONE',  ( -11.35316468749999608, 229.4270833367473301, 3.042071309553173730 ) ) ;
#70445=CARTESIAN_POINT ( 'NONE',  ( 3.042071309553163516, 227.4479166700806445, -11.35316468749999785 ) ) ;
#70449=CARTESIAN_POINT ( 'NONE',  ( -11.35316468749999963, 234.2187500034139873, 0.000000000000000000 ) ) ;
#70497=ORIENTED_EDGE ( 'NONE', *, *, #68024, .F. ) ;
#70501=CARTESIAN_POINT ( 'NONE',  ( 5.000000000000004441, 261.6666666666666856, 8.660254037844385522 ) ) ;
#70504=CARTESIAN_POINT ( 'NONE',  ( 2.679491924311235174, 254.5833333401613174, 9.999999999999998224 ) ) ;
#70513=EDGE_CURVE ( 'NONE', #26674, #64909, #64159, .T. ) ;
#70549=CARTESIAN_POINT ( 'NONE',  ( -6.123233995736766282E-16, 248.7500000000000284, -10.00000000000000000 ) ) ;
#70551=CARTESIAN_POINT ( 'NONE',  ( -5.676582343749992710, 225.0520833367473017, 9.832129032723422313 ) ) ;
#70575=CARTESIAN_POINT ( 'NONE',  ( 0.000000000000000000, 0.000000000000000000, 0.000000000000000000 ) ) ;
#70586=CARTESIAN_POINT ( 'NONE',  ( 5.676582343750005144, 245.5729166700806729, 9.832129032723416984 ) ) ;
#70633=CARTESIAN_POINT ( 'NONE',  ( -5.676582343750000703, 263.3854166700806445, -9.832129032723418760 ) ) ;
#70662=ORIENTED_EDGE ( 'NONE', *, *, #34321, .T. ) ;
#70715=CARTESIAN_POINT ( 'NONE',  ( 5.676582343749997150, 227.2395833367473301, -9.832129032723418760 ) ) ;
#70724=CARTESIAN_POINT ( 'NONE',  ( 2.679491924311292905, 239.5833333401613174, 9.999999999999968026 ) ) ;
#70752=CARTESIAN_POINT ( 'NONE',  ( 8.311093377946839666, 226.0937500034139589, 8.311093377946830785 ) ) ;
#70775=( BOUNDED_CURVE ( )  B_SPLINE_CURVE ( 2, ( #69272, #22869, #45882, #52666, #40977, #57217, #11556, #63983, #53038, #12297, #74557, #28906, #17958 ),
 .UNSPECIFIED., .F., .F. ) 
 B_SPLINE_CURVE_WITH_KNOTS ( ( 3, 2, 2, 2, 2, 2, 3 ),
 ( 0.8611111111111111605, 0.8703703703703703498, 0.8796296296296297612, 0.8888888888888889506, 0.8981481481481482509, 0.9074074074074076623, 0.9166666666666668517 ),
 .UNSPECIFIED. ) 
 CURVE ( )  GEOMETRIC_REPRESENTATION_ITEM ( )  RATIONAL_B_SPLINE_CURVE ( ( 1.000000000000000000, 0.9659258262890683122, 1.000000000000000000, 0.9659258262890683122, 1.000000000000000000, 0.9659258262890683122, 1.000000000000000000, 0.9659258262890683122, 1.000000000000000000, 0.9659258262890683122, 1.000000000000000000, 0.9659258262890675351, 1.000000000000000888 ) ) 
 REPRESENTATION_ITEM ( '' )  );
#70804=CARTESIAN_POINT ( 'NONE',  ( -8.311093377946836114, 233.2812500034139589, -8.311093377946836114 ) ) ;
#70811=CARTESIAN_POINT ( 'NONE',  ( 11.35316468749999963, 226.7187500034139873, -1.390361679473963556E-15 ) ) ;
#70865=FACE_OUTER_BOUND ( 'NONE', #2184, .T. ) ;
#70866=CARTESIAN_POINT ( 'NONE',  ( 10.00000000000000000, 262.5000000000000000, -1.224646799147353256E-15 ) ) ;
#70869=CARTESIAN_POINT ( 'NONE',  ( -5.000000000000000888, 237.2916666734946318, -8.660254037844387298 ) ) ;
#70912=CARTESIAN_POINT ( 'NONE',  ( -6.123233995736766282E-16, 241.8750000068280031, -10.00000000000000000 ) ) ;
#70916=CARTESIAN_POINT ( 'NONE',  ( -8.311093377946834337, 234.8437500034139305, 8.311093377946837890 ) ) ;
#70942=ORIENTED_EDGE ( 'NONE', *, *, #41301, .F. ) ;
#70948=CARTESIAN_POINT ( 'NONE',  ( 3.042071309553173286, 235.3645833367473017, 11.35316468749999608 ) ) ;
#70995=CARTESIAN_POINT ( 'NONE',  ( 5.676582343749997150, 262.5520833367473301, -9.832129032723418760 ) ) ;
#71031=ORIENTED_EDGE ( 'NONE', *, *, #58612, .T. ) ;
#71075=( BOUNDED_SURFACE ( )  B_SPLINE_SURFACE ( 1, 2, ( 
 ( #13724, #48442, #64329, #70365, #18679, #24328, #8458, #71445, #36035, #36769, #30732, #19773, #65051, #71821, #2062, #71080, #31478, #41688, #59051, #30367, #59780, #54501, #1711, #65798, #19397, #31093, #35666, #47699, #42781, #8090, #25795, #58680, #6989, #29999, #53014, #66924, #49188, #20892, #72198, #20511, #26927, #32230, #27296, #56358, #10332, #43914, #3554, #4677, #66541, #44662, #67302, #15601, #38261, #32613, #27673, #32992, #3182, #61642, #14476, #72959, #20140, #15229, #72587, #14850, #26544, #49569, #67675, #9594, #54873, #15974, #37890, #61264, #43156, #43526, #55620, #50679, #3937, #21265, #31850, #49945, #39003, #9959, #73333, #44289, #55992, #60888, #26169, #38640, #4306, #8839, #66172, #9210, #50312, #21637, #62007, #33357, #55248, #37515, #60514, #11813, #16335, #63866, #23128, #17843, #51057, #5792, #28789, #56734, #45769, #28421, #17466, #29172, #69157, #11444, #6533, #58234, #22370, #17090, #6163, #40486, #34852, #10699, #57487, #29539, #11078, #51804, #57857, #45392, #46512, #57101, #34479, #74440, #40112, #51428, #68408, #68780, #73697, #63118, #16708, #52187, #35215, #46140, #22748, #62369, #39738, #33732, #63491, #152, #22009, #40859, #45036, #69531, #23498, #518, #12178, #5053, #68044, #39373, #28048, #74070, #62738, #34106, #5415, #13642, #53662, #58591, #19682, #18587, #12909, #1256, #71357, #47248, #59692, #8367, #13273, #47982, #31007, #7269, #53297, #1622, #6897, #14009, #64239, #29908, #18952, #35943, #54032, #23874, #24234, #52923, #42692, #24602, #30277, #2342, #41232, #12549, #64963, #52550, #65705, #889, #25336, #48351, #59328, #1974, #35577, #42322, #37045, #46884, #36312, #8001, #47609, #60046, #36680, #24966, #70275, #69907, #41598 ),
 ( #64613, #58962, #19311, #18219, #70633, #41956, #7638, #30644, #70995, #65340, #38174, #43439, #38553, #67590, #21551, #55159, #14762, #15886, #3091, #55908, #3845, #26841, #49478, #43825, #38918, #44203, #14389, #72874, #25704, #9507, #31383, #3464, #9122, #26076, #37802, #60797, #4219, #20806, #32522, #67216, #54409, #55535, #26453, #72497, #20423, #43063, #61920, #44577, #27208, #54780, #50225, #66079, #73246, #49097, #15513, #32138, #49856, #72110, #2716, #66839, #66454, #15142, #61177, #21178, #37423, #61554, #9875, #32903, #48724, #71731, #20045, #60423, #8750, #31760, #67956, #63401, #27584, #6074, #46429, #74351, #16249, #68325, #39287, #39658, #69443, #5333, #51342, #28701, #44949, #57020, #29082, #50971, #56271, #23043, #22288, #23414, #46054, #62656, #57394, #17379, #51715, #69073, #21918, #68695, #17754, #45311, #17005, #40403, #33643, #57769, #16623, #22661, #10990, #45680, #34023, #56650, #28335, #40769, #40031, #27966, #11727, #10245, #34393, #63033, #73611, #73985, #62288, #62, #11358, #33272, #52102, #4590, #434, #34767, #5702, #50593, #10617, #4965, #48267, #19593, #24521, #70916, #12823, #25250, #24877, #64886, #69815, #30921, #29823, #24147, #12461, #7916, #58504, #19230, #63776, #47526, #59243, #42236, #18500, #64525, #35858, #18131, #71274, #803, #41147, #30190, #47159, #65249, #35130, #35492, #64152, #53943, #58873, #41509, #13554, #52465, #23789, #46793, #59603, #6810, #7184, #12093, #52835, #53207, #58146, #1541, #13187, #1168, #70551, #36592, #53576, #2257, #36225, #1890, #70191, #18867, #41873, #7553, #30560, #6453, #47896, #29456, #22110, #45134, #55442, #25622, #14675, #68146, #3752, #59965, #33839, #66747, #62474, #19967, #49386, #72405, #48636 ) ),
 .UNSPECIFIED., .F., .F., .F. ) 
 B_SPLINE_SURFACE_WITH_KNOTS ( ( 2, 2 ),
 ( 3, 2, 2, 2, 2, 2, 2, 2, 2, 2, 2, 2, 2, 2, 2, 2, 2, 2, 2, 2, 2, 2, 2, 2, 2, 2, 2, 2, 2, 2, 2, 2, 2, 2, 2, 2, 2, 2, 2, 2, 2, 2, 2, 2, 2, 2, 2, 2, 2, 2, 2, 2, 2, 2, 2, 2, 2, 2, 2, 2, 2, 2, 2, 2, 2, 2, 2, 2, 2, 2, 2, 2, 2, 2, 2, 2, 2, 2, 2, 2, 2, 2, 2, 2, 2, 2, 2, 2, 2, 2, 2, 2, 2, 2, 2, 2, 2, 2, 2, 2, 2, 2, 2, 2, 2, 2, 2, 2, 3 ),
 ( 0.000000000000000000, 1.000000000000000000 ),
 ( 0.000000000000000000, 0.009259259259259258745, 0.01851851851851851749, 0.02777777777777777624, 0.03703703703703703498, 0.04629629629629629373, 0.05555555555555555247, 0.06481481481481481122, 0.07407407407407406996, 0.08333333333333332871, 0.09259259259259258745, 0.1018518518518518462, 0.1111111111111111049, 0.1203703703703703637, 0.1296296296296296224, 0.1388888888888888951, 0.1481481481481481399, 0.1574074074074074125, 0.1666666666666666574, 0.1759259259259259300, 0.1851851851851851749, 0.1944444444444444475, 0.2037037037037036924, 0.2129629629629629650, 0.2222222222222222099, 0.2314814814814814825, 0.2407407407407407274, 0.2500000000000000000, 0.2592592592592592449, 0.2685185185185185452, 0.2777777777777777901, 0.2870370370370370350, 0.2962962962962962798, 0.3055555555555555802, 0.3148148148148148251, 0.3240740740740740700, 0.3333333333333333148, 0.3425925925925926152, 0.3518518518518518601, 0.3611111111111111049, 0.3703703703703703498, 0.3796296296296296502, 0.3888888888888888951, 0.3981481481481481399, 0.4074074074074073848, 0.4166666666666666852, 0.4259259259259259300, 0.4351851851851851749, 0.4444444444444444198, 0.4537037037037037202, 0.4629629629629629650, 0.4722222222222222099, 0.4814814814814814548, 0.4907407407407407551, 0.5000000000000000000, 0.5092592592592593004, 0.5185185185185184897, 0.5277777777777777901, 0.5370370370370370905, 0.5462962962962962798, 0.5555555555555555802, 0.5648148148148147696, 0.5740740740740740700, 0.5833333333333333703, 0.5925925925925925597, 0.6018518518518518601, 0.6111111111111111605, 0.6203703703703703498, 0.6296296296296296502, 0.6388888888888888395, 0.6481481481481481399, 0.6574074074074074403, 0.6666666666666666297, 0.6759259259259259300, 0.6851851851851852304, 0.6944444444444444198, 0.7037037037037037202, 0.7129629629629629095, 0.7222222222222222099, 0.7314814814814815103, 0.7407407407407406996, 0.7500000000000000000, 0.7592592592592593004, 0.7685185185185184897, 0.7777777777777777901, 0.7870370370370370905, 0.7962962962962962798, 0.8055555555555555802, 0.8148148148148147696, 0.8240740740740740700, 0.8333333333333333703, 0.8425925925925925597, 0.8518518518518518601, 0.8611111111111111605, 0.8703703703703703498, 0.8796296296296296502, 0.8888888888888888395, 0.8981481481481481399, 0.9074074074074074403, 0.9166666666666666297, 0.9259259259259259300, 0.9351851851851852304, 0.9444444444444444198, 0.9537037037037037202, 0.9629629629629629095, 0.9722222222222222099, 0.9814814814814815103, 0.9907407407407406996, 1.000000000000000000 ),
 .UNSPECIFIED. ) 
 GEOMETRIC_REPRESENTATION_ITEM ( )  RATIONAL_B_SPLINE_SURFACE ( (
 ( 1.000000000000000000, 0.9659258262890683122, 1.000000000000000000, 0.9659258262890683122, 1.000000000000000000, 0.9659258262890683122, 1.000000000000000000, 0.9659258262890683122, 1.000000000000000000, 0.9659258262890683122, 1.000000000000000000, 0.9659258262890683122, 1.000000000000000000, 0.9659258262890683122, 1.000000000000000000, 0.9659258262890683122, 1.000000000000000000, 0.9659258262890683122, 1.000000000000000000, 0.9659258262890683122, 1.000000000000000000, 0.9659258262890683122, 1.000000000000000000, 0.9659258262890683122, 1.000000000000000000, 0.9659258262890683122, 1.000000000000000000, 0.9659258262890683122, 1.000000000000000000, 0.9659258262890683122, 1.000000000000000000, 0.9659258262890683122, 1.000000000000000000, 0.9659258262890683122, 1.000000000000000000, 0.9659258262890683122, 1.000000000000000000, 0.9659258262890683122, 1.000000000000000000, 0.9659258262890683122, 1.000000000000000000, 0.9659258262890683122, 1.000000000000000000, 0.9659258262890683122, 1.000000000000000000, 0.9659258262890683122, 1.000000000000000000, 0.9659258262890683122, 1.000000000000000000, 0.9659258262890683122, 1.000000000000000000, 0.9659258262890683122, 1.000000000000000000, 0.9659258262890683122, 1.000000000000000000, 0.9659258262890683122, 1.000000000000000000, 0.9659258262890683122, 1.000000000000000000, 0.9659258262890683122, 1.000000000000000000, 0.9659258262890683122, 1.000000000000000000, 0.9659258262890683122, 1.000000000000000000, 0.9659258262890683122, 1.000000000000000000, 0.9659258262890683122, 1.000000000000000000, 0.9659258262890683122, 1.000000000000000000, 0.9659258262890683122, 1.000000000000000000, 0.9659258262890683122, 1.000000000000000000, 0.9659258262890683122, 1.000000000000000000, 0.9659258262890683122, 1.000000000000000000, 0.9659258262890683122, 1.000000000000000000, 0.9659258262890683122, 1.000000000000000000, 0.9659258262890683122, 1.000000000000000000, 0.9659258262890683122, 1.000000000000000000, 0.9659258262890683122, 1.000000000000000000, 0.9659258262890683122, 1.000000000000000000, 0.9659258262890683122, 1.000000000000000000, 0.9659258262890683122, 1.000000000000000000, 0.9659258262890683122, 1.000000000000000000, 0.9659258262890683122, 1.000000000000000000, 0.9659258262890683122, 1.000000000000000000, 0.9659258262890683122, 1.000000000000000000, 0.9659258262890683122, 1.000000000000000000, 0.9659258262890683122, 1.000000000000000000, 0.9659258262890683122, 1.000000000000000000, 0.9659258262890683122, 1.000000000000000000, 0.9659258262890683122, 1.000000000000000000, 0.9659258262890683122, 1.000000000000000000, 0.9659258262890683122, 1.000000000000000000, 0.9659258262890683122, 1.000000000000000000, 0.9659258262890683122, 1.000000000000000000, 0.9659258262890683122, 1.000000000000000000, 0.9659258262890683122, 1.000000000000000000, 0.9659258262890683122, 1.000000000000000000, 0.9659258262890683122, 1.000000000000000000, 0.9659258262890683122, 1.000000000000000000, 0.9659258262890683122, 1.000000000000000000, 0.9659258262890683122, 1.000000000000000000, 0.9659258262890683122, 1.000000000000000000, 0.9659258262890683122, 1.000000000000000000, 0.9659258262890683122, 1.000000000000000000, 0.9659258262890683122, 1.000000000000000000, 0.9659258262890683122, 1.000000000000000000, 0.9659258262890683122, 1.000000000000000000, 0.9659258262890683122, 1.000000000000000000, 0.9659258262890683122, 1.000000000000000000, 0.9659258262890683122, 1.000000000000000000, 0.9659258262890683122, 1.000000000000000000, 0.9659258262890683122, 1.000000000000000000, 0.9659258262890683122, 1.000000000000000000, 0.9659258262890683122, 1.000000000000000000, 0.9659258262890683122, 1.000000000000000000, 0.9659258262890683122, 1.000000000000000000, 0.9659258262890683122, 1.000000000000000000, 0.9659258262890683122, 1.000000000000000000, 0.9659258262890683122, 1.000000000000000000, 0.9659258262890683122, 1.000000000000000000, 0.9659258262890683122, 1.000000000000000000, 0.9659258262890683122, 1.000000000000000000, 0.9659258262890683122, 1.000000000000000000, 0.9659258262890683122, 1.000000000000000000, 0.9659258262890683122, 1.000000000000000000, 0.9659258262890683122, 1.000000000000000000, 0.9659258262890683122, 1.000000000000000000, 0.9659258262890683122, 1.000000000000000000, 0.9659258262890683122, 1.000000000000000000, 0.9659258262890683122, 1.000000000000000000, 0.9659258262890683122, 1.000000000000000000, 0.9659258262890683122, 1.000000000000000000, 0.9659258262890683122, 1.000000000000000000, 0.9659258262890683122, 1.000000000000000000, 0.9659258262890683122, 1.000000000000000000, 0.9659258262890683122, 1.000000000000000000, 0.9659258262890683122, 1.000000000000000000, 0.9659258262890683122, 1.000000000000000000, 0.9659258262890683122, 1.000000000000000000, 0.9659258262890683122, 1.000000000000000000, 0.9659258262890683122, 1.000000000000000000, 0.9659258262890683122, 1.000000000000000000),
 ( 1.000000000000000000, 0.9659258262890683122, 1.000000000000000000, 0.9659258262890683122, 1.000000000000000000, 0.9659258262890683122, 1.000000000000000000, 0.9659258262890683122, 1.000000000000000000, 0.9659258262890683122, 1.000000000000000000, 0.9659258262890683122, 1.000000000000000000, 0.9659258262890683122, 1.000000000000000000, 0.9659258262890683122, 1.000000000000000000, 0.9659258262890683122, 1.000000000000000000, 0.9659258262890683122, 1.000000000000000000, 0.9659258262890683122, 1.000000000000000000, 0.9659258262890683122, 1.000000000000000000, 0.9659258262890683122, 1.000000000000000000, 0.9659258262890683122, 1.000000000000000000, 0.9659258262890683122, 1.000000000000000000, 0.9659258262890683122, 1.000000000000000000, 0.9659258262890683122, 1.000000000000000000, 0.9659258262890683122, 1.000000000000000000, 0.9659258262890683122, 1.000000000000000000, 0.9659258262890683122, 1.000000000000000000, 0.9659258262890683122, 1.000000000000000000, 0.9659258262890683122, 1.000000000000000000, 0.9659258262890683122, 1.000000000000000000, 0.9659258262890683122, 1.000000000000000000, 0.9659258262890683122, 1.000000000000000000, 0.9659258262890683122, 1.000000000000000000, 0.9659258262890683122, 1.000000000000000000, 0.9659258262890683122, 1.000000000000000000, 0.9659258262890683122, 1.000000000000000000, 0.9659258262890683122, 1.000000000000000000, 0.9659258262890683122, 1.000000000000000000, 0.9659258262890683122, 1.000000000000000000, 0.9659258262890683122, 1.000000000000000000, 0.9659258262890683122, 1.000000000000000000, 0.9659258262890683122, 1.000000000000000000, 0.9659258262890683122, 1.000000000000000000, 0.9659258262890683122, 1.000000000000000000, 0.9659258262890683122, 1.000000000000000000, 0.9659258262890683122, 1.000000000000000000, 0.9659258262890683122, 1.000000000000000000, 0.9659258262890683122, 1.000000000000000000, 0.9659258262890683122, 1.000000000000000000, 0.9659258262890683122, 1.000000000000000000, 0.9659258262890683122, 1.000000000000000000, 0.9659258262890683122, 1.000000000000000000, 0.9659258262890683122, 1.000000000000000000, 0.9659258262890683122, 1.000000000000000000, 0.9659258262890683122, 1.000000000000000000, 0.9659258262890683122, 1.000000000000000000, 0.9659258262890683122, 1.000000000000000000, 0.9659258262890683122, 1.000000000000000000, 0.9659258262890683122, 1.000000000000000000, 0.9659258262890683122, 1.000000000000000000, 0.9659258262890683122, 1.000000000000000000, 0.9659258262890683122, 1.000000000000000000, 0.9659258262890683122, 1.000000000000000000, 0.9659258262890683122, 1.000000000000000000, 0.9659258262890683122, 1.000000000000000000, 0.9659258262890683122, 1.000000000000000000, 0.9659258262890683122, 1.000000000000000000, 0.9659258262890683122, 1.000000000000000000, 0.9659258262890683122, 1.000000000000000000, 0.9659258262890683122, 1.000000000000000000, 0.9659258262890683122, 1.000000000000000000, 0.9659258262890683122, 1.000000000000000000, 0.9659258262890683122, 1.000000000000000000, 0.9659258262890683122, 1.000000000000000000, 0.9659258262890683122, 1.000000000000000000, 0.9659258262890683122, 1.000000000000000000, 0.9659258262890683122, 1.000000000000000000, 0.9659258262890683122, 1.000000000000000000, 0.9659258262890683122, 1.000000000000000000, 0.9659258262890683122, 1.000000000000000000, 0.9659258262890683122, 1.000000000000000000, 0.9659258262890683122, 1.000000000000000000, 0.9659258262890683122, 1.000000000000000000, 0.9659258262890683122, 1.000000000000000000, 0.9659258262890683122, 1.000000000000000000, 0.9659258262890683122, 1.000000000000000000, 0.9659258262890683122, 1.000000000000000000, 0.9659258262890683122, 1.000000000000000000, 0.9659258262890683122, 1.000000000000000000, 0.9659258262890683122, 1.000000000000000000, 0.9659258262890683122, 1.000000000000000000, 0.9659258262890683122, 1.000000000000000000, 0.9659258262890683122, 1.000000000000000000, 0.9659258262890683122, 1.000000000000000000, 0.9659258262890683122, 1.000000000000000000, 0.9659258262890683122, 1.000000000000000000, 0.9659258262890683122, 1.000000000000000000, 0.9659258262890683122, 1.000000000000000000, 0.9659258262890683122, 1.000000000000000000, 0.9659258262890683122, 1.000000000000000000, 0.9659258262890683122, 1.000000000000000000, 0.9659258262890683122, 1.000000000000000000, 0.9659258262890683122, 1.000000000000000000, 0.9659258262890683122, 1.000000000000000000, 0.9659258262890683122, 1.000000000000000000, 0.9659258262890683122, 1.000000000000000000, 0.9659258262890683122, 1.000000000000000000, 0.9659258262890683122, 1.000000000000000000, 0.9659258262890683122, 1.000000000000000000, 0.9659258262890683122, 1.000000000000000000, 0.9659258262890683122, 1.000000000000000000, 0.9659258262890683122, 1.000000000000000000, 0.9659258262890683122, 1.000000000000000000, 0.9659258262890683122, 1.000000000000000000, 0.9659258262890683122, 1.000000000000000000) ) ) 
 REPRESENTATION_ITEM ( '' )  SURFACE ( )  );
#71076=CARTESIAN_POINT ( 'NONE',  ( -9.832129032723418760, 233.4895833367473301, -5.676582343749998927 ) ) ;
#71080=CARTESIAN_POINT ( 'NONE',  ( 7.320508075688776373, 261.8750000000000568, 7.320508075688767491 ) ) ;
#71084=CARTESIAN_POINT ( 'NONE',  ( -6.123233995736766282E-16, 241.8750000068280031, -10.00000000000000000 ) ) ;
#71092=ORIENTED_EDGE ( 'NONE', *, *, #20887, .T. ) ;
#71109=CARTESIAN_POINT ( 'NONE',  ( 3.042071309553173286, 230.6770833367473301, 11.35316468749999608 ) ) ;
#71118=CARTESIAN_POINT ( 'NONE',  ( 6.250510011802020927, 219.9999999999999432, 8.054087016449219760 ) ) ;
#71126=DIRECTION ( 'NONE',  ( 0.000000000000000000, 0.000000000000000000, -1.000000000000000000 ) ) ;
#71163=CARTESIAN_POINT ( 'NONE',  ( 9.832129032723416984, 236.8229166700806445, -5.676582343750003368 ) ) ;
#71166=CARTESIAN_POINT ( 'NONE',  ( -8.311093377946836114, 223.5937500034139589, -8.311093377946836114 ) ) ;
#71173=CARTESIAN_POINT ( 'NONE',  ( -9.526279441628823008, 219.1190169426842829, 5.500000000000005329 ) ) ;
#71224=CARTESIAN_POINT ( 'NONE',  ( 4.999999999999997335, 241.4583333401613174, -8.660254037844387298 ) ) ;
#71237=EDGE_CURVE ( 'NONE', #64909, #8328, #38610, .T. ) ;
#71250=CARTESIAN_POINT ( 'NONE',  ( 0.000000000000000000, 0.000000000000000000, 0.000000000000000000 ) ) ;
#71254=ORIENTED_EDGE ( 'NONE', *, *, #15505, .T. ) ;
#71274=CARTESIAN_POINT ( 'NONE',  ( 2.085542519210945334E-15, 230.4687500034139873, 11.35316468749999963 ) ) ;
#71281=CARTESIAN_POINT ( 'NONE',  ( -5.000000000000000888, 239.1666666666666572, -8.660254037844387298 ) ) ;
#71313=CARTESIAN_POINT ( 'NONE',  ( 11.35316468749999963, 236.4062500034140157, -1.390361679473963556E-15 ) ) ;
#71357=CARTESIAN_POINT ( 'NONE',  ( -8.660254037844387298, 229.5833333333333712, -4.999999999999999112 ) ) ;
#71376=CARTESIAN_POINT ( 'NONE',  ( -4.999999999999992895, 230.8333333333333428, 8.660254037844390851 ) ) ;
#71383=DIRECTION ( 'NONE',  ( 0.000000000000000000, 0.000000000000000000, -1.000000000000000000 ) ) ;
#71441=CARTESIAN_POINT ( 'NONE',  ( 9.832129032723420536, 225.9895833367473585, 5.676582343749996262 ) ) ;
#71445=CARTESIAN_POINT ( 'NONE',  ( 2.679491924311225848, 263.5416666666666856, -10.00000000000000000 ) ) ;
#71476=CARTESIAN_POINT ( 'NONE',  ( 11.35316468749999608, 236.9270833367473017, -3.042071309553167513 ) ) ;
#71529=CARTESIAN_POINT ( 'NONE',  ( -3.042071309553159075, 219.9479166700806445, 11.35316468749999963 ) ) ;
#71532=CARTESIAN_POINT ( 'NONE',  ( -3.042071309553166181, 223.1770833367473017, -11.35316468749999608 ) ) ;
#71536=DIRECTION ( 'NONE',  ( -0.000000000000000000, -1.000000000000000000, -0.000000000000000000 ) ) ;
#71550=ADVANCED_FACE ( 'NONE', ( #684 ), #34265, .F. ) ;
#71564=ORIENTED_EDGE ( 'NONE', *, *, #57824, .F. ) ;
#71569=CARTESIAN_POINT ( 'NONE',  ( 2.679491924311226292, 233.5416666666666856, -10.00000000000000000 ) ) ;
#71592=CARTESIAN_POINT ( 'NONE',  ( 8.660254037844385522, 262.9166666666666856, -5.000000000000003553 ) ) ;
#71595=CARTESIAN_POINT ( 'NONE',  ( 8.660254037844389075, 240.2083333401613174, 4.999999999999997335 ) ) ;
#71616=CARTESIAN_POINT ( 'NONE',  ( -9.832129032723418760, 258.4895833367473301, -5.676582343749998927 ) ) ;
#71659=CARTESIAN_POINT ( 'NONE',  ( -8.660254037844385522, 260.4166666666666856, 5.000000000000004441 ) ) ;
#71673=DIRECTION ( 'NONE',  ( -0.000000000000000000, -1.000000000000000000, -0.000000000000000000 ) ) ;
#71681=CARTESIAN_POINT ( 'NONE',  ( -6.951808397369817780E-16, 237.6562500034140157, -11.35316468749999963 ) ) ;
#71731=CARTESIAN_POINT ( 'NONE',  ( -8.311093377946834337, 249.8437500034139589, 8.311093377946837890 ) ) ;
#71751=CARTESIAN_POINT ( 'NONE',  ( -8.660254037844387298, 229.5833333333333712, -4.999999999999999112 ) ) ;
#71776=CARTESIAN_POINT ( 'NONE',  ( -10.67658234375000070, 219.6093750017069794, 0.000000000000000000 ) ) ;
#71780=ORIENTED_EDGE ( 'NONE', *, *, #56695, .F. ) ;
#71816=CARTESIAN_POINT ( 'NONE',  ( -3.042071309553166181, 227.8645833367473301, -11.35316468749999608 ) ) ;
#71821=CARTESIAN_POINT ( 'NONE',  ( 10.00000000000000178, 262.2916666666666288, 2.679491924311222739 ) ) ;
#71826=CARTESIAN_POINT ( 'NONE',  ( 9.999999999999998224, 240.8333333401612890, -2.679491924311229401 ) ) ;
#71830=CARTESIAN_POINT ( 'NONE',  ( 4.999999999999997335, 261.4583333401613459, -8.660254037844387298 ) ) ;
#71847=VERTEX_POINT ( 'NONE', #39498 ) ;
#71852=CARTESIAN_POINT ( 'NONE',  ( 3.042071309553173286, 235.6770833367473017, 11.35316468749999608 ) ) ;
#71860=CARTESIAN_POINT ( 'NONE',  ( 3.115309517308847198, 219.9999999999999716, 10.23006779404638777 ) ) ;
#71865=ORIENTED_EDGE ( 'NONE', *, *, #25924, .T. ) ;
#71911=CARTESIAN_POINT ( 'NONE',  ( -3.042071309553166181, 233.1770833367473017, -11.35316468749999608 ) ) ;
#71917=CARTESIAN_POINT ( 'NONE',  ( -10.99999999999999645, 218.9106836093509116, 2.947441116742358425 ) ) ;
#71970=CARTESIAN_POINT ( 'NONE',  ( -9.999999999999998224, 238.3333333401613174, 2.679491924311235618 ) ) ;
#71972=VERTEX_POINT ( 'NONE', #23254 ) ;
#71992=CARTESIAN_POINT ( 'NONE',  ( -2.679491924311081963, 259.1666666734946034, 10.00000000000008171 ) ) ;
#71993=CARTESIAN_POINT ( 'NONE',  ( 8.311093377946834337, 262.0312500034139589, -8.311093377946836114 ) ) ;
#72055=CARTESIAN_POINT ( 'NONE',  ( 8.311093377946834337, 232.0312500034139873, -8.311093377946836114 ) ) ;
#72110=CARTESIAN_POINT ( 'NONE',  ( 8.311093377946834337, 252.3437500034139873, -8.311093377946836114 ) ) ;
#72162=CARTESIAN_POINT ( 'NONE',  ( -6.123233995736766282E-16, 231.8750000068279746, -10.00000000000000000 ) ) ;
#72172=( BOUNDED_CURVE ( )  B_SPLINE_CURVE ( 2, ( #58229, #74435, #10694, #57481, #28783, #5411, #17085, #51799, #17838, #46506, #147, #6528, #33727 ),
 .UNSPECIFIED., .F., .F. ) 
 B_SPLINE_CURVE_WITH_KNOTS ( ( 3, 2, 2, 2, 2, 2, 3 ),
 ( 0.2499999999999995837, 0.2592592592592588563, 0.2685185185185181567, 0.2777777777777774015, 0.2870370370370366464, 0.2962962962962958913, 0.3055555555555551916 ),
 .UNSPECIFIED. ) 
 CURVE ( )  GEOMETRIC_REPRESENTATION_ITEM ( )  RATIONAL_B_SPLINE_CURVE ( ( 1.000000000000001554, 0.9659258262890668689, 1.000000000000000000, 0.9659258262890683122, 1.000000000000000000, 0.9659258262890683122, 1.000000000000000000, 0.9659258262890683122, 1.000000000000000000, 0.9659258262890683122, 1.000000000000000000, 0.9659258262890697555, 0.9999999999999985567 ) ) 
 REPRESENTATION_ITEM ( '' )  );
#72198=CARTESIAN_POINT ( 'NONE',  ( 8.660254037844389075, 257.0833333333333144, 4.999999999999997335 ) ) ;
#72206=CARTESIAN_POINT ( 'NONE',  ( 9.999999999999998224, 260.8333333401612890, -2.679491924311229401 ) ) ;
#72211=VERTEX_POINT ( 'NONE', #73731 ) ;
#72241=ORIENTED_EDGE ( 'NONE', *, *, #30933, .F. ) ;
#72256=CARTESIAN_POINT ( 'NONE',  ( 2.679491924311168560, 238.5416666666666856, -10.00000000000003375 ) ) ;
#72289=CARTESIAN_POINT ( 'NONE',  ( 9.832129032723416984, 227.1354166700806729, -5.676582343750003368 ) ) ;
#72354=CARTESIAN_POINT ( 'NONE',  ( -2.679491924311228512, 237.0833333401613459, -9.999999999999998224 ) ) ;
#72355=CARTESIAN_POINT ( 'NONE',  ( -10.00000000000000000, 253.1250000068279746, 0.000000000000000000 ) ) ;
#72362=VECTOR ( 'NONE', #47397, 1000.000000000000000 ) ;
#72376=CARTESIAN_POINT ( 'NONE',  ( 8.311093377946839666, 255.7812500034139589, 8.311093377946830785 ) ) ;
#72380=CARTESIAN_POINT ( 'NONE',  ( 5.676582343750005144, 260.8854166700806445, 9.832129032723416984 ) ) ;
#72401=CARTESIAN_POINT ( 'NONE',  ( -5.000000000000000888, 242.2916666734946318, -8.660254037844387298 ) ) ;
#72405=CARTESIAN_POINT ( 'NONE',  ( -11.35316468749999608, 219.4270833367473301, 3.042071309553173730 ) ) ;
#72446=CARTESIAN_POINT ( 'NONE',  ( -11.35316468749999608, 239.1145833367473301, 3.042071309553173730 ) ) ;
#72472=CARTESIAN_POINT ( 'NONE',  ( 1.836970198721029589E-15, 234.3750000068279746, 10.00000000000000178 ) ) ;
#72486=EDGE_CURVE ( 'NONE', #3433, #67329, #58477, .T. ) ;
#72497=CARTESIAN_POINT ( 'NONE',  ( -3.042071309553159075, 255.2604166700806445, 11.35316468749999963 ) ) ;
#72558=LINE ( 'NONE', #31823, #70334 ) ;
#72580=CARTESIAN_POINT ( 'NONE',  ( -10.00000000000000000, 254.7916666666666856, -2.679491924311226292 ) ) ;
#72585=DIRECTION ( 'NONE',  ( 0.000000000000000000, 0.000000000000000000, 1.000000000000000000 ) ) ;
#72587=CARTESIAN_POINT ( 'NONE',  ( 8.660254037844389075, 252.0833333333333144, 4.999999999999997335 ) ) ;
#72617=CARTESIAN_POINT ( 'NONE',  ( 11.35316468749999608, 221.9270833367473017, -3.042071309553167513 ) ) ;
#72641=CARTESIAN_POINT ( 'NONE',  ( 1.836970198721029589E-15, 244.3750000068280031, 10.00000000000000000 ) ) ;
#72675=CARTESIAN_POINT ( 'NONE',  ( 11.35316468749999963, 256.1979166700806445, 3.042071309553159519 ) ) ;
#72708=CARTESIAN_POINT ( 'NONE',  ( -2.679491924311171225, 222.0833333401612890, -10.00000000000003197 ) ) ;
#72709=CARTESIAN_POINT ( 'NONE',  ( -5.676582343750000703, 258.3854166700806445, -9.832129032723418760 ) ) ;
#72737=CARTESIAN_POINT ( 'NONE',  ( 7.320508075688776373, 220.0000000068280031, 7.320508075688767491 ) ) ;
#72760=CARTESIAN_POINT ( 'NONE',  ( -9.832129032723415207, 259.3229166700806445, 5.676582343750005144 ) ) ;
#72763=CARTESIAN_POINT ( 'NONE',  ( 3.042071309553173286, 250.6770833367473017, 11.35316468749999608 ) ) ;
#72780=ORIENTED_EDGE ( 'NONE', *, *, #72486, .F. ) ;
#72822=CARTESIAN_POINT ( 'NONE',  ( 9.832129032723420536, 225.9895833367473585, 5.676582343749996262 ) ) ;
#72845=LINE ( 'NONE', #65314, #70383 ) ;
#72874=CARTESIAN_POINT ( 'NONE',  ( -8.311093377946836114, 258.5937500034140157, -8.311093377946836114 ) ) ;
#72922=CARTESIAN_POINT ( 'NONE',  ( -9.999999999999998224, 248.3333333401613174, 2.679491924311235174 ) ) ;
#72953=CARTESIAN_POINT ( 'NONE',  ( 8.311093377946834337, 222.0312500034139873, -8.311093377946836114 ) ) ;
#72959=CARTESIAN_POINT ( 'NONE',  ( 9.999999999999998224, 252.7083333333333712, -2.679491924311229401 ) ) ;
#72983=CARTESIAN_POINT ( 'NONE',  ( 0.000000000000000000, 0.000000000000000000, 0.000000000000000000 ) ) ;
#73037=CYLINDRICAL_SURFACE ( 'NONE', #3116, 10.00000000000000000 ) ;
#73039=CARTESIAN_POINT ( 'NONE',  ( 5.676582343750005144, 220.5729166700806729, 9.832129032723416984 ) ) ;
#73043=CARTESIAN_POINT ( 'NONE',  ( 11.35316468749999963, 261.4062500034140157, -1.390361679473963556E-15 ) ) ;
#73046=DIRECTION ( 'NONE',  ( -0.000000000000000000, -1.000000000000000000, -0.000000000000000000 ) ) ;
#73077=CARTESIAN_POINT ( 'NONE',  ( -11.35316468749999608, 259.4270833367472164, 3.042071309553173730 ) ) ;
#73104=CARTESIAN_POINT ( 'NONE',  ( 2.679491924311235174, 219.5833333401612890, 9.999999999999998224 ) ) ;
#73105=CARTESIAN_POINT ( 'NONE',  ( -6.123233995736766282E-16, 243.7500000000000284, -10.00000000000000000 ) ) ;
#73129=CARTESIAN_POINT ( 'NONE',  ( 5.676582343750005144, 255.5729166700806445, 9.832129032723416984 ) ) ;
#73133=CARTESIAN_POINT ( 'NONE',  ( -11.35316468749999963, 254.2187500034139873, 0.000000000000000000 ) ) ;
#73135=ORIENTED_EDGE ( 'NONE', *, *, #10394, .F. ) ;
#73194=CARTESIAN_POINT ( 'NONE',  ( -6.951808397369817780E-16, 227.6562500034139873, -11.35316468749999963 ) ) ;
#73217=ORIENTED_EDGE ( 'NONE', *, *, #33260, .T. ) ;
#73221=CARTESIAN_POINT ( 'NONE',  ( 5.000000000000004441, 234.7916666734946602, 8.660254037844385522 ) ) ;
#73246=CARTESIAN_POINT ( 'NONE',  ( -5.676582343750000703, 253.3854166700806445, -9.832129032723418760 ) ) ;
#73280=CARTESIAN_POINT ( 'NONE',  ( 11.35316468749999963, 261.1979166700807014, 3.042071309553159519 ) ) ;
#73290=CARTESIAN_POINT ( 'NONE',  ( 7.320508075688776373, 230.0000000068279462, 7.320508075688767491 ) ) ;
#73326=ORIENTED_EDGE ( 'NONE', *, *, #9654, .T. ) ;
#73327=CARTESIAN_POINT ( 'NONE',  ( 3.042071309553163960, 222.4479166700806729, -11.35316468749999785 ) ) ;
#73333=CARTESIAN_POINT ( 'NONE',  ( 8.660254037844385522, 247.9166666666666856, -5.000000000000003553 ) ) ;
#73340=CARTESIAN_POINT ( 'NONE',  ( 8.660254037844389075, 260.2083333401612890, 4.999999999999997335 ) ) ;
#73370=FACE_OUTER_BOUND ( 'NONE', #12518, .T. ) ;
#73382=CARTESIAN_POINT ( 'NONE',  ( 2.679491924311263151, 236.4583333333333144, 9.999999999999980460 ) ) ;
#73395=ORIENTED_EDGE ( 'NONE', *, *, #45783, .T. ) ;
#73413=CARTESIAN_POINT ( 'NONE',  ( 8.311093377946839666, 255.7812500034139589, 8.311093377946829008 ) ) ;
#73446=CARTESIAN_POINT ( 'NONE',  ( -3.042071309553166625, 253.1770833367473301, -11.35316468749999608 ) ) ;
#73470=CARTESIAN_POINT ( 'NONE',  ( -5.000000000000000888, 222.2916666734946602, -8.660254037844387298 ) ) ;
#73471=CARTESIAN_POINT ( 'NONE',  ( -8.660254037844387298, 252.7083333401612890, -4.999999999999999112 ) ) ;
#73493=CARTESIAN_POINT ( 'NONE',  ( 11.35316468749999963, 246.4062500034139873, -1.390361679473963556E-15 ) ) ;
#73497=CARTESIAN_POINT ( 'NONE',  ( 9.832129032723416984, 252.1354166700806445, -5.676582343750003368 ) ) ;
#73510=AXIS2_PLACEMENT_3D ( 'NONE', #64046, #1062, #12356 ) ;
#73560=CARTESIAN_POINT ( 'NONE',  ( -5.676582343749992710, 224.7395833367473301, 9.832129032723422313 ) ) ;
#73611=CARTESIAN_POINT ( 'NONE',  ( -5.676582343750000703, 238.3854166700806445, -9.832129032723418760 ) ) ;
#73639=DIRECTION ( 'NONE',  ( 0.000000000000000000, 0.000000000000000000, -1.000000000000000000 ) ) ;
#73648=CARTESIAN_POINT ( 'NONE',  ( -6.951808397369817780E-16, 257.6562500034140157, -11.35316468749999963 ) ) ;
#73655=CARTESIAN_POINT ( 'NONE',  ( 2.679491924311234730, 229.5833333401612890, 9.999999999999998224 ) ) ;
#73697=CARTESIAN_POINT ( 'NONE',  ( 5.000000000000004441, 236.6666666666666856, 8.660254037844385522 ) ) ;
#73728=CARTESIAN_POINT ( 'NONE',  ( -8.311093377946834337, 219.8437500034139873, 8.311093377946837890 ) ) ;
#73731=CARTESIAN_POINT ( 'NONE',  ( 1.836970198721029589E-15, 221.2500000000000000, 10.00000000000000000 ) ) ;
#73754=CYLINDRICAL_SURFACE ( 'NONE', #42493, 10.00000000000000000 ) ;
#73780=VERTEX_POINT ( 'NONE', #49239 ) ;
#73781=CARTESIAN_POINT ( 'NONE',  ( -9.832129032723415207, 219.6354166700806445, 5.676582343750005144 ) ) ;
#73784=CARTESIAN_POINT ( 'NONE',  ( -10.09417438056707006, 220.0000000000001137, 1.602760042864921353 ) ) ;
#73816=CARTESIAN_POINT ( 'NONE',  ( 11.35316468749999963, 261.5104166700807014, 3.042071309553159519 ) ) ;
#73843=CARTESIAN_POINT ( 'NONE',  ( -2.679491924311228512, 222.0833333401613174, -9.999999999999998224 ) ) ;
#73870=CARTESIAN_POINT ( 'NONE',  ( -8.311093377946834337, 244.5312500034139589, 8.311093377946837890 ) ) ;
#73875=CARTESIAN_POINT ( 'NONE',  ( -11.35316468749999608, 249.4270833367472733, 3.042071309553173730 ) ) ;
#73933=CARTESIAN_POINT ( 'NONE',  ( -3.042071309553159075, 224.9479166700806445, 11.35316468749999963 ) ) ;
#73985=CARTESIAN_POINT ( 'NONE',  ( -3.042071309553166181, 238.1770833367473301, -11.35316468749999608 ) ) ;
#74025=ORIENTED_EDGE ( 'NONE', *, *, #32187, .T. ) ;
#74052=CARTESIAN_POINT ( 'NONE',  ( 1.224646799147353256E-15, 0.000000000000000000, 10.00000000000000000 ) ) ;
#74070=CARTESIAN_POINT ( 'NONE',  ( 7.320508075688776373, 231.8750000000000000, 7.320508075688767491 ) ) ;
#74097=ORIENTED_EDGE ( 'NONE', *, *, #37000, .T. ) ;
#74113=FACE_OUTER_BOUND ( 'NONE', #15541, .T. ) ;
#74140=CARTESIAN_POINT ( 'NONE',  ( 2.679491924311176998, 249.5833333401612890, 10.00000000000003197 ) ) ;
#74152=CARTESIAN_POINT ( 'NONE',  ( -6.951808397369817780E-16, 242.6562500034140157, -11.35316468749999963 ) ) ;
#74186=CARTESIAN_POINT ( 'NONE',  ( -11.35316468749999963, 264.2187500034140157, 0.000000000000000000 ) ) ;
#74216=CARTESIAN_POINT ( 'NONE',  ( 10.00000000000000178, 220.4166666734946318, 2.679491924311222739 ) ) ;
#74241=CARTESIAN_POINT ( 'NONE',  ( -5.676582343750000703, 248.0729166700806729, -9.832129032723418760 ) ) ;
#74245=CARTESIAN_POINT ( 'NONE',  ( 11.35316468749999963, 246.7187500034139873, -1.390361679473963556E-15 ) ) ;
#74306=CARTESIAN_POINT ( 'NONE',  ( 8.660254037844385522, 261.0416666734946602, -5.000000000000003553 ) ) ;
#74325=CARTESIAN_POINT ( 'NONE',  ( 7.320508075688776373, 221.8750000000000284, 7.320508075688767491 ) ) ;
#74351=CARTESIAN_POINT ( 'NONE',  ( 3.042071309553163960, 247.7604166700806161, -11.35316468749999785 ) ) ;
#74387=CARTESIAN_POINT ( 'NONE',  ( 9.999999999999998224, 225.8333333401612606, -2.679491924311229401 ) ) ;
#74389=CARTESIAN_POINT ( 'NONE',  ( 11.35316468749999963, 261.4062500034140157, -1.390361679473963556E-15 ) ) ;
#74435=CARTESIAN_POINT ( 'NONE',  ( 2.679491924311117934, 253.5416666666666572, -10.00000000000006217 ) ) ;
#74440=CARTESIAN_POINT ( 'NONE',  ( 9.999999999999998224, 237.7083333333333144, -2.679491924311229401 ) ) ;
#74441=LINE ( 'NONE', #6164, #43902 ) ;
#74478=CARTESIAN_POINT ( 'NONE',  ( 10.00000000000000000, 247.5000000000000000, -1.224646799147353256E-15 ) ) ;
#74511=CARTESIAN_POINT ( 'NONE',  ( 4.999999999999997335, 251.4583333401613174, -8.660254037844387298 ) ) ;
#74528=CARTESIAN_POINT ( 'NONE',  ( -8.311093377946836114, 238.2812500034140157, -8.311093377946836114 ) ) ;
#74557=CARTESIAN_POINT ( 'NONE',  ( -5.000000000000000888, 224.1666666666666856, -8.660254037844387298 ) ) ;
#74564=CARTESIAN_POINT ( 'NONE',  ( -3.042071309553166625, 238.1770833367473017, -11.35316468749999608 ) ) ;
#74618=CARTESIAN_POINT ( 'NONE',  ( 8.311093377946834337, 242.0312500034139873, -8.311093377946836114 ) ) ;
#74623=CARTESIAN_POINT ( 'NONE',  ( 2.085542519210945334E-15, 235.4687500034139873, 11.35316468749999963 ) ) ;
#74686=COLOUR_RGB('Sky Blue',0.24,0.69,0.87);
#74687=FILL_AREA_STYLE_COLOUR('',#74686);
#74688=FILL_AREA_STYLE('',(#74687));
#74689=SURFACE_STYLE_FILL_AREA(#74688);
#74690=SURFACE_SIDE_STYLE('',(#74689));
#74691=SURFACE_STYLE_USAGE(.BOTH.,#74690);
#74692=PRESENTATION_STYLE_ASSIGNMENT((#74691));
ENDSEC;
END-ISO-10303-21;
